ISO-10303-21;
HEADER;
FILE_DESCRIPTION (('STEP AP203'),
    '1' );
FILE_NAME ('Plastic Part 1.step',
    '2026-10-08T23:54:15',
    ( '' ),
    ( '' ),
    'SwSTEP 2.0',
    'SolidWorks 2024',
    '' );
FILE_SCHEMA (( 'AUTOMOTIVE_DESIGN' ));
ENDSEC;

DATA;
#2=VECTOR ( 'NONE', #18887, 1000.000000000000000 ) ;
#3=CARTESIAN_POINT ( 'NONE',  ( -28.32169924589829080, 0.3587747205143964613, -8.244178532169451401 ) ) ;
#31=CARTESIAN_POINT ( 'NONE',  ( -4.993225604111834137, 0.3587747205143964613, -29.11654937215279304 ) ) ;
#47=DIRECTION ( 'NONE',  ( 0.000000000000000000, 1.000000000000000000, 0.000000000000000000 ) ) ;
#49=EDGE_CURVE ( 'NONE', #39472, #30477, #6341, .T. ) ;
#52=EDGE_CURVE ( 'NONE', #64249, #62056, #30271, .T. ) ;
#88=CARTESIAN_POINT ( 'NONE',  ( 30.93860345374796594, 0.6647747205144265426, 28.83647319851474933 ) ) ;
#92=CYLINDRICAL_SURFACE ( 'NONE', #60343, 8.452410033082761842 ) ;
#122=CARTESIAN_POINT ( 'NONE',  ( 14.83405752585718496, 4.881907540129191148, -27.54622755360254516 ) ) ;
#138=CARTESIAN_POINT ( 'NONE',  ( 33.74607884027702909, -5.965225279485572685, -4.999864028243830916 ) ) ;
#147=DIRECTION ( 'NONE',  ( 0.6599726524652350657, 0.000000000000000000, -0.7512896232465892110 ) ) ;
#149=VERTEX_POINT ( 'NONE', #67859 ) ;
#162=LINE ( 'NONE', #7772, #59931 ) ;
#169=ORIENTED_EDGE ( 'NONE', *, *, #41304, .T. ) ;
#171=EDGE_CURVE ( 'NONE', #82004, #10266, #15546, .T. ) ;
#181=CARTESIAN_POINT ( 'NONE',  ( 32.95642386911166710, 3.601225610321291182, -13.01540364303327380 ) ) ;
#187=CARTESIAN_POINT ( 'NONE',  ( 1.305682803664691249, -5.965225279485572685, 29.57950906855421991 ) ) ;
#191=CARTESIAN_POINT ( 'NONE',  ( 16.26279755680690542, -6.475225279485573360, -27.67997040356620531 ) ) ;
#226=ORIENTED_EDGE ( 'NONE', *, *, #92027, .F. ) ;
#242=ORIENTED_EDGE ( 'NONE', *, *, #44768, .T. ) ;
#251=EDGE_LOOP ( 'NONE', ( #52195, #19336, #31483, #49094, #27965, #14246, #22960, #25333, #21362, #63679, #17102, #94843, #14089, #95653, #36853, #77118, #64971, #20831, #46153, #91222, #51880, #19595, #36808, #17745, #12211, #19237, #59711, #42959 ) ) ;
#259=EDGE_LOOP ( 'NONE', ( #70483, #94459, #10754, #74894, #15740 ) ) ;
#271=CIRCLE ( 'NONE', #60197, 22.69500000000000384 ) ;
#279=LINE ( 'NONE', #14000, #91749 ) ;
#282=CARTESIAN_POINT ( 'NONE',  ( 30.53060340732036337, 1.682774720514426114, -1.352392034746782823 ) ) ;
#288=CARTESIAN_POINT ( 'NONE',  ( 30.09341516180546350, 1.682774720514426114, -11.39311774897855756 ) ) ;
#304=ORIENTED_EDGE ( 'NONE', *, *, #22085, .F. ) ;
#311=LINE ( 'NONE', #38370, #36067 ) ;
#312=DIRECTION ( 'NONE',  ( -0.9994733861282923959, -0.000000000000000000, -0.03244919754393515293 ) ) ;
#313=EDGE_CURVE ( 'NONE', #82268, #35739, #55515, .T. ) ;
#316=DIRECTION ( 'NONE',  ( 0.000000000000000000, 0.000000000000000000, -1.000000000000000000 ) ) ;
#330=DIRECTION ( 'NONE',  ( -0.000000000000000000, -0.000000000000000000, -1.000000000000000000 ) ) ;
#344=CARTESIAN_POINT ( 'NONE',  ( 30.59073162224239084, 4.540774720514408891, 26.30400772315274338 ) ) ;
#356=AXIS2_PLACEMENT_3D ( 'NONE', #17788, #64990, #90170 ) ;
#386=LINE ( 'NONE', #63821, #6032 ) ;
#391=ORIENTED_EDGE ( 'NONE', *, *, #52, .F. ) ;
#393=CARTESIAN_POINT ( 'NONE',  ( -28.98875734969026396, -5.965225279485572685, -0.08597719988137648983 ) ) ;
#396=VERTEX_POINT ( 'NONE', #32781 ) ;
#397=CARTESIAN_POINT ( 'NONE',  ( -0.02075734969026423599, 0.3587747205144213303, -0.08597719988137648983 ) ) ;
#399=AXIS2_PLACEMENT_3D ( 'NONE', #34022, #78666, #9681 ) ;
#406=DIRECTION ( 'NONE',  ( 0.000000000000000000, 1.000000000000000000, -0.000000000000000000 ) ) ;
#415=EDGE_CURVE ( 'NONE', #68317, #49971, #89571, .T. ) ;
#436=VECTOR ( 'NONE', #75067, 1000.000000000000000 ) ;
#446=CARTESIAN_POINT ( 'NONE',  ( 27.86270917940689174, -5.965225279485572685, 29.49402280011862487 ) ) ;
#460=EDGE_CURVE ( 'NONE', #77487, #13521, #16037, .T. ) ;
#475=DIRECTION ( 'NONE',  ( -0.9496245541219268116, -6.454799914155188842E-16, -0.3133898629642187239 ) ) ;
#505=ORIENTED_EDGE ( 'NONE', *, *, #37962, .F. ) ;
#509=EDGE_LOOP ( 'NONE', ( #49662, #42848, #63810, #16595 ) ) ;
#522=EDGE_CURVE ( 'NONE', #9188, #31632, #19306, .T. ) ;
#573=B_SPLINE_CURVE_WITH_KNOTS ( 'NONE', 3,
 ( #10709, #72616, #34049, #51647, #59764, #80721 ),
 .UNSPECIFIED., .F., .F.,
 ( 4, 2, 4 ),
 ( 0.07528258264012024914, 0.07727090165436052704, 0.07925922066860080495 ),
 .UNSPECIFIED. ) ;
#576=ORIENTED_EDGE ( 'NONE', *, *, #40914, .F. ) ;
#587=CARTESIAN_POINT ( 'NONE',  ( 15.63605935613269438, -6.475225279485573360, -27.55169773172585934 ) ) ;
#598=CARTESIAN_POINT ( 'NONE',  ( 0.000000000000000000, -1.473225279485573802, 0.000000000000000000 ) ) ;
#610=VECTOR ( 'NONE', #64166, 1000.000000000000000 ) ;
#627=EDGE_LOOP ( 'NONE', ( #68451, #54996, #83617, #2674, #2516, #91000, #34023, #57845, #97952, #9654, #26816, #51309 ) ) ;
#628=VERTEX_POINT ( 'NONE', #45401 ) ;
#634=EDGE_CURVE ( 'NONE', #82156, #32410, #91059, .T. ) ;
#654=VERTEX_POINT ( 'NONE', #37281 ) ;
#664=CYLINDRICAL_SURFACE ( 'NONE', #80009, 2.040000000000000036 ) ;
#665=EDGE_CURVE ( 'NONE', #22596, #17009, #37775, .T. ) ;
#676=AXIS2_PLACEMENT_3D ( 'NONE', #42786, #67617, #36160 ) ;
#680=EDGE_CURVE ( 'NONE', #63086, #95598, #33946, .T. ) ;
#687=VECTOR ( 'NONE', #5114, 1000.000000000000000 ) ;
#714=CIRCLE ( 'NONE', #18542, 2.249999999999998668 ) ;
#747=CARTESIAN_POINT ( 'NONE',  ( 16.26279755680690542, 1.684774720514426560, -27.67997040356620531 ) ) ;
#750=DIRECTION ( 'NONE',  ( 1.286817348990133162E-16, 0.000000000000000000, -1.000000000000000000 ) ) ;
#763=CARTESIAN_POINT ( 'NONE',  ( -10.28806225508158612, 4.941275956067651798, 28.69510307482446976 ) ) ;
#770=ORIENTED_EDGE ( 'NONE', *, *, #77456, .F. ) ;
#774=ORIENTED_EDGE ( 'NONE', *, *, #31657, .T. ) ;
#781=ORIENTED_EDGE ( 'NONE', *, *, #1325, .T. ) ;
#783=DIRECTION ( 'NONE',  ( 6.030048488936326810E-14, 0.000000000000000000, -1.000000000000000000 ) ) ;
#795=DIRECTION ( 'NONE',  ( 0.000000000000000000, 0.000000000000000000, -1.000000000000000000 ) ) ;
#796=ORIENTED_EDGE ( 'NONE', *, *, #76715, .T. ) ;
#797=EDGE_LOOP ( 'NONE', ( #41880, #27016, #53336, #74875 ) ) ;
#800=ADVANCED_FACE ( 'NONE', ( #47892 ), #62620, .T. ) ;
#804=CARTESIAN_POINT ( 'NONE',  ( 31.79364159983995464, -5.965225279485572685, -11.59305536555894278 ) ) ;
#813=PLANE ( 'NONE',  #66018 ) ;
#871=VERTEX_POINT ( 'NONE', #10823 ) ;
#899=ORIENTED_EDGE ( 'NONE', *, *, #89411, .F. ) ;
#902=ORIENTED_EDGE ( 'NONE', *, *, #44602, .F. ) ;
#904=ORIENTED_EDGE ( 'NONE', *, *, #47832, .F. ) ;
#905=VECTOR ( 'NONE', #69263, 1000.000000000000227 ) ;
#913=CARTESIAN_POINT ( 'NONE',  ( -4.929522925832171332, 6.376774720514426953, -28.63504101147569614 ) ) ;
#921=CARTESIAN_POINT ( 'NONE',  ( 0.000000000000000000, 4.772774720514425972, 0.000000000000000000 ) ) ;
#952=LINE ( 'NONE', #47638, #10957 ) ;
#959=CARTESIAN_POINT ( 'NONE',  ( 30.53060340732035982, 4.594240983522013266, 19.84760796525321780 ) ) ;
#968=ORIENTED_EDGE ( 'NONE', *, *, #28936, .T. ) ;
#977=VECTOR ( 'NONE', #82147, 1000.000000000000000 ) ;
#984=ORIENTED_EDGE ( 'NONE', *, *, #31906, .F. ) ;
#985=FACE_OUTER_BOUND ( 'NONE', #37343, .T. ) ;
#1000=ORIENTED_EDGE ( 'NONE', *, *, #17276, .T. ) ;
#1028=LINE ( 'NONE', #84756, #39864 ) ;
#1034=CARTESIAN_POINT ( 'NONE',  ( 33.74607884027702909, 0.3587747205144265483, -4.999864028243830916 ) ) ;
#1046=EDGE_CURVE ( 'NONE', #8729, #14476, #30027, .T. ) ;
#1052=CARTESIAN_POINT ( 'NONE',  ( 22.81105451610979173, 1.684774720501991618, -20.71691820600746681 ) ) ;
#1053=VECTOR ( 'NONE', #44095, 1000.000000000000000 ) ;
#1057=ORIENTED_EDGE ( 'NONE', *, *, #25862, .T. ) ;
#1058=DIRECTION ( 'NONE',  ( -1.000000000000000000, 8.503546450866701308E-16, 0.000000000000000000 ) ) ;
#1069=DIRECTION ( 'NONE',  ( 0.000000000000000000, 0.000000000000000000, -1.000000000000000000 ) ) ;
#1084=AXIS2_PLACEMENT_3D ( 'NONE', #98728, #67807, #14988 ) ;
#1085=DIRECTION ( 'NONE',  ( 0.000000000000000000, 0.000000000000000000, -1.000000000000000000 ) ) ;
#1092=DIRECTION ( 'NONE',  ( -0.9913618264504691080, -4.164321980682960499E-15, 0.1311553622875927805 ) ) ;
#1113=AXIS2_PLACEMENT_3D ( 'NONE', #3266, #34207, #17467 ) ;
#1121=CARTESIAN_POINT ( 'NONE',  ( 31.69157588112856061, 3.316774720514426456, 29.47507169338741662 ) ) ;
#1123=DIRECTION ( 'NONE',  ( 0.000000000000000000, 0.000000000000000000, -1.000000000000000000 ) ) ;
#1131=FACE_OUTER_BOUND ( 'NONE', #52472, .T. ) ;
#1149=PLANE ( 'NONE',  #75563 ) ;
#1157=AXIS2_PLACEMENT_3D ( 'NONE', #37386, #99268, #29766 ) ;
#1160=CARTESIAN_POINT ( 'NONE',  ( -27.96875734969026084, 3.316774720514426456, 24.50402280011861933 ) ) ;
#1175=CARTESIAN_POINT ( 'NONE',  ( 27.86270917940689174, -5.965225279485572685, 29.49402280011862487 ) ) ;
#1187=CIRCLE ( 'NONE', #28779, 8.452410033082761842 ) ;
#1217=DIRECTION ( 'NONE',  ( 0.000000000000000000, -0.000000000000000000, -1.000000000000000000 ) ) ;
#1227=AXIS2_PLACEMENT_3D ( 'NONE', #5527, #58831, #28368 ) ;
#1232=AXIS2_PLACEMENT_3D ( 'NONE', #93901, #55360, #86291 ) ;
#1258=DIRECTION ( 'NONE',  ( 0.000000000000000000, -1.000000000000000000, 0.000000000000000000 ) ) ;
#1261=DIRECTION ( 'NONE',  ( -0.000000000000000000, -1.000000000000000000, 8.393823270855534040E-16 ) ) ;
#1262=ORIENTED_EDGE ( 'NONE', *, *, #73493, .T. ) ;
#1280=LINE ( 'NONE', #40333, #30253 ) ;
#1316=ORIENTED_EDGE ( 'NONE', *, *, #313, .T. ) ;
#1318=DIRECTION ( 'NONE',  ( 0.000000000000000000, 0.000000000000000000, 1.000000000000000000 ) ) ;
#1325=EDGE_CURVE ( 'NONE', #86005, #27949, #1355, .T. ) ;
#1355=CIRCLE ( 'NONE', #96950, 0.8160000000000007248 ) ;
#1365=ORIENTED_EDGE ( 'NONE', *, *, #57930, .F. ) ;
#1375=ORIENTED_EDGE ( 'NONE', *, *, #44564, .F. ) ;
#1376=CARTESIAN_POINT ( 'NONE',  ( -23.29179552176161749, -5.965225279485594001, -17.29637630388738501 ) ) ;
#1397=ORIENTED_EDGE ( 'NONE', *, *, #93110, .F. ) ;
#1402=CARTESIAN_POINT ( 'NONE',  ( 29.72843915439144524, 4.948038888671026037, 27.41656699113896067 ) ) ;
#1422=CARTESIAN_POINT ( 'NONE',  ( -22.05275734969026047, -5.965225279485572685, 31.02402280011862246 ) ) ;
#1428=DIRECTION ( 'NONE',  ( 0.000000000000000000, 0.000000000000000000, -1.000000000000000000 ) ) ;
#1450=CARTESIAN_POINT ( 'NONE',  ( 13.10664265030973930, -5.965225279485574461, -28.64597719988137570 ) ) ;
#1451=ADVANCED_FACE ( 'NONE', ( #44158 ), #51271, .T. ) ;
#1452=CARTESIAN_POINT ( 'NONE',  ( 5.717289507243528135, 5.356774720514425603, -25.39219853617310818 ) ) ;
#1456=CARTESIAN_POINT ( 'NONE',  ( -28.98875734969026041, 0.3587747205144262708, 23.37402280011862743 ) ) ;
#1465=VECTOR ( 'NONE', #98941, 1000.000000000000000 ) ;
#1481=VECTOR ( 'NONE', #77699, 1000.000000000000114 ) ;
#1487=CARTESIAN_POINT ( 'NONE',  ( 33.62145766639996936, 4.037870770857261427, -12.08356088300365094 ) ) ;
#1495=DIRECTION ( 'NONE',  ( -1.000000000000000000, 0.000000000000000000, -0.000000000000000000 ) ) ;
#1500=DIRECTION ( 'NONE',  ( 0.000000000000000000, -1.000000000000000000, 0.000000000000000000 ) ) ;
#1530=CIRCLE ( 'NONE', #50136, 129.7684398600581517 ) ;
#1533=CARTESIAN_POINT ( 'NONE',  ( 0.000000000000000000, 0.000000000000000000, 0.000000000000000000 ) ) ;
#1537=DIRECTION ( 'NONE',  ( 0.000000000000000000, 1.000000000000000000, 0.000000000000000000 ) ) ;
#1545=EDGE_LOOP ( 'NONE', ( #3931, #75255, #37132, #55953 ) ) ;
#1553=VERTEX_POINT ( 'NONE', #35052 ) ;
#1568=EDGE_CURVE ( 'NONE', #47577, #88761, #77083, .T. ) ;
#1575=EDGE_CURVE ( 'NONE', #63086, #27656, #38036, .T. ) ;
#1581=ORIENTED_EDGE ( 'NONE', *, *, #99852, .F. ) ;
#1596=CARTESIAN_POINT ( 'NONE',  ( 12.30588647384254841, 6.376774720514765349, -28.11066263748569227 ) ) ;
#1611=CIRCLE ( 'NONE', #19412, 2.499999999999995115 ) ;
#1627=EDGE_CURVE ( 'NONE', #80644, #84008, #23034, .T. ) ;
#1629=PLANE ( 'NONE',  #59842 ) ;
#1640=ORIENTED_EDGE ( 'NONE', *, *, #69436, .T. ) ;
#1658=CARTESIAN_POINT ( 'NONE',  ( 29.60442047479375205, 4.849628492681046232, 28.81422082199668466 ) ) ;
#1661=ORIENTED_EDGE ( 'NONE', *, *, #46484, .T. ) ;
#1663=CIRCLE ( 'NONE', #43810, 28.96799999999999287 ) ;
#1668=ORIENTED_EDGE ( 'NONE', *, *, #36947, .T. ) ;
#1674=DIRECTION ( 'NONE',  ( 0.06916465693916189206, 0.000000000000000000, -0.9976052577199502336 ) ) ;
#1677=ORIENTED_EDGE ( 'NONE', *, *, #1568, .T. ) ;
#1678=CARTESIAN_POINT ( 'NONE',  ( 26.73860345374794534, 5.058662225110310828, -7.113848178280766099 ) ) ;
#1682=AXIS2_PLACEMENT_3D ( 'NONE', #43986, #21135, #36874 ) ;
#1691=DIRECTION ( 'NONE',  ( -0.000000000000000000, 1.000000000000000000, -0.000000000000000000 ) ) ;
#1702=CARTESIAN_POINT ( 'NONE',  ( 17.51792015816173986, 0.3587747205144265483, 29.01255224319336889 ) ) ;
#1708=CARTESIAN_POINT ( 'NONE',  ( -20.27875734969026311, -6.143225279485574397, 24.00402280011862288 ) ) ;
#1711=LINE ( 'NONE', #94044, #69902 ) ;
#1724=ORIENTED_EDGE ( 'NONE', *, *, #96724, .T. ) ;
#1740=DIRECTION ( 'NONE',  ( 0.000000000000000000, -1.478457507934778393E-16, -1.000000000000000000 ) ) ;
#1742=ORIENTED_EDGE ( 'NONE', *, *, #17484, .T. ) ;
#1745=CARTESIAN_POINT ( 'NONE',  ( -10.27747606359964117, 6.067502657846070235, 28.80925224784997596 ) ) ;
#1766=DIRECTION ( 'NONE',  ( -0.000000000000000000, 0.000000000000000000, -1.000000000000000000 ) ) ;
#1779=CARTESIAN_POINT ( 'NONE',  ( -4.926336369345164279, -5.965225279485592225, -28.61095484066304451 ) ) ;
#1803=ORIENTED_EDGE ( 'NONE', *, *, #95268, .T. ) ;
#1805=CARTESIAN_POINT ( 'NONE',  ( -0.02075734969026423599, 5.866774720514426278, -0.08597719988137648983 ) ) ;
#1823=CARTESIAN_POINT ( 'NONE',  ( 4.784292611721462585, 5.356774720514426491, -25.54547254883130947 ) ) ;
#1845=DIRECTION ( 'NONE',  ( 0.000000000000000000, 0.000000000000000000, -1.000000000000000000 ) ) ;
#1866=DIRECTION ( 'NONE',  ( -0.4009304992412300317, 0.000000000000000000, -0.9161084732596779245 ) ) ;
#1870=CARTESIAN_POINT ( 'NONE',  ( 22.02124265030973760, 3.456774720514426136, 16.20402280011862217 ) ) ;
#1883=DIRECTION ( 'NONE',  ( 0.000000000000000000, 0.000000000000000000, -1.000000000000000000 ) ) ;
#1897=ADVANCED_FACE ( 'NONE', ( #59646 ), #90575, .F. ) ;
#1900=LINE ( 'NONE', #17617, #87082 ) ;
#1910=ADVANCED_FACE ( 'NONE', ( #40786 ), #24000, .F. ) ;
#1916=CARTESIAN_POINT ( 'NONE',  ( -23.59123376470063960, -6.143225279485574397, 24.50402280011862288 ) ) ;
#1926=ORIENTED_EDGE ( 'NONE', *, *, #65751, .F. ) ;
#1931=ORIENTED_EDGE ( 'NONE', *, *, #33555, .F. ) ;
#1932=ORIENTED_EDGE ( 'NONE', *, *, #1575, .F. ) ;
#1933=LINE ( 'NONE', #72445, #9402 ) ;
#1964=EDGE_CURVE ( 'NONE', #96941, #43106, #43511, .T. ) ;
#1971=ORIENTED_EDGE ( 'NONE', *, *, #86242, .F. ) ;
#1987=CARTESIAN_POINT ( 'NONE',  ( 33.60604063885286052, 3.409250796720436405, -11.91850954671862617 ) ) ;
#1988=CARTESIAN_POINT ( 'NONE',  ( 30.56715118582953750, -3.660718435927268199, 25.08875473125879196 ) ) ;
#2003=VECTOR ( 'NONE', #55101, 1000.000000000000000 ) ;
#2018=ORIENTED_EDGE ( 'NONE', *, *, #67379, .F. ) ;
#2021=CYLINDRICAL_SURFACE ( 'NONE', #83816, 3.349999999999998757 ) ;
#2040=CARTESIAN_POINT ( 'NONE',  ( 13.10664265030973930, 0.3587747205144256601, -28.18129937523770678 ) ) ;
#2052=ORIENTED_EDGE ( 'NONE', *, *, #7371, .T. ) ;
#2057=ORIENTED_EDGE ( 'NONE', *, *, #13555, .T. ) ;
#2061=ORIENTED_EDGE ( 'NONE', *, *, #19177, .F. ) ;
#2089=CARTESIAN_POINT ( 'NONE',  ( 30.93860345374796594, 0.000000000000000000, 0.000000000000000000 ) ) ;
#2092=DIRECTION ( 'NONE',  ( 1.000000000000000000, 0.000000000000000000, -0.000000000000000000 ) ) ;
#2095=DIRECTION ( 'NONE',  ( -1.000000000000000000, 0.000000000000000000, -1.334402673828313586E-16 ) ) ;
#2099=AXIS2_PLACEMENT_3D ( 'NONE', #91241, #21714, #52688 ) ;
#2118=ORIENTED_EDGE ( 'NONE', *, *, #28634, .T. ) ;
#2119=AXIS2_PLACEMENT_3D ( 'NONE', #53883, #84815, #46262 ) ;
#2131=VERTEX_POINT ( 'NONE', #99540 ) ;
#2135=CARTESIAN_POINT ( 'NONE',  ( 31.63443928675788186, 3.712996582965905290, 27.28441363938236464 ) ) ;
#2141=CARTESIAN_POINT ( 'NONE',  ( 32.16024265030974050, 0.3587747205144265483, 14.03360796525321774 ) ) ;
#2142=EDGE_CURVE ( 'NONE', #14697, #92497, #66653, .T. ) ;
#2147=ORIENTED_EDGE ( 'NONE', *, *, #88168, .F. ) ;
#2168=CARTESIAN_POINT ( 'NONE',  ( 29.72131469344797239, 6.278265095287072661, 26.95488797742164877 ) ) ;
#2173=FACE_BOUND ( 'NONE', #61977, .T. ) ;
#2189=ORIENTED_EDGE ( 'NONE', *, *, #49385, .T. ) ;
#2191=VECTOR ( 'NONE', #64908, 1000.000000000000000 ) ;
#2209=DIRECTION ( 'NONE',  ( 0.000000000000000000, 0.000000000000000000, 1.000000000000000000 ) ) ;
#2219=EDGE_CURVE ( 'NONE', #88543, #23364, #47286, .T. ) ;
#2228=DIRECTION ( 'NONE',  ( -0.000000000000000000, -0.000000000000000000, -1.000000000000000000 ) ) ;
#2233=ORIENTED_EDGE ( 'NONE', *, *, #82441, .F. ) ;
#2255=DIRECTION ( 'NONE',  ( 1.000000000000000000, -0.000000000000000000, -0.000000000000000000 ) ) ;
#2263=TOROIDAL_SURFACE ( 'NONE', #81645, 3.060000000000000053, 2.040000000000000036 ) ;
#2271=ORIENTED_EDGE ( 'NONE', *, *, #46204, .T. ) ;
#2278=EDGE_CURVE ( 'NONE', #39077, #4955, #63023, .T. ) ;
#2281=CARTESIAN_POINT ( 'NONE',  ( 33.00535138976609062, 6.376774720514426953, -12.97242311383962310 ) ) ;
#2324=ORIENTED_EDGE ( 'NONE', *, *, #70695, .F. ) ;
#2337=CARTESIAN_POINT ( 'NONE',  ( 14.43441819135929371, 3.316774720514426456, -28.36222020317710246 ) ) ;
#2356=CARTESIAN_POINT ( 'NONE',  ( 15.34241074214975065, 3.824162593742471028, -28.48848699765728654 ) ) ;
#2360=AXIS2_PLACEMENT_3D ( 'NONE', #22404, #52883, #54385 ) ;
#2369=AXIS2_PLACEMENT_3D ( 'NONE', #52296, #76606, #54306 ) ;
#2379=ORIENTED_EDGE ( 'NONE', *, *, #13484, .F. ) ;
#2386=ORIENTED_EDGE ( 'NONE', *, *, #88943, .F. ) ;
#2387=DIRECTION ( 'NONE',  ( -0.000000000000000000, -1.000000000000000000, -0.000000000000000000 ) ) ;
#2398=EDGE_CURVE ( 'NONE', #98622, #77754, #49300, .T. ) ;
#2415=ORIENTED_EDGE ( 'NONE', *, *, #58727, .F. ) ;
#2419=ORIENTED_EDGE ( 'NONE', *, *, #37289, .T. ) ;
#2430=CARTESIAN_POINT ( 'NONE',  ( -20.77875734969026311, -6.143225279485574397, 29.49402280011862487 ) ) ;
#2434=ORIENTED_EDGE ( 'NONE', *, *, #83260, .T. ) ;
#2441=PLANE ( 'NONE',  #77560 ) ;
#2453=FACE_OUTER_BOUND ( 'NONE', #97474, .T. ) ;
#2464=CARTESIAN_POINT ( 'NONE',  ( -29.49875734969026198, 0.3587747205144265483, 10.11402280011862587 ) ) ;
#2475=CARTESIAN_POINT ( 'NONE',  ( 22.81105451610979173, 2.682774720514426559, -18.46691820600746681 ) ) ;
#2478=AXIS2_PLACEMENT_3D ( 'NONE', #78693, #15304, #69611 ) ;
#2489=EDGE_CURVE ( 'NONE', #54228, #47065, #63254, .T. ) ;
#2491=ORIENTED_EDGE ( 'NONE', *, *, #78685, .F. ) ;
#2492=DIRECTION ( 'NONE',  ( 0.000000000000000000, 0.000000000000000000, -1.000000000000000000 ) ) ;
#2516=ORIENTED_EDGE ( 'NONE', *, *, #61885, .F. ) ;
#2517=CARTESIAN_POINT ( 'NONE',  ( 22.02124265030973760, 3.456774720514426136, 17.35402280011862786 ) ) ;
#2518=CARTESIAN_POINT ( 'NONE',  ( 23.91005183030481263, 4.132774720514426292, -14.40591128290692069 ) ) ;
#2520=ADVANCED_FACE ( 'NONE', ( #4114 ), #13196, .F. ) ;
#2566=DIRECTION ( 'NONE',  ( -0.000000000000000000, 1.000000000000000000, -0.000000000000000000 ) ) ;
#2572=CARTESIAN_POINT ( 'NONE',  ( -27.96875734969026084, 3.316774720514426456, -0.08597719988137648983 ) ) ;
#2574=CARTESIAN_POINT ( 'NONE',  ( -24.57525087998973845, 6.376774720514426953, -15.45548830044933197 ) ) ;
#2583=CARTESIAN_POINT ( 'NONE',  ( 9.069233782100962316, 3.316774720514428232, -28.07145878873749112 ) ) ;
#2586=CARTESIAN_POINT ( 'NONE',  ( 33.74607884027702909, -5.965225279485572685, -4.999864028243830916 ) ) ;
#2587=VECTOR ( 'NONE', #42779, 1000.000000000000000 ) ;
#2598=LINE ( 'NONE', #84931, #49603 ) ;
#2599=EDGE_CURVE ( 'NONE', #35613, #51748, #90837, .T. ) ;
#2608=DIRECTION ( 'NONE',  ( -1.000000000000000000, -1.232047923278981953E-16, 0.000000000000000000 ) ) ;
#2624=CARTESIAN_POINT ( 'NONE',  ( 14.62889129739865446, 4.326482771706361419, -28.09837290214758099 ) ) ;
#2629=CARTESIAN_POINT ( 'NONE',  ( 31.62551770808318707, 4.240436435409185911, 26.92952082091879973 ) ) ;
#2634=EDGE_CURVE ( 'NONE', #51264, #20042, #44675, .T. ) ;
#2662=AXIS2_PLACEMENT_3D ( 'NONE', #78837, #17963, #33690 ) ;
#2666=DIRECTION ( 'NONE',  ( -0.000000000000000000, 1.000000000000000000, -0.000000000000000000 ) ) ;
#2672=CARTESIAN_POINT ( 'NONE',  ( 26.74698519091204574, 1.682774720514426114, -10.98683230472873973 ) ) ;
#2674=ORIENTED_EDGE ( 'NONE', *, *, #27192, .F. ) ;
#2706=EDGE_CURVE ( 'NONE', #20861, #52175, #91331, .T. ) ;
#2710=AXIS2_PLACEMENT_3D ( 'NONE', #94424, #63505, #26429 ) ;
#2728=CARTESIAN_POINT ( 'NONE',  ( 25.61870917940689196, -5.965225279485572685, 29.49402280011862487 ) ) ;
#2749=LINE ( 'NONE', #70247, #83620 ) ;
#2758=AXIS2_PLACEMENT_3D ( 'NONE', #96157, #87542, #94139 ) ;
#2780=CARTESIAN_POINT ( 'NONE',  ( -23.71328795744024376, 0.3587747205144057872, -17.58350715675015863 ) ) ;
#2781=DIRECTION ( 'NONE',  ( 4.472869286569333237E-16, 1.000000000000000000, -7.102795889480452575E-16 ) ) ;
#2783=VECTOR ( 'NONE', #82547, 1000.000000000000000 ) ;
#2785=DIRECTION ( 'NONE',  ( 0.000000000000000000, 0.000000000000000000, -1.000000000000000000 ) ) ;
#2799=AXIS2_PLACEMENT_3D ( 'NONE', #12390, #35746, #66717 ) ;
#2815=ORIENTED_EDGE ( 'NONE', *, *, #21069, .F. ) ;
#2819=CARTESIAN_POINT ( 'NONE',  ( -29.49875734969026198, 0.3587747205144265483, 10.11402280011862587 ) ) ;
#2827=DIRECTION ( 'NONE',  ( 0.000000000000000000, 0.000000000000000000, -1.000000000000000000 ) ) ;
#2831=CARTESIAN_POINT ( 'NONE',  ( 31.13709916799238897, 5.945958180706680807, -1.190136329645604230 ) ) ;
#2837=CYLINDRICAL_SURFACE ( 'NONE', #8587, 22.69500000000000384 ) ;
#2838=ORIENTED_EDGE ( 'NONE', *, *, #39555, .T. ) ;
#2840=CIRCLE ( 'NONE', #62823, 129.7684398600581233 ) ;
#2852=CARTESIAN_POINT ( 'NONE',  ( 282.9764569301858046, 0.3587747205144265483, 20.79159422840526616 ) ) ;
#2855=CARTESIAN_POINT ( 'NONE',  ( 12.88745205056431864, 5.152774720521900775, -28.14312002385407041 ) ) ;
#2861=AXIS2_PLACEMENT_3D ( 'NONE', #89804, #67472, #21272 ) ;
#2878=DIRECTION ( 'NONE',  ( -0.000000000000000000, 1.000000000000000000, -0.000000000000000000 ) ) ;
#2891=CARTESIAN_POINT ( 'NONE',  ( 31.90158556755667973, 4.901725665521331265, -4.230180255418043878 ) ) ;
#2906=CARTESIAN_POINT ( 'NONE',  ( 14.43441819135929194, 3.316774720514426456, -28.36222020317710957 ) ) ;
#2915=ORIENTED_EDGE ( 'NONE', *, *, #97147, .F. ) ;
#2946=DIRECTION ( 'NONE',  ( -0.000000000000000000, 0.000000000000000000, 1.000000000000000000 ) ) ;
#2949=FACE_OUTER_BOUND ( 'NONE', #45637, .T. ) ;
#2964=DIRECTION ( 'NONE',  ( -0.4009304992412306978, -6.454799914155190814E-16, -0.9161084732596777025 ) ) ;
#2984=SHAPE_DEFINITION_REPRESENTATION ( #64431, #44034 ) ;
#3003=CARTESIAN_POINT ( 'NONE',  ( -28.98875734969026041, 3.316774720514426456, 26.43402280011862615 ) ) ;
#3014=VECTOR ( 'NONE', #49035, 1000.000000000000000 ) ;
#3017=ORIENTED_EDGE ( 'NONE', *, *, #25149, .T. ) ;
#3022=DIRECTION ( 'NONE',  ( -0.000000000000000000, 1.000000000000000000, -0.000000000000000000 ) ) ;
#3023=CARTESIAN_POINT ( 'NONE',  ( 26.37445894957760828, 1.682774720514426114, -11.69480419648520986 ) ) ;
#3027=ORIENTED_EDGE ( 'NONE', *, *, #44790, .T. ) ;
#3035=VERTEX_POINT ( 'NONE', #5480 ) ;
#3052=ORIENTED_EDGE ( 'NONE', *, *, #35638, .T. ) ;
#3053=EDGE_LOOP ( 'NONE', ( #97371, #48906, #90486, #17493 ) ) ;
#3089=CYLINDRICAL_SURFACE ( 'NONE', #77343, 4.300000000000000711 ) ;
#3092=CARTESIAN_POINT ( 'NONE',  ( -65.05438548721848235, 5.356774720514425603, 0.7300228001186309656 ) ) ;
#3093=VECTOR ( 'NONE', #1740, 1000.000000000000000 ) ;
#3120=CARTESIAN_POINT ( 'NONE',  ( 33.69795529655567634, -6.475225279485573360, 20.86760796525322093 ) ) ;
#3132=AXIS2_PLACEMENT_3D ( 'NONE', #53415, #44805, #83848 ) ;
#3135=CARTESIAN_POINT ( 'NONE',  ( 31.62961302973990030, 4.065030569019225659, 27.09489828165477476 ) ) ;
#3137=ORIENTED_EDGE ( 'NONE', *, *, #51496, .F. ) ;
#3141=VECTOR ( 'NONE', #68135, 1000.000000000000000 ) ;
#3153=VERTEX_POINT ( 'NONE', #99318 ) ;
#3154=ORIENTED_EDGE ( 'NONE', *, *, #3971, .F. ) ;
#3166=ADVANCED_FACE ( 'NONE', ( #37434 ), #38425, .T. ) ;
#3168=CARTESIAN_POINT ( 'NONE',  ( 32.33217928425156629, -6.475225279485573360, -12.20610769812808982 ) ) ;
#3169=LINE ( 'NONE', #95497, #9213 ) ;
#3171=CARTESIAN_POINT ( 'NONE',  ( 29.65385891689261655, 5.748374461104726940, 28.02705487427158104 ) ) ;
#3185=DIRECTION ( 'NONE',  ( 0.000000000000000000, 0.000000000000000000, -1.000000000000000000 ) ) ;
#3189=CARTESIAN_POINT ( 'NONE',  ( 25.82028661651826340, 4.376709120396486519, -11.31108007975979923 ) ) ;
#3193=EDGE_LOOP ( 'NONE', ( #93746, #91635, #100206, #8613 ) ) ;
#3196=ORIENTED_EDGE ( 'NONE', *, *, #92370, .F. ) ;
#3217=VECTOR ( 'NONE', #11143, 1000.000000000000000 ) ;
#3225=VERTEX_POINT ( 'NONE', #42944 ) ;
#3229=VECTOR ( 'NONE', #54579, 1000.000000000000000 ) ;
#3231=ORIENTED_EDGE ( 'NONE', *, *, #8216, .T. ) ;
#3245=DIRECTION ( 'NONE',  ( -0.000000000000000000, -1.000000000000000000, -0.000000000000000000 ) ) ;
#3259=LINE ( 'NONE', #42325, #610 ) ;
#3262=CARTESIAN_POINT ( 'NONE',  ( -10.11875734969026119, 3.519249775642004696, 30.51402280011862445 ) ) ;
#3266=CARTESIAN_POINT ( 'NONE',  ( 31.79364159983995464, -6.475225279485573360, -11.59305536555894278 ) ) ;
#3288=CARTESIAN_POINT ( 'NONE',  ( -10.21507754268103696, 3.584423063163226786, 29.48076484700401068 ) ) ;
#3289=CARTESIAN_POINT ( 'NONE',  ( 28.30015606816038698, -1.477225279485574028, -13.13501953239208575 ) ) ;
#3297=AXIS2_PLACEMENT_3D ( 'NONE', #70447, #69445, #85667 ) ;
#3302=VERTEX_POINT ( 'NONE', #12962 ) ;
#3306=AXIS2_PLACEMENT_3D ( 'NONE', #34145, #87414, #40247 ) ;
#3329=CARTESIAN_POINT ( 'NONE',  ( -27.96875734969026084, -6.475225279485573360, -0.08597719988137648983 ) ) ;
#3336=CARTESIAN_POINT ( 'NONE',  ( 31.55236408230781819, 6.376774720514426953, 19.84760796525321780 ) ) ;
#3338=CARTESIAN_POINT ( 'NONE',  ( 9.464509667904351886, 3.316774720514128028, -27.03659963365196717 ) ) ;
#3344=ORIENTED_EDGE ( 'NONE', *, *, #13484, .T. ) ;
#3349=AXIS2_PLACEMENT_3D ( 'NONE', #13992, #44969, #99227 ) ;
#3358=DIRECTION ( 'NONE',  ( 0.000000000000000000, 0.000000000000000000, -1.000000000000000000 ) ) ;
#3360=DIRECTION ( 'NONE',  ( 0.000000000000000000, 0.000000000000000000, -1.000000000000000000 ) ) ;
#3386=DIRECTION ( 'NONE',  ( -1.000000000000000000, 0.000000000000000000, 0.000000000000000000 ) ) ;
#3393=CARTESIAN_POINT ( 'NONE',  ( 32.76111974776238611, 3.316774720514426900, -3.850861272813261849 ) ) ;
#3425=ORIENTED_EDGE ( 'NONE', *, *, #71491, .F. ) ;
#3427=EDGE_LOOP ( 'NONE', ( #44782, #68483, #92247, #41809 ) ) ;
#3439=CYLINDRICAL_SURFACE ( 'NONE', #57196, 4.080000000000000071 ) ;
#3467=CARTESIAN_POINT ( 'NONE',  ( -24.90875734969025501, 3.316774720514426456, 26.43402280011862615 ) ) ;
#3492=VERTEX_POINT ( 'NONE', #76842 ) ;
#3502=CARTESIAN_POINT ( 'NONE',  ( -27.25988310792305214, 0.3587747205144265483, 30.32664379231667695 ) ) ;
#3506=CARTESIAN_POINT ( 'NONE',  ( 31.48454476783385658, 4.132774720514426292, -1.134026763942596494 ) ) ;
#3508=ORIENTED_EDGE ( 'NONE', *, *, #67495, .F. ) ;
#3512=ORIENTED_EDGE ( 'NONE', *, *, #77043, .T. ) ;
#3517=DIRECTION ( 'NONE',  ( 0.000000000000000000, 0.000000000000000000, -1.000000000000000000 ) ) ;
#3518=CARTESIAN_POINT ( 'NONE',  ( -29.49875734969026198, -5.965225279485572685, 7.870022800118625206 ) ) ;
#3524=ADVANCED_FACE ( 'NONE', ( #54047 ), #1629, .F. ) ;
#3534=DIRECTION ( 'NONE',  ( 0.000000000000000000, -1.000000000000000000, 0.000000000000000000 ) ) ;
#3547=EDGE_LOOP ( 'NONE', ( #30552, #92804, #78996, #78974 ) ) ;
#3567=DIRECTION ( 'NONE',  ( 0.000000000000000000, 0.000000000000000000, -1.000000000000000000 ) ) ;
#3584=CARTESIAN_POINT ( 'NONE',  ( 7.681304422638354445, 3.316774720514426900, -28.19747436301255661 ) ) ;
#3589=ORIENTED_EDGE ( 'NONE', *, *, #85474, .F. ) ;
#3592=DIRECTION ( 'NONE',  ( -0.000000000000000000, -1.000000000000000000, -0.000000000000000000 ) ) ;
#3623=CARTESIAN_POINT ( 'NONE',  ( 15.76197349289695815, 3.603191427427850257, -28.09505689080078739 ) ) ;
#3630=CARTESIAN_POINT ( 'NONE',  ( 31.66639312903740944, 5.493490882720638346, 28.57493973316412905 ) ) ;
#3632=DIRECTION ( 'NONE',  ( 0.000000000000000000, -1.000000000000000000, 0.000000000000000000 ) ) ;
#3649=VECTOR ( 'NONE', #24484, 1000.000000000000114 ) ;
#3663=DIRECTION ( 'NONE',  ( 0.000000000000000000, 0.000000000000000000, -1.000000000000000000 ) ) ;
#3684=VERTEX_POINT ( 'NONE', #56264 ) ;
#3704=CARTESIAN_POINT ( 'NONE',  ( 32.25249349869196891, 1.682774720514426114, -12.65342752644895441 ) ) ;
#3705=LINE ( 'NONE', #48378, #38291 ) ;
#3740=DIRECTION ( 'NONE',  ( -0.000000000000000000, -1.000000000000000000, -0.000000000000000000 ) ) ;
#3742=ORIENTED_EDGE ( 'NONE', *, *, #76201, .T. ) ;
#3746=ORIENTED_EDGE ( 'NONE', *, *, #8761, .T. ) ;
#3751=VECTOR ( 'NONE', #47453, 1000.000000000000114 ) ;
#3755=DIRECTION ( 'NONE',  ( 1.000000000000000000, 0.000000000000000000, 0.000000000000000000 ) ) ;
#3757=AXIS2_PLACEMENT_3D ( 'NONE', #83958, #76823, #30670 ) ;
#3777=CARTESIAN_POINT ( 'NONE',  ( 27.53860345374808105, -1.477225279485574028, 19.84760796525321780 ) ) ;
#3785=ORIENTED_EDGE ( 'NONE', *, *, #67950, .F. ) ;
#3807=ORIENTED_EDGE ( 'NONE', *, *, #171, .T. ) ;
#3815=ORIENTED_EDGE ( 'NONE', *, *, #88286, .T. ) ;
#3819=CARTESIAN_POINT ( 'NONE',  ( 31.37501302269236092, 4.132774720514428068, -3.717120176012355781 ) ) ;
#3828=CARTESIAN_POINT ( 'NONE',  ( 8.583179188118256420, 5.356774720514425603, -25.03641645905366886 ) ) ;
#3839=DIRECTION ( 'NONE',  ( 0.000000000000000000, -1.000000000000000000, 0.000000000000000000 ) ) ;
#3842=EDGE_CURVE ( 'NONE', #61654, #14296, #84305, .T. ) ;
#3862=CARTESIAN_POINT ( 'NONE',  ( 14.44544951633968566, 3.759487683616679288, -28.33948095063585271 ) ) ;
#3869=ORIENTED_EDGE ( 'NONE', *, *, #20780, .T. ) ;
#3892=ORIENTED_EDGE ( 'NONE', *, *, #95387, .T. ) ;
#3901=LINE ( 'NONE', #82989, #19405 ) ;
#3905=CIRCLE ( 'NONE', #62208, 91.74549126261076992 ) ;
#3912=ORIENTED_EDGE ( 'NONE', *, *, #89824, .F. ) ;
#3919=ORIENTED_EDGE ( 'NONE', *, *, #47278, .T. ) ;
#3931=ORIENTED_EDGE ( 'NONE', *, *, #88286, .F. ) ;
#3945=LINE ( 'NONE', #50609, #75965 ) ;
#3948=CYLINDRICAL_SURFACE ( 'NONE', #76717, 2.249999999999998668 ) ;
#3954=CARTESIAN_POINT ( 'NONE',  ( 29.73828978136054602, 4.772774720514425972, -4.021765098496561386 ) ) ;
#3955=CARTESIAN_POINT ( 'NONE',  ( -12.84880425037202656, 0.3587747205143964613, -26.59900746623529244 ) ) ;
#3960=DIRECTION ( 'NONE',  ( 0.000000000000000000, 1.000000000000000000, -0.000000000000000000 ) ) ;
#3965=FACE_OUTER_BOUND ( 'NONE', #97634, .T. ) ;
#3971=EDGE_CURVE ( 'NONE', #69379, #76864, #66545, .T. ) ;
#4001=CYLINDRICAL_SURFACE ( 'NONE', #66332, 7.652410033082762020 ) ;
#4012=ORIENTED_EDGE ( 'NONE', *, *, #1046, .T. ) ;
#4019=ORIENTED_EDGE ( 'NONE', *, *, #52185, .T. ) ;
#4026=ORIENTED_EDGE ( 'NONE', *, *, #83778, .F. ) ;
#4053=CARTESIAN_POINT ( 'NONE',  ( -23.62875734969026453, -6.143225279485574397, 24.50402280011862288 ) ) ;
#4071=DIRECTION ( 'NONE',  ( 0.000000000000000000, -0.000000000000000000, 1.000000000000000000 ) ) ;
#4102=CARTESIAN_POINT ( 'NONE',  ( -28.47875734969025885, -5.965225279485572685, -0.08597719988137300651 ) ) ;
#4105=PLANE ( 'NONE',  #93204 ) ;
#4110=ORIENTED_EDGE ( 'NONE', *, *, #90775, .F. ) ;
#4114=FACE_OUTER_BOUND ( 'NONE', #25491, .T. ) ;
#4124=CARTESIAN_POINT ( 'NONE',  ( 31.64388307978944326, 6.098167052574009261, 27.71102684943996053 ) ) ;
#4125=ORIENTED_EDGE ( 'NONE', *, *, #31913, .T. ) ;
#4129=CARTESIAN_POINT ( 'NONE',  ( 26.73860345374794178, -1.477225279485574028, 19.84760796525321780 ) ) ;
#4141=ORIENTED_EDGE ( 'NONE', *, *, #65545, .T. ) ;
#4164=VECTOR ( 'NONE', #1261, 1000.000000000000000 ) ;
#4172=VECTOR ( 'NONE', #89910, 1000.000000000000000 ) ;
#4176=VERTEX_POINT ( 'NONE', #80495 ) ;
#4177=CARTESIAN_POINT ( 'NONE',  ( 25.02738304948465853, 5.067934468345774768, -9.480319778648102158 ) ) ;
#4180=AXIS2_PLACEMENT_3D ( 'NONE', #71005, #2492, #1495 ) ;
#4182=DIRECTION ( 'NONE',  ( 0.000000000000000000, 1.000000000000000000, -0.000000000000000000 ) ) ;
#4226=LINE ( 'NONE', #95569, #43080 ) ;
#4255=CARTESIAN_POINT ( 'NONE',  ( -2.701720430790308214, 0.3587747205144061202, -28.90526747363640681 ) ) ;
#4258=DIRECTION ( 'NONE',  ( 0.000000000000000000, 1.000000000000000000, -0.000000000000000000 ) ) ;
#4264=LINE ( 'NONE', #96113, #34053 ) ;
#4271=DIRECTION ( 'NONE',  ( 0.000000000000000000, 0.000000000000000000, -1.000000000000000000 ) ) ;
#4272=VECTOR ( 'NONE', #62106, 1000.000000000000000 ) ;
#4285=ORIENTED_EDGE ( 'NONE', *, *, #88332, .F. ) ;
#4298=ORIENTED_EDGE ( 'NONE', *, *, #92745, .F. ) ;
#4302=ORIENTED_EDGE ( 'NONE', *, *, #8115, .F. ) ;
#4304=EDGE_CURVE ( 'NONE', #31114, #24140, #93087, .T. ) ;
#4306=CARTESIAN_POINT ( 'NONE',  ( -19.77875734969026311, 5.356774720514425603, 27.31649921512899937 ) ) ;
#4312=AXIS2_PLACEMENT_3D ( 'NONE', #70618, #85842, #47790 ) ;
#4321=VERTEX_POINT ( 'NONE', #69769 ) ;
#4324=CARTESIAN_POINT ( 'NONE',  ( 9.405830370894557646, 5.356774720514425603, -24.99732136569351226 ) ) ;
#4337=EDGE_CURVE ( 'NONE', #22003, #43651, #51243, .T. ) ;
#4353=CIRCLE ( 'NONE', #43247, 253.2618649670780826 ) ;
#4366=DIRECTION ( 'NONE',  ( 0.000000000000000000, -0.000000000000000000, 1.000000000000000000 ) ) ;
#4383=AXIS2_PLACEMENT_3D ( 'NONE', #79861, #33700, #10355 ) ;
#4397=DIRECTION ( 'NONE',  ( 0.000000000000000000, -1.000000000000000000, 0.000000000000000000 ) ) ;
#4411=ORIENTED_EDGE ( 'NONE', *, *, #21402, .T. ) ;
#4418=CARTESIAN_POINT ( 'NONE',  ( -11.64875734969026233, 0.3587747205144265483, 31.02402280011862246 ) ) ;
#4424=VERTEX_POINT ( 'NONE', #66557 ) ;
#4438=ORIENTED_EDGE ( 'NONE', *, *, #20775, .T. ) ;
#4445=ORIENTED_EDGE ( 'NONE', *, *, #51520, .T. ) ;
#4448=VECTOR ( 'NONE', #99985, 1000.000000000000000 ) ;
#4476=EDGE_CURVE ( 'NONE', #86005, #84008, #62621, .T. ) ;
#4477=ORIENTED_EDGE ( 'NONE', *, *, #33366, .T. ) ;
#4485=DIRECTION ( 'NONE',  ( 0.9822594791677485837, 0.000000000000000000, -0.1875268396392987258 ) ) ;
#4502=CARTESIAN_POINT ( 'NONE',  ( 4.784292611718075072, 3.316774720514426456, -25.54547254883186014 ) ) ;
#4503=CARTESIAN_POINT ( 'NONE',  ( -0.02075734969026423599, -6.475225279485573360, -0.08597719988137648983 ) ) ;
#4517=AXIS2_PLACEMENT_3D ( 'NONE', #38624, #54365, #23896 ) ;
#4542=EDGE_CURVE ( 'NONE', #74051, #97749, #42703, .T. ) ;
#4571=CARTESIAN_POINT ( 'NONE',  ( 32.42932432802503939, 6.376774720514426953, -0.2107846672978405389 ) ) ;
#4594=DIRECTION ( 'NONE',  ( 0.000000000000000000, 0.000000000000000000, 1.000000000000000000 ) ) ;
#4600=CARTESIAN_POINT ( 'NONE',  ( 13.02836919244612623, 3.777199458296179646, -28.16488413836729521 ) ) ;
#4601=EDGE_CURVE ( 'NONE', #74060, #14845, #30224, .T. ) ;
#4613=DIRECTION ( 'NONE',  ( -0.9978940991575084851, -0.000000000000000000, -0.06486421869277853025 ) ) ;
#4616=DIRECTION ( 'NONE',  ( -0.000000000000000000, -1.000000000000000000, -0.000000000000000000 ) ) ;
#4618=CARTESIAN_POINT ( 'NONE',  ( 27.86270917940689174, -5.965225279485572685, 29.49402280011862487 ) ) ;
#4625=CARTESIAN_POINT ( 'NONE',  ( 29.77147767949870882, 6.376774720514427841, 26.15915692125050995 ) ) ;
#4626=VERTEX_POINT ( 'NONE', #85235 ) ;
#4643=CARTESIAN_POINT ( 'NONE',  ( -20.27875734969026311, 5.356774720514425603, 24.00402280011862288 ) ) ;
#4655=CARTESIAN_POINT ( 'NONE',  ( 30.73873608389078527, -2.297196155479623414, 24.67598410064775294 ) ) ;
#4660=EDGE_CURVE ( 'NONE', #89884, #94148, #79125, .T. ) ;
#4662=ADVANCED_FACE ( 'NONE', ( #56320 ), #95856, .T. ) ;
#4677=ORIENTED_EDGE ( 'NONE', *, *, #29638, .F. ) ;
#4698=LINE ( 'NONE', #35648, #16572 ) ;
#4703=ORIENTED_EDGE ( 'NONE', *, *, #67950, .T. ) ;
#4704=CARTESIAN_POINT ( 'NONE',  ( 33.61456970919601872, 6.376774720514426953, -11.35828564741663627 ) ) ;
#4707=ADVANCED_FACE ( 'NONE', ( #48704 ), #98237, .T. ) ;
#4723=AXIS2_PLACEMENT_3D ( 'NONE', #6512, #76005, #21221 ) ;
#4725=CARTESIAN_POINT ( 'NONE',  ( 13.91401389203221406, 3.316774720514426456, 158.0376437107427137 ) ) ;
#4764=ORIENTED_EDGE ( 'NONE', *, *, #91347, .T. ) ;
#4766=CARTESIAN_POINT ( 'NONE',  ( 3.176458874063931681, 0.3587747205143967943, -28.85257003503889806 ) ) ;
#4770=FACE_OUTER_BOUND ( 'NONE', #63705, .T. ) ;
#4772=CYLINDRICAL_SURFACE ( 'NONE', #35577, 28.96799999999999642 ) ;
#4783=ORIENTED_EDGE ( 'NONE', *, *, #16436, .F. ) ;
#4787=AXIS2_PLACEMENT_3D ( 'NONE', #17343, #48304, #71639 ) ;
#4798=ORIENTED_EDGE ( 'NONE', *, *, #2142, .T. ) ;
#4799=AXIS2_PLACEMENT_3D ( 'NONE', #88391, #2666, #9253 ) ;
#4804=AXIS2_PLACEMENT_3D ( 'NONE', #83098, #62662, #55547 ) ;
#4832=FACE_OUTER_BOUND ( 'NONE', #20359, .T. ) ;
#4843=DIRECTION ( 'NONE',  ( 0.000000000000000000, 1.000000000000000000, -0.000000000000000000 ) ) ;
#4849=CARTESIAN_POINT ( 'NONE',  ( 30.93898937471034216, 4.884441105398384941, -1.603546260404424606 ) ) ;
#4854=CARTESIAN_POINT ( 'NONE',  ( 30.63451081005166543, 4.279369518130740069, 28.08236555530620038 ) ) ;
#4874=CARTESIAN_POINT ( 'NONE',  ( -12.84880425037203011, -5.965225279485592225, -26.59900746623528534 ) ) ;
#4876=AXIS2_PLACEMENT_3D ( 'NONE', #17911, #86914, #95531 ) ;
#4886=ORIENTED_EDGE ( 'NONE', *, *, #52235, .F. ) ;
#4910=EDGE_LOOP ( 'NONE', ( #12098, #31468, #8888, #17356 ) ) ;
#4937=DIRECTION ( 'NONE',  ( 1.000000000000000000, 0.000000000000000000, -0.000000000000000000 ) ) ;
#4939=CIRCLE ( 'NONE', #56817, 130.7884398600581335 ) ;
#4943=LINE ( 'NONE', #80565, #60078 ) ;
#4946=VECTOR ( 'NONE', #13039, 1000.000000000000227 ) ;
#4949=CARTESIAN_POINT ( 'NONE',  ( 30.53060340732037048, 2.682774720514426559, -2.322449884495168870 ) ) ;
#4955=VERTEX_POINT ( 'NONE', #90744 ) ;
#4969=ORIENTED_EDGE ( 'NONE', *, *, #27648, .F. ) ;
#4970=CARTESIAN_POINT ( 'NONE',  ( 31.41423154468143153, 2.682774720514426559, -0.3119954678742140053 ) ) ;
#4971=PLANE ( 'NONE',  #72115 ) ;
#4987=VECTOR ( 'NONE', #56965, 1000.000000000000000 ) ;
#4996=ORIENTED_EDGE ( 'NONE', *, *, #63895, .T. ) ;
#5005=DIRECTION ( 'NONE',  ( -0.000000000000000000, 1.000000000000000000, -0.000000000000000000 ) ) ;
#5011=VECTOR ( 'NONE', #68536, 1000.000000000000000 ) ;
#5017=EDGE_CURVE ( 'NONE', #32090, #62563, #42969, .T. ) ;
#5021=ORIENTED_EDGE ( 'NONE', *, *, #23347, .F. ) ;
#5032=ORIENTED_EDGE ( 'NONE', *, *, #41304, .F. ) ;
#5045=CARTESIAN_POINT ( 'NONE',  ( 9.016989526679575206, 3.316774720514426900, -27.05137190084761301 ) ) ;
#5049=B_SPLINE_CURVE_WITH_KNOTS ( 'NONE', 3,
 ( #16655, #1452, #8047, #38997 ),
 .UNSPECIFIED., .F., .F.,
 ( 4, 4 ),
 ( 0.000000000000000000, 0.001418231214350569244 ),
 .UNSPECIFIED. ) ;
#5066=DIRECTION ( 'NONE',  ( -0.9952638024365005887, -0.000000000000000000, -0.09721092304694052555 ) ) ;
#5090=LINE ( 'NONE', #52770, #81326 ) ;
#5094=DIRECTION ( 'NONE',  ( 0.7512896232465891000, 0.000000000000000000, 0.6599726524652351767 ) ) ;
#5098=CARTESIAN_POINT ( 'NONE',  ( 22.02124265030973760, -4.543225279485573864, 16.20402280011862217 ) ) ;
#5104=AXIS2_PLACEMENT_3D ( 'NONE', #41875, #33240, #72819 ) ;
#5114=DIRECTION ( 'NONE',  ( -0.000000000000000000, -1.000000000000000000, -0.000000000000000000 ) ) ;
#5119=ORIENTED_EDGE ( 'NONE', *, *, #44571, .F. ) ;
#5125=ORIENTED_EDGE ( 'NONE', *, *, #74861, .T. ) ;
#5126=VERTEX_POINT ( 'NONE', #67808 ) ;
#5130=ORIENTED_EDGE ( 'NONE', *, *, #85027, .F. ) ;
#5131=ORIENTED_EDGE ( 'NONE', *, *, #68220, .F. ) ;
#5148=VECTOR ( 'NONE', #75199, 1000.000000000000000 ) ;
#5163=DIRECTION ( 'NONE',  ( 0.000000000000000000, 0.000000000000000000, -1.000000000000000000 ) ) ;
#5169=EDGE_LOOP ( 'NONE', ( #44368, #96460, #91645, #20830 ) ) ;
#5233=ORIENTED_EDGE ( 'NONE', *, *, #82139, .F. ) ;
#5263=DIRECTION ( 'NONE',  ( -0.7512896232465894331, 0.000000000000000000, -0.6599726524652348436 ) ) ;
#5275=ORIENTED_EDGE ( 'NONE', *, *, #26358, .T. ) ;
#5290=VECTOR ( 'NONE', #89316, 1000.000000000000000 ) ;
#5326=PRODUCT ( 'Plastic Part 1', 'Plastic Part 1', '', ( #52878 ) ) ;
#5329=DIRECTION ( 'NONE',  ( -1.000000000000000000, 0.000000000000000000, -0.000000000000000000 ) ) ;
#5376=VERTEX_POINT ( 'NONE', #74279 ) ;
#5378=VERTEX_POINT ( 'NONE', #96610 ) ;
#5380=VERTEX_POINT ( 'NONE', #58077 ) ;
#5381=CARTESIAN_POINT ( 'NONE',  ( -0.02075734969026423599, -5.965225279485572685, -0.08597719988137648983 ) ) ;
#5383=CYLINDRICAL_SURFACE ( 'NONE', #47108, 3.500000000000000000 ) ;
#5425=EDGE_LOOP ( 'NONE', ( #77297, #51376 ) ) ;
#5431=CARTESIAN_POINT ( 'NONE',  ( 13.10664265030973930, -5.965225279485574461, -28.18129937516157568 ) ) ;
#5439=VECTOR ( 'NONE', #66863, 1000.000000000000000 ) ;
#5469=CARTESIAN_POINT ( 'NONE',  ( -19.38764004357183168, 0.3587747205143967943, -21.62823517627351322 ) ) ;
#5474=CARTESIAN_POINT ( 'NONE',  ( 15.29947330337543754, -6.475225279485573360, -27.16854002387008649 ) ) ;
#5480=CARTESIAN_POINT ( 'NONE',  ( -28.98875734969026041, -5.965225279485572685, -0.08597719988137116076 ) ) ;
#5486=CARTESIAN_POINT ( 'NONE',  ( -65.05438548721848235, 3.316774720514426456, 27.45402280011862572 ) ) ;
#5502=CARTESIAN_POINT ( 'NONE',  ( 10.86264265030973952, -5.965225279485574461, -28.64597719988137570 ) ) ;
#5514=VERTEX_POINT ( 'NONE', #35226 ) ;
#5527=CARTESIAN_POINT ( 'NONE',  ( -27.83739072329610664, 0.3587747205143967943, -8.084349702057700426 ) ) ;
#5536=ADVANCED_FACE ( 'NONE', ( #4770 ), #35169, .F. ) ;
#5544=CARTESIAN_POINT ( 'NONE',  ( 12.17747153392518733, 4.565036639100802596, -27.62487831441275787 ) ) ;
#5552=EDGE_CURVE ( 'NONE', #52365, #41503, #88012, .T. ) ;
#5581=CARTESIAN_POINT ( 'NONE',  ( 8.868390920966309210, 6.053523946337313610, -26.43277665853620206 ) ) ;
#5595=EDGE_LOOP ( 'NONE', ( #27226, #52542, #28497, #70797, #70436, #4677 ) ) ;
#5614=CARTESIAN_POINT ( 'NONE',  ( -20.27875734969026311, -4.543225279485573864, 25.15402280011862146 ) ) ;
#5624=VERTEX_POINT ( 'NONE', #45334 ) ;
#5631=DIRECTION ( 'NONE',  ( -0.000000000000000000, -1.000000000000000000, -0.000000000000000000 ) ) ;
#5664=EDGE_CURVE ( 'NONE', #51748, #24998, #77745, .T. ) ;
#5682=AXIS2_PLACEMENT_3D ( 'NONE', #75015, #27361, #58322 ) ;
#5684=DIRECTION ( 'NONE',  ( 0.000000000000000000, -1.000000000000000000, 0.000000000000000000 ) ) ;
#5696=LINE ( 'NONE', #21404, #87286 ) ;
#5699=LINE ( 'NONE', #98535, #12049 ) ;
#5707=ORIENTED_EDGE ( 'NONE', *, *, #11016, .T. ) ;
#5739=CIRCLE ( 'NONE', #41471, 252.4458649670781085 ) ;
#5740=DIRECTION ( 'NONE',  ( 1.000000000000000000, 0.000000000000000000, 0.000000000000000000 ) ) ;
#5745=ORIENTED_EDGE ( 'NONE', *, *, #35402, .T. ) ;
#5762=CARTESIAN_POINT ( 'NONE',  ( 15.92621150404962016, -6.475225279485573360, -27.29681269571041824 ) ) ;
#5765=EDGE_LOOP ( 'NONE', ( #68931, #14063, #81932, #83262 ) ) ;
#5776=EDGE_CURVE ( 'NONE', #59325, #97546, #31590, .T. ) ;
#5783=CARTESIAN_POINT ( 'NONE',  ( 31.99559323149412648, 3.570691370340881576, -11.82294999027247862 ) ) ;
#5789=VERTEX_POINT ( 'NONE', #43224 ) ;
#5818=CIRCLE ( 'NONE', #46378, 4.300000000000000711 ) ;
#5826=VECTOR ( 'NONE', #16529, 999.9999999999998863 ) ;
#5827=CARTESIAN_POINT ( 'NONE',  ( -6.741682653110981249, -5.965225279485572685, 30.62569541381301619 ) ) ;
#5834=CIRCLE ( 'NONE', #72339, 2.040000000000000036 ) ;
#5837=EDGE_CURVE ( 'NONE', #88037, #65689, #57458, .T. ) ;
#5839=DIRECTION ( 'NONE',  ( 0.000000000000000000, 0.000000000000000000, -1.000000000000000000 ) ) ;
#5843=CARTESIAN_POINT ( 'NONE',  ( 31.21829842716237735, 4.540774721315884221, 2.131740660352481775 ) ) ;
#5848=FACE_OUTER_BOUND ( 'NONE', #55846, .T. ) ;
#5853=VERTEX_POINT ( 'NONE', #65578 ) ;
#5882=AXIS2_PLACEMENT_3D ( 'NONE', #64268, #87578, #57150 ) ;
#5893=CARTESIAN_POINT ( 'NONE',  ( -28.98875734969026041, 0.3587747205144265483, 25.61802280011862720 ) ) ;
#5895=ORIENTED_EDGE ( 'NONE', *, *, #15857, .T. ) ;
#5896=VECTOR ( 'NONE', #66051, 1000.000000000000000 ) ;
#5904=ORIENTED_EDGE ( 'NONE', *, *, #67020, .T. ) ;
#5906=ADVANCED_FACE ( 'NONE', ( #41220 ), #25482, .F. ) ;
#5950=EDGE_CURVE ( 'NONE', #64064, #61556, #3169, .T. ) ;
#5958=DIRECTION ( 'NONE',  ( 0.000000000000000000, 0.000000000000000000, -1.000000000000000000 ) ) ;
#5961=CARTESIAN_POINT ( 'NONE',  ( 33.74607884027702909, 0.3587747205144265483, -4.999864028243830916 ) ) ;
#5990=ORIENTED_EDGE ( 'NONE', *, *, #28011, .F. ) ;
#5992=EDGE_LOOP ( 'NONE', ( #41990, #47814, #20136, #18360 ) ) ;
#6008=CIRCLE ( 'NONE', #22140, 1.150000000000003464 ) ;
#6012=VERTEX_POINT ( 'NONE', #62323 ) ;
#6014=ORIENTED_EDGE ( 'NONE', *, *, #9336, .T. ) ;
#6032=VECTOR ( 'NONE', #69403, 1000.000000000000000 ) ;
#6035=ORIENTED_EDGE ( 'NONE', *, *, #57930, .T. ) ;
#6037=CARTESIAN_POINT ( 'NONE',  ( -13.89275734969026388, -5.965225279485572685, 30.51402280011862089 ) ) ;
#6038=CARTESIAN_POINT ( 'NONE',  ( 22.02124265030973760, 5.356774720514425603, 16.20402280011862217 ) ) ;
#6041=CARTESIAN_POINT ( 'NONE',  ( 5.097264368844749427, 3.316774720514425567, -27.56135813788841560 ) ) ;
#6056=CARTESIAN_POINT ( 'NONE',  ( -27.96875734969026084, -6.143225279485574397, 24.50402280011861933 ) ) ;
#6073=CARTESIAN_POINT ( 'NONE',  ( 7.526024287269984292, 4.772774720514425972, 9.032262774691707463 ) ) ;
#6082=EDGE_CURVE ( 'NONE', #69136, #42281, #53208, .T. ) ;
#6083=ORIENTED_EDGE ( 'NONE', *, *, #52560, .F. ) ;
#6088=DIRECTION ( 'NONE',  ( -0.000000000000000000, 1.000000000000000000, -0.000000000000000000 ) ) ;
#6098=DIRECTION ( 'NONE',  ( 0.000000000000000000, -1.000000000000000000, 0.000000000000000000 ) ) ;
#6109=EDGE_CURVE ( 'NONE', #75450, #9293, #95059, .T. ) ;
#6123=FACE_BOUND ( 'NONE', #77144, .T. ) ;
#6140=CARTESIAN_POINT ( 'NONE',  ( 32.70426658926474062, 3.547616055647111022, -3.273583889775387057 ) ) ;
#6144=DIRECTION ( 'NONE',  ( 0.000000000000000000, -0.000000000000000000, -1.000000000000000000 ) ) ;
#6156=CARTESIAN_POINT ( 'NONE',  ( -27.13414387080440093, 0.3587747205144061202, -10.21530720150730609 ) ) ;
#6160=VECTOR ( 'NONE', #27173, 1000.000000000000000 ) ;
#6178=VECTOR ( 'NONE', #18816, 1000.000000000000000 ) ;
#6188=AXIS2_PLACEMENT_3D ( 'NONE', #84952, #16435, #71243 ) ;
#6195=CARTESIAN_POINT ( 'NONE',  ( -16.22218391600152643, -6.475225279485573360, -54.85883559227303863 ) ) ;
#6201=CARTESIAN_POINT ( 'NONE',  ( 4.784292611718075072, 6.376774720514426953, -25.54547254883186014 ) ) ;
#6216=LINE ( 'NONE', #20434, #100299 ) ;
#6220=CARTESIAN_POINT ( 'NONE',  ( 20.57455539870835537, 4.132774720514415634, -18.22080502500613974 ) ) ;
#6235=CARTESIAN_POINT ( 'NONE',  ( 31.02038118199824268, 5.152774720514427642, -4.893189986691015569 ) ) ;
#6236=ORIENTED_EDGE ( 'NONE', *, *, #460, .F. ) ;
#6238=ORIENTED_EDGE ( 'NONE', *, *, #41569, .T. ) ;
#6260=VECTOR ( 'NONE', #22906, 1000.000000000000000 ) ;
#6298=DIRECTION ( 'NONE',  ( 0.000000000000000000, 1.000000000000000000, 0.000000000000000000 ) ) ;
#6305=ORIENTED_EDGE ( 'NONE', *, *, #62012, .T. ) ;
#6329=DIRECTION ( 'NONE',  ( 0.000000000000000000, 0.000000000000000000, -1.000000000000000000 ) ) ;
#6341=CIRCLE ( 'NONE', #100255, 2.039999999999998703 ) ;
#6346=CARTESIAN_POINT ( 'NONE',  ( 29.77147767949870882, 5.356774720514427379, 26.15915692125050995 ) ) ;
#6356=ADVANCED_FACE ( 'NONE', ( #77892 ), #94128, .T. ) ;
#6370=ORIENTED_EDGE ( 'NONE', *, *, #42025, .T. ) ;
#6383=ORIENTED_EDGE ( 'NONE', *, *, #89842, .F. ) ;
#6385=CIRCLE ( 'NONE', #79310, 3.349999999999998757 ) ;
#6418=ORIENTED_EDGE ( 'NONE', *, *, #77124, .T. ) ;
#6438=DIRECTION ( 'NONE',  ( -1.000000000000000000, 0.000000000000000000, -0.000000000000000000 ) ) ;
#6440=VECTOR ( 'NONE', #3740, 1000.000000000000000 ) ;
#6444=CARTESIAN_POINT ( 'NONE',  ( 31.31283134548411340, 1.682774720514426114, -10.20862453625735533 ) ) ;
#6446=DIRECTION ( 'NONE',  ( 0.1827036106964188000, 3.614007241618350743E-15, -0.9831680378442393398 ) ) ;
#6452=CARTESIAN_POINT ( 'NONE',  ( -2.872281323269014752, -16.94322527948557422, 1.999999999999999556 ) ) ;
#6458=CIRCLE ( 'NONE', #27544, 0.8160000000000007248 ) ;
#6461=CARTESIAN_POINT ( 'NONE',  ( 5.184553252003285984, -6.475225279485573360, -28.06387035751381731 ) ) ;
#6483=DIRECTION ( 'NONE',  ( 0.000000000000000000, 0.000000000000000000, -1.000000000000000000 ) ) ;
#6493=DIRECTION ( 'NONE',  ( 0.000000000000000000, 0.000000000000000000, -1.000000000000000000 ) ) ;
#6496=ORIENTED_EDGE ( 'NONE', *, *, #82765, .F. ) ;
#6512=CARTESIAN_POINT ( 'NONE',  ( -53.01255352321339842, 1.682774720514426114, 35.59556822165056644 ) ) ;
#6517=LINE ( 'NONE', #7509, #18341 ) ;
#6533=AXIS2_PLACEMENT_3D ( 'NONE', #94344, #94845, #79120 ) ;
#6537=AXIS2_PLACEMENT_3D ( 'NONE', #92290, #60371, #100380 ) ;
#6553=PLANE ( 'NONE',  #64721 ) ;
#6569=ORIENTED_EDGE ( 'NONE', *, *, #66322, .F. ) ;
#6570=DIRECTION ( 'NONE',  ( -0.000000000000000000, -1.000000000000000000, -0.000000000000000000 ) ) ;
#6586=DIRECTION ( 'NONE',  ( 0.000000000000000000, -1.000000000000000000, -0.000000000000000000 ) ) ;
#6592=ORIENTED_EDGE ( 'NONE', *, *, #6645, .T. ) ;
#6604=CARTESIAN_POINT ( 'NONE',  ( 29.64064043116815128, -5.965225279485572685, 28.71191112024341408 ) ) ;
#6609=EDGE_CURVE ( 'NONE', #72159, #62379, #46532, .T. ) ;
#6612=ORIENTED_EDGE ( 'NONE', *, *, #11576, .T. ) ;
#6628=ORIENTED_EDGE ( 'NONE', *, *, #14530, .F. ) ;
#6639=LINE ( 'NONE', #91873, #29041 ) ;
#6641=ORIENTED_EDGE ( 'NONE', *, *, #7174, .T. ) ;
#6645=EDGE_CURVE ( 'NONE', #28007, #93008, #59499, .T. ) ;
#6672=ORIENTED_EDGE ( 'NONE', *, *, #88387, .F. ) ;
#6678=VERTEX_POINT ( 'NONE', #60089 ) ;
#6713=DIRECTION ( 'NONE',  ( 0.000000000000000000, 1.000000000000000000, 0.000000000000000000 ) ) ;
#6732=CARTESIAN_POINT ( 'NONE',  ( 15.14080536460164694, 5.152774720514426754, -26.62908960815040516 ) ) ;
#6736=CARTESIAN_POINT ( 'NONE',  ( 33.10875634548599322, -5.965225279485572685, -11.42349945801155719 ) ) ;
#6753=FACE_OUTER_BOUND ( 'NONE', #66928, .T. ) ;
#6778=ORIENTED_EDGE ( 'NONE', *, *, #16101, .F. ) ;
#6790=ORIENTED_EDGE ( 'NONE', *, *, #10326, .T. ) ;
#6810=CARTESIAN_POINT ( 'NONE',  ( 29.73860345376319358, 1.682774720514426114, -8.849814207987163783 ) ) ;
#6823=EDGE_CURVE ( 'NONE', #20097, #22611, #10280, .T. ) ;
#6839=ADVANCED_FACE ( 'NONE', ( #80798 ), #42748, .F. ) ;
#6856=AXIS2_PLACEMENT_3D ( 'NONE', #79955, #58139, #72859 ) ;
#6859=CARTESIAN_POINT ( 'NONE',  ( 0.000000000000000000, -16.94322527948557422, 0.000000000000000000 ) ) ;
#6860=VECTOR ( 'NONE', #49666, 1000.000000000000114 ) ;
#6898=VECTOR ( 'NONE', #50962, 1000.000000000000114 ) ;
#6907=VERTEX_POINT ( 'NONE', #88411 ) ;
#6914=ORIENTED_EDGE ( 'NONE', *, *, #53735, .F. ) ;
#6924=EDGE_CURVE ( 'NONE', #14228, #75250, #21865, .T. ) ;
#6925=DIRECTION ( 'NONE',  ( 0.000000000000000000, 0.000000000000000000, -1.000000000000000000 ) ) ;
#6929=VECTOR ( 'NONE', #99030, 1000.000000000000000 ) ;
#6960=CARTESIAN_POINT ( 'NONE',  ( 30.61238849909758031, 3.934983946744459171, 27.21775687185679615 ) ) ;
#6965=ORIENTED_EDGE ( 'NONE', *, *, #78604, .T. ) ;
#6986=CARTESIAN_POINT ( 'NONE',  ( 10.95759398273795249, 4.132774720514426292, -26.86884997114579932 ) ) ;
#6994=ORIENTED_EDGE ( 'NONE', *, *, #57239, .T. ) ;
#7003=CARTESIAN_POINT ( 'NONE',  ( 32.98733314340959311, 0.3587747205144265483, 2.074222136288530027 ) ) ;
#7009=AXIS2_PLACEMENT_3D ( 'NONE', #25558, #95073, #39275 ) ;
#7014=ORIENTED_EDGE ( 'NONE', *, *, #94197, .T. ) ;
#7032=VECTOR ( 'NONE', #19060, 1000.000000000000000 ) ;
#7034=ORIENTED_EDGE ( 'NONE', *, *, #93418, .T. ) ;
#7048=CARTESIAN_POINT ( 'NONE',  ( 32.66876533700883556, -5.965225279485572685, -12.58926540598386445 ) ) ;
#7091=DIRECTION ( 'NONE',  ( 0.000000000000000000, -1.000000000000000000, 0.000000000000000000 ) ) ;
#7092=EDGE_CURVE ( 'NONE', #5624, #22977, #78150, .T. ) ;
#7103=CARTESIAN_POINT ( 'NONE',  ( 0.000000000000000000, 5.356774720514425603, 0.000000000000000000 ) ) ;
#7106=AXIS2_PLACEMENT_3D ( 'NONE', #42648, #33516, #65995 ) ;
#7107=ORIENTED_EDGE ( 'NONE', *, *, #37970, .F. ) ;
#7115=EDGE_LOOP ( 'NONE', ( #83697, #23480, #62003, #60217 ) ) ;
#7168=CARTESIAN_POINT ( 'NONE',  ( 2.449489742783178770, -1.473225279485573358, 2.499999999999999556 ) ) ;
#7169=ORIENTED_EDGE ( 'NONE', *, *, #81947, .F. ) ;
#7174=EDGE_CURVE ( 'NONE', #64559, #40372, #1028, .T. ) ;
#7180=ORIENTED_EDGE ( 'NONE', *, *, #93757, .F. ) ;
#7181=CARTESIAN_POINT ( 'NONE',  ( 6.783277369150963132, 3.316774720515097030, -28.31678455703255892 ) ) ;
#7183=CIRCLE ( 'NONE', #80140, 130.2784398600581710 ) ;
#7187=CARTESIAN_POINT ( 'NONE',  ( -16.22218391600152643, -6.475225279485573360, -54.85883559227303863 ) ) ;
#7191=PLANE ( 'NONE',  #84577 ) ;
#7192=CARTESIAN_POINT ( 'NONE',  ( 13.10664265030973930, 0.3587747205144256601, -28.64597719988137570 ) ) ;
#7202=CARTESIAN_POINT ( 'NONE',  ( 29.73860345376319358, 5.356774720514428267, 17.72811383290910570 ) ) ;
#7236=CARTESIAN_POINT ( 'NONE',  ( 282.9764569301858046, -6.475225279485573360, 20.79159422840526616 ) ) ;
#7251=ORIENTED_EDGE ( 'NONE', *, *, #75219, .T. ) ;
#7252=VECTOR ( 'NONE', #87087, 1000.000000000000000 ) ;
#7271=DIRECTION ( 'NONE',  ( 0.000000000000000000, -0.000000000000000000, -1.000000000000000000 ) ) ;
#7272=ORIENTED_EDGE ( 'NONE', *, *, #39596, .T. ) ;
#7273=CIRCLE ( 'NONE', #21819, 1.836000000000000743 ) ;
#7311=DIRECTION ( 'NONE',  ( 0.000000000000000000, 0.000000000000000000, -1.000000000000000000 ) ) ;
#7324=VECTOR ( 'NONE', #24821, 1000.000000000000227 ) ;
#7330=LINE ( 'NONE', #30677, #21918 ) ;
#7331=FACE_OUTER_BOUND ( 'NONE', #92671, .T. ) ;
#7334=CIRCLE ( 'NONE', #20303, 2.249999999999998668 ) ;
#7336=EDGE_LOOP ( 'NONE', ( #94266, #96149, #63303, #25912, #14216 ) ) ;
#7354=CARTESIAN_POINT ( 'NONE',  ( 33.96422015159436114, -5.965225279485572685, -7.233236000911337449 ) ) ;
#7356=ORIENTED_EDGE ( 'NONE', *, *, #18724, .T. ) ;
#7359=ORIENTED_EDGE ( 'NONE', *, *, #36750, .F. ) ;
#7371=EDGE_CURVE ( 'NONE', #87883, #34838, #98861, .T. ) ;
#7374=ORIENTED_EDGE ( 'NONE', *, *, #10830, .F. ) ;
#7380=LINE ( 'NONE', #30218, #13081 ) ;
#7394=DIRECTION ( 'NONE',  ( 0.000000000000000000, 1.000000000000000000, 0.000000000000000000 ) ) ;
#7405=DIRECTION ( 'NONE',  ( -0.03244919754393515293, 0.000000000000000000, 0.9994733861282923959 ) ) ;
#7411=EDGE_CURVE ( 'NONE', #84489, #65436, #15131, .T. ) ;
#7412=CIRCLE ( 'NONE', #77089, 253.2618649670780826 ) ;
#7418=CARTESIAN_POINT ( 'NONE',  ( 32.45853543194704116, 0.3587747205144265483, 9.169203677920338080 ) ) ;
#7421=FACE_OUTER_BOUND ( 'NONE', #84530, .T. ) ;
#7439=CARTESIAN_POINT ( 'NONE',  ( 13.91401389203221406, -5.965225279485572685, 28.26920385068457264 ) ) ;
#7444=ADVANCED_FACE ( 'NONE', ( #30859 ), #44724, .F. ) ;
#7452=ORIENTED_EDGE ( 'NONE', *, *, #2398, .F. ) ;
#7455=LINE ( 'NONE', #38412, #91491 ) ;
#7458=CARTESIAN_POINT ( 'NONE',  ( 22.02124265030973760, -4.543225279485573864, 18.45402280011862217 ) ) ;
#7459=CARTESIAN_POINT ( 'NONE',  ( 32.34323322234308762, 6.036341485554500785, 0.7979233379450167973 ) ) ;
#7469=DIRECTION ( 'NONE',  ( -1.000000000000000000, 0.000000000000000000, 0.000000000000000000 ) ) ;
#7477=CARTESIAN_POINT ( 'NONE',  ( 32.45853543194704116, 0.3587747205144265483, 9.169203677920338080 ) ) ;
#7485=ORIENTED_EDGE ( 'NONE', *, *, #68898, .F. ) ;
#7497=CIRCLE ( 'NONE', #70659, 11.85241003308275864 ) ;
#7506=ORIENTED_EDGE ( 'NONE', *, *, #54767, .F. ) ;
#7509=CARTESIAN_POINT ( 'NONE',  ( 27.53860345374808105, -1.477225279485574028, 19.84760796525321780 ) ) ;
#7517=ADVANCED_FACE ( 'NONE', ( #76515 ), #16130, .F. ) ;
#7525=EDGE_LOOP ( 'NONE', ( #53611, #77228, #80081, #6569, #90860, #79894 ) ) ;
#7534=CARTESIAN_POINT ( 'NONE',  ( 30.09341516180546350, -1.477225279485574028, -11.39311774897855756 ) ) ;
#7547=CARTESIAN_POINT ( 'NONE',  ( 12.00135123753652877, 5.092666038735283784, -26.74699110798160007 ) ) ;
#7561=AXIS2_PLACEMENT_3D ( 'NONE', #48955, #79885, #2785 ) ;
#7568=PLANE ( 'NONE',  #89887 ) ;
#7574=CIRCLE ( 'NONE', #18935, 4.080000000000000071 ) ;
#7590=ORIENTED_EDGE ( 'NONE', *, *, #93052, .F. ) ;
#7597=CARTESIAN_POINT ( 'NONE',  ( 12.66784028006542151, 2.682774720514427003, -27.12025593822526304 ) ) ;
#7613=FACE_OUTER_BOUND ( 'NONE', #90014, .T. ) ;
#7628=DIRECTION ( 'NONE',  ( 0.000000000000000000, -1.000000000000000000, 0.000000000000000000 ) ) ;
#7636=LINE ( 'NONE', #93358, #92488 ) ;
#7643=LINE ( 'NONE', #84759, #27078 ) ;
#7659=ORIENTED_EDGE ( 'NONE', *, *, #47736, .F. ) ;
#7686=CIRCLE ( 'NONE', #2861, 2.499999999999995115 ) ;
#7689=CARTESIAN_POINT ( 'NONE',  ( 5.271800844967073907, 6.376774720514426953, -28.56638892015272546 ) ) ;
#7692=ADVANCED_BREP_SHAPE_REPRESENTATION ( '', ( #11338, #37391 ), #11455 ) ;
#7700=VECTOR ( 'NONE', #96393, 1000.000000000000000 ) ;
#7733=CARTESIAN_POINT ( 'NONE',  ( 16.04643365539530109, 3.607965404481768612, -27.87003593022056691 ) ) ;
#7740=ORIENTED_EDGE ( 'NONE', *, *, #30392, .T. ) ;
#7755=ORIENTED_EDGE ( 'NONE', *, *, #24441, .F. ) ;
#7760=VERTEX_POINT ( 'NONE', #76892 ) ;
#7772=CARTESIAN_POINT ( 'NONE',  ( -28.98875734969026396, -5.965225279485572685, 0.1180228001186258285 ) ) ;
#7788=CARTESIAN_POINT ( 'NONE',  ( 32.18888049830260911, 5.126885235861809775, -11.87322522691203908 ) ) ;
#7807=ORIENTED_EDGE ( 'NONE', *, *, #634, .T. ) ;
#7837=CARTESIAN_POINT ( 'NONE',  ( 5.395440699609677537, -5.965225279485594001, -28.51842087987364138 ) ) ;
#7851=ADVANCED_FACE ( 'NONE', ( #16006 ), #62206, .T. ) ;
#7856=EDGE_CURVE ( 'NONE', #82017, #50385, #66777, .T. ) ;
#7862=EDGE_LOOP ( 'NONE', ( #8187, #56997, #22115, #70143 ) ) ;
#7865=ORIENTED_EDGE ( 'NONE', *, *, #91115, .T. ) ;
#7873=CARTESIAN_POINT ( 'NONE',  ( -10.27832545704433365, 4.855524038559839717, 28.80005113363453972 ) ) ;
#7888=EDGE_LOOP ( 'NONE', ( #45994, #3919 ) ) ;
#7893=DIRECTION ( 'NONE',  ( 0.000000000000000000, -1.000000000000000000, 0.000000000000000000 ) ) ;
#7907=AXIS2_PLACEMENT_3D ( 'NONE', #7837, #55026, #16441 ) ;
#7913=DIRECTION ( 'NONE',  ( 0.9994733861282923959, 0.000000000000000000, 0.03244919754393515293 ) ) ;
#7917=VERTEX_POINT ( 'NONE', #53098 ) ;
#7928=DIRECTION ( 'NONE',  ( -0.000000000000000000, 1.000000000000000000, -0.000000000000000000 ) ) ;
#7932=EDGE_CURVE ( 'NONE', #23364, #94830, #54097, .T. ) ;
#7959=AXIS2_PLACEMENT_3D ( 'NONE', #46053, #8479, #6483 ) ;
#7966=CIRCLE ( 'NONE', #4799, 2.499999999999995115 ) ;
#7974=ORIENTED_EDGE ( 'NONE', *, *, #87345, .T. ) ;
#7975=AXIS2_PLACEMENT_3D ( 'NONE', #7103, #70004, #93331 ) ;
#8009=DIRECTION ( 'NONE',  ( -1.334402673828313093E-16, -0.000000000000000000, -1.000000000000000000 ) ) ;
#8041=EDGE_LOOP ( 'NONE', ( #16342, #79500, #45109, #4477 ) ) ;
#8047=CARTESIAN_POINT ( 'NONE',  ( 5.250998264632098511, 5.356774720514425603, -25.47015671074453280 ) ) ;
#8069=CARTESIAN_POINT ( 'NONE',  ( 14.61581670307174008, 2.682774720514426559, -27.35847990810646024 ) ) ;
#8071=EDGE_CURVE ( 'NONE', #12577, #74051, #33749, .T. ) ;
#8099=FACE_OUTER_BOUND ( 'NONE', #74777, .T. ) ;
#8104=ADVANCED_FACE ( 'NONE', ( #57103 ), #88040, .F. ) ;
#8108=FACE_OUTER_BOUND ( 'NONE', #33456, .T. ) ;
#8115=EDGE_CURVE ( 'NONE', #86861, #41039, #49991, .T. ) ;
#8118=CIRCLE ( 'NONE', #67882, 6.000000000000000888 ) ;
#8132=AXIS2_PLACEMENT_3D ( 'NONE', #97877, #90282, #11650 ) ;
#8149=B_SPLINE_CURVE_WITH_KNOTS ( 'NONE', 3,
 ( #33393, #39516, #78555, #94291, #17674, #70468 ),
 .UNSPECIFIED., .F., .F.,
 ( 4, 2, 4 ),
 ( 0.000000000000000000, 0.5000000000000000000, 1.000000000000000000 ),
 .UNSPECIFIED. ) ;
#8160=DIRECTION ( 'NONE',  ( 0.000000000000000000, 0.000000000000000000, -1.000000000000000000 ) ) ;
#8187=ORIENTED_EDGE ( 'NONE', *, *, #38850, .F. ) ;
#8216=EDGE_CURVE ( 'NONE', #6907, #54320, #11904, .T. ) ;
#8223=CARTESIAN_POINT ( 'NONE',  ( 14.83405752585509596, 4.881907540129173384, -27.54622755360215791 ) ) ;
#8231=ADVANCED_FACE ( 'NONE', ( #50980 ), #82902, .F. ) ;
#8233=DIRECTION ( 'NONE',  ( 0.000000000000000000, 0.000000000000000000, -1.000000000000000000 ) ) ;
#8290=CARTESIAN_POINT ( 'NONE',  ( 30.93860345374796594, -6.475225279485573360, 19.84760796525321780 ) ) ;
#8305=EDGE_CURVE ( 'NONE', #20861, #47172, #40109, .T. ) ;
#8313=VECTOR ( 'NONE', #37757, 1000.000000000000000 ) ;
#8336=ORIENTED_EDGE ( 'NONE', *, *, #74542, .F. ) ;
#8353=CARTESIAN_POINT ( 'NONE',  ( 282.9764569301858046, -5.965225279485572685, 20.79159422840526616 ) ) ;
#8359=ORIENTED_EDGE ( 'NONE', *, *, #85474, .T. ) ;
#8361=DIRECTION ( 'NONE',  ( 0.9161084732596777025, -7.885106708985488048E-16, -0.4009304992412306978 ) ) ;
#8363=CARTESIAN_POINT ( 'NONE',  ( 14.76093561896379214, 3.316774720514426456, -27.37148769130089931 ) ) ;
#8375=DIRECTION ( 'NONE',  ( 0.000000000000000000, 1.000000000000000000, 0.000000000000000000 ) ) ;
#8384=CIRCLE ( 'NONE', #97472, 6.000000000000000888 ) ;
#8401=CARTESIAN_POINT ( 'NONE',  ( -23.62875734969026453, -6.143225279485574397, 23.50402280011862288 ) ) ;
#8406=ORIENTED_EDGE ( 'NONE', *, *, #63432, .F. ) ;
#8416=ADVANCED_FACE ( 'NONE', ( #17265 ), #86775, .T. ) ;
#8417=CYLINDRICAL_SURFACE ( 'NONE', #79540, 1.325999999999943446 ) ;
#8420=ORIENTED_EDGE ( 'NONE', *, *, #50567, .T. ) ;
#8423=ADVANCED_FACE ( 'NONE', ( #79160, #25377 ), #87274, .F. ) ;
#8425=DIRECTION ( 'NONE',  ( -0.000000000000000000, 1.000000000000000000, -0.000000000000000000 ) ) ;
#8429=ADVANCED_FACE ( 'NONE', ( #34993 ), #43112, .T. ) ;
#8445=DIRECTION ( 'NONE',  ( -0.6599726524652352877, 0.000000000000000000, 0.7512896232465892110 ) ) ;
#8457=VECTOR ( 'NONE', #330, 1000.000000000000000 ) ;
#8459=DIRECTION ( 'NONE',  ( -0.000000000000000000, -1.000000000000000000, 0.000000000000000000 ) ) ;
#8461=CARTESIAN_POINT ( 'NONE',  ( 22.81105451610979173, -6.475225279485573360, -20.71691820600746681 ) ) ;
#8463=DIRECTION ( 'NONE',  ( 0.09721092304694051167, 0.000000000000000000, -0.9952638024365005887 ) ) ;
#8465=ORIENTED_EDGE ( 'NONE', *, *, #73953, .F. ) ;
#8479=DIRECTION ( 'NONE',  ( -0.000000000000000000, -1.000000000000000000, -0.000000000000000000 ) ) ;
#8490=ORIENTED_EDGE ( 'NONE', *, *, #34263, .F. ) ;
#8493=ORIENTED_EDGE ( 'NONE', *, *, #93110, .T. ) ;
#8495=VERTEX_POINT ( 'NONE', #19748 ) ;
#8504=CARTESIAN_POINT ( 'NONE',  ( 14.52511747680497933, -5.965225279485572685, -27.86035006098926559 ) ) ;
#8512=ORIENTED_EDGE ( 'NONE', *, *, #98582, .T. ) ;
#8516=CARTESIAN_POINT ( 'NONE',  ( 29.73860345376319003, -1.477225279485574028, 19.84760796525321780 ) ) ;
#8543=PLANE ( 'NONE',  #71882 ) ;
#8544=PLANE ( 'NONE',  #82715 ) ;
#8562=EDGE_CURVE ( 'NONE', #74181, #48376, #99102, .T. ) ;
#8568=CARTESIAN_POINT ( 'NONE',  ( 11.98973536156539943, 2.682774720514426559, -26.26140391504922178 ) ) ;
#8573=LINE ( 'NONE', #10068, #35848 ) ;
#8587=AXIS2_PLACEMENT_3D ( 'NONE', #26661, #41901, #10426 ) ;
#8595=EDGE_CURVE ( 'NONE', #52090, #88744, #59838, .T. ) ;
#8596=DIRECTION ( 'NONE',  ( -0.3133898629642186684, 0.000000000000000000, 0.9496245541219267006 ) ) ;
#8611=EDGE_CURVE ( 'NONE', #22611, #149, #63406, .T. ) ;
#8613=ORIENTED_EDGE ( 'NONE', *, *, #16315, .T. ) ;
#8619=EDGE_LOOP ( 'NONE', ( #60818, #37687, #21358, #81138 ) ) ;
#8630=CIRCLE ( 'NONE', #44270, 1.149999999999999911 ) ;
#8636=EDGE_CURVE ( 'NONE', #81022, #17829, #75531, .T. ) ;
#8673=VECTOR ( 'NONE', #76047, 1000.000000000000000 ) ;
#8694=LINE ( 'NONE', #93409, #32813 ) ;
#8703=CARTESIAN_POINT ( 'NONE',  ( 9.818046095181445665, 6.376774720513751937, -28.04791983960493695 ) ) ;
#8706=EDGE_LOOP ( 'NONE', ( #29697, #46836, #21403, #4783 ) ) ;
#8712=DIRECTION ( 'NONE',  ( -0.9888510809027408754, 0.000000000000000000, -0.1489078231574183231 ) ) ;
#8728=DIRECTION ( 'NONE',  ( -0.000000000000000000, 1.000000000000000000, -0.000000000000000000 ) ) ;
#8729=VERTEX_POINT ( 'NONE', #84151 ) ;
#8732=CIRCLE ( 'NONE', #11995, 251.4258649670780699 ) ;
#8735=PLANE ( 'NONE',  #4787 ) ;
#8745=ORIENTED_EDGE ( 'NONE', *, *, #21123, .F. ) ;
#8761=EDGE_CURVE ( 'NONE', #16980, #23842, #36035, .T. ) ;
#8785=EDGE_CURVE ( 'NONE', #6907, #31632, #63348, .T. ) ;
#8786=EDGE_LOOP ( 'NONE', ( #35320, #70752, #31595, #62069 ) ) ;
#8789=ORIENTED_EDGE ( 'NONE', *, *, #68744, .T. ) ;
#8790=CARTESIAN_POINT ( 'NONE',  ( -4.993225604111835914, -5.965225279485592225, -29.11654937215278593 ) ) ;
#8801=ORIENTED_EDGE ( 'NONE', *, *, #87931, .T. ) ;
#8806=ADVANCED_FACE ( 'NONE', ( #93767 ), #24257, .T. ) ;
#8807=VECTOR ( 'NONE', #79511, 1000.000000000000000 ) ;
#8833=VECTOR ( 'NONE', #39522, 1000.000000000000000 ) ;
#8845=FACE_OUTER_BOUND ( 'NONE', #54105, .T. ) ;
#8853=EDGE_LOOP ( 'NONE', ( #18878, #79136, #3344, #37036 ) ) ;
#8859=ORIENTED_EDGE ( 'NONE', *, *, #26757, .T. ) ;
#8868=ORIENTED_EDGE ( 'NONE', *, *, #89096, .F. ) ;
#8888=ORIENTED_EDGE ( 'NONE', *, *, #33182, .F. ) ;
#8919=LINE ( 'NONE', #3336, #69248 ) ;
#8942=CARTESIAN_POINT ( 'NONE',  ( 30.53060340732036693, 4.740362442169048229, -2.970849955429423872 ) ) ;
#8943=FACE_OUTER_BOUND ( 'NONE', #88476, .T. ) ;
#8945=ORIENTED_EDGE ( 'NONE', *, *, #31472, .F. ) ;
#8949=CARTESIAN_POINT ( 'NONE',  ( -22.05275734969026047, -5.965225279485572685, 31.02402280011862246 ) ) ;
#8965=FACE_OUTER_BOUND ( 'NONE', #30901, .T. ) ;
#8975=VECTOR ( 'NONE', #97695, 1000.000000000000000 ) ;
#8990=ORIENTED_EDGE ( 'NONE', *, *, #4337, .F. ) ;
#9014=CIRCLE ( 'NONE', #88401, 84.48086791635432746 ) ;
#9018=ORIENTED_EDGE ( 'NONE', *, *, #91792, .F. ) ;
#9021=AXIS2_PLACEMENT_3D ( 'NONE', #58483, #36130, #49878 ) ;
#9031=ORIENTED_EDGE ( 'NONE', *, *, #40405, .F. ) ;
#9049=DIRECTION ( 'NONE',  ( 0.000000000000000000, 0.000000000000000000, -1.000000000000000000 ) ) ;
#9055=CYLINDRICAL_SURFACE ( 'NONE', #20369, 3.979149600822063704 ) ;
#9073=CARTESIAN_POINT ( 'NONE',  ( -19.80875734969026425, -5.965225279485572685, 31.02402280011862246 ) ) ;
#9087=VECTOR ( 'NONE', #97290, 1000.000000000000000 ) ;
#9090=AXIS2_PLACEMENT_3D ( 'NONE', #83299, #13779, #14281 ) ;
#9114=PLANE ( 'NONE',  #81741 ) ;
#9137=AXIS2_PLACEMENT_3D ( 'NONE', #94302, #46143, #38521 ) ;
#9144=EDGE_LOOP ( 'NONE', ( #33586, #62177, #85307, #15851 ) ) ;
#9145=CIRCLE ( 'NONE', #65898, 3.500000000000000000 ) ;
#9159=DIRECTION ( 'NONE',  ( -7.994117400814786717E-16, -0.000000000000000000, 1.000000000000000000 ) ) ;
#9179=CARTESIAN_POINT ( 'NONE',  ( 27.53860345374784657, 1.682774720514426114, -8.321925749325748356 ) ) ;
#9188=VERTEX_POINT ( 'NONE', #14521 ) ;
#9191=CARTESIAN_POINT ( 'NONE',  ( 11.40529837384167777, 3.316774720514342967, -28.07356074712937044 ) ) ;
#9209=CYLINDRICAL_SURFACE ( 'NONE', #4312, 130.7884398600581335 ) ;
#9213=VECTOR ( 'NONE', #25984, 1000.000000000000000 ) ;
#9221=ORIENTED_EDGE ( 'NONE', *, *, #46047, .T. ) ;
#9235=ORIENTED_EDGE ( 'NONE', *, *, #90540, .F. ) ;
#9242=EDGE_CURVE ( 'NONE', #47768, #48919, #83534, .T. ) ;
#9253=DIRECTION ( 'NONE',  ( -5.551115123125793746E-15, 0.000000000000000000, -1.000000000000000000 ) ) ;
#9256=AXIS2_PLACEMENT_3D ( 'NONE', #59610, #97655, #51992 ) ;
#9259=ORIENTED_EDGE ( 'NONE', *, *, #84505, .F. ) ;
#9274=AXIS2_PLACEMENT_3D ( 'NONE', #41006, #87676, #40508 ) ;
#9276=ORIENTED_EDGE ( 'NONE', *, *, #36706, .F. ) ;
#9283=VECTOR ( 'NONE', #76229, 1000.000000000000000 ) ;
#9284=DIRECTION ( 'NONE',  ( -0.9976052577199500115, 0.000000000000000000, -0.06916465693916190594 ) ) ;
#9293=VERTEX_POINT ( 'NONE', #15515 ) ;
#9295=DIRECTION ( 'NONE',  ( -0.000000000000000000, -1.000000000000000000, -0.000000000000000000 ) ) ;
#9318=AXIS2_PLACEMENT_3D ( 'NONE', #78392, #10393, #49478 ) ;
#9319=ADVANCED_FACE ( 'NONE', ( #68822 ), #92641, .F. ) ;
#9332=CARTESIAN_POINT ( 'NONE',  ( 30.45304879119406394, 1.682774720514426114, -10.07140455160086567 ) ) ;
#9336=EDGE_CURVE ( 'NONE', #12272, #63916, #77907, .T. ) ;
#9340=AXIS2_PLACEMENT_3D ( 'NONE', #54604, #70327, #24141 ) ;
#9341=ORIENTED_EDGE ( 'NONE', *, *, #13400, .T. ) ;
#9363=LINE ( 'NONE', #71780, #97200 ) ;
#9371=DIRECTION ( 'NONE',  ( -0.000000000000000000, 1.000000000000000000, -0.000000000000000000 ) ) ;
#9376=ORIENTED_EDGE ( 'NONE', *, *, #76019, .T. ) ;
#9402=VECTOR ( 'NONE', #96275, 1000.000000000000000 ) ;
#9406=DIRECTION ( 'NONE',  ( -1.000000000000000000, 0.000000000000000000, 0.000000000000000000 ) ) ;
#9416=FACE_OUTER_BOUND ( 'NONE', #59700, .T. ) ;
#9418=AXIS2_PLACEMENT_3D ( 'NONE', #60248, #74937, #20656 ) ;
#9425=DIRECTION ( 'NONE',  ( -0.000000000000000000, -0.000000000000000000, 1.000000000000000000 ) ) ;
#9440=AXIS2_PLACEMENT_3D ( 'NONE', #18326, #65531, #89342 ) ;
#9442=LINE ( 'NONE', #54137, #53874 ) ;
#9446=ADVANCED_FACE ( 'NONE', ( #34265 ), #56108, .T. ) ;
#9453=AXIS2_PLACEMENT_3D ( 'NONE', #62134, #17443, #32166 ) ;
#9467=EDGE_CURVE ( 'NONE', #28216, #88881, #26140, .T. ) ;
#9469=DIRECTION ( 'NONE',  ( 0.000000000000000000, 0.000000000000000000, -1.000000000000000000 ) ) ;
#9470=ORIENTED_EDGE ( 'NONE', *, *, #15639, .T. ) ;
#9499=CARTESIAN_POINT ( 'NONE',  ( 29.70435979725210274, 3.845442984095253536, 28.14021868772163160 ) ) ;
#9501=DIRECTION ( 'NONE',  ( -0.000000000000000000, 1.000000000000000000, -0.000000000000000000 ) ) ;
#9502=EDGE_CURVE ( 'NONE', #5789, #42735, #18026, .T. ) ;
#9509=ORIENTED_EDGE ( 'NONE', *, *, #48468, .T. ) ;
#9552=LINE ( 'NONE', #17667, #22313 ) ;
#9574=AXIS2_PLACEMENT_3D ( 'NONE', #41285, #18444, #16940 ) ;
#9583=EDGE_CURVE ( 'NONE', #51818, #76194, #82913, .T. ) ;
#9588=CARTESIAN_POINT ( 'NONE',  ( 33.63416148851499088, 3.931067265920685561, -11.97433369283768734 ) ) ;
#9599=VERTEX_POINT ( 'NONE', #35763 ) ;
#9615=ORIENTED_EDGE ( 'NONE', *, *, #63852, .F. ) ;
#9617=FACE_OUTER_BOUND ( 'NONE', #68677, .T. ) ;
#9633=VECTOR ( 'NONE', #33185, 1000.000000000000000 ) ;
#9637=( NAMED_UNIT ( * ) PLANE_ANGLE_UNIT ( ) SI_UNIT ( $, .RADIAN. ) );
#9654=ORIENTED_EDGE ( 'NONE', *, *, #45916, .T. ) ;
#9663=APPLICATION_CONTEXT ( 'configuration controlled 3d designs of mechanical parts and assemblies' ) ;
#9681=DIRECTION ( 'NONE',  ( 0.000000000000000000, -0.000000000000000000, -1.000000000000000000 ) ) ;
#9687=FACE_OUTER_BOUND ( 'NONE', #21059, .T. ) ;
#9702=AXIS2_PLACEMENT_3D ( 'NONE', #65730, #49496, #42880 ) ;
#9729=CARTESIAN_POINT ( 'NONE',  ( 29.58524742607616176, 4.112217781777255610, 29.11978736867098760 ) ) ;
#9753=FACE_OUTER_BOUND ( 'NONE', #24210, .T. ) ;
#9778=CARTESIAN_POINT ( 'NONE',  ( 25.25345159561841868, 4.807191536106888208, -10.50260803520238895 ) ) ;
#9782=ORIENTED_EDGE ( 'NONE', *, *, #68327, .T. ) ;
#9787=CIRCLE ( 'NONE', #84304, 80.18232118519037499 ) ;
#9831=CARTESIAN_POINT ( 'NONE',  ( -12.65407072091355722, 0.3587747205143968499, -26.15404995688569301 ) ) ;
#9833=DIRECTION ( 'NONE',  ( 0.000000000000000000, -0.000000000000000000, -1.000000000000000000 ) ) ;
#9834=CIRCLE ( 'NONE', #61719, 132.8284398600581824 ) ;
#9838=CARTESIAN_POINT ( 'NONE',  ( 29.73860345376319003, 5.356774720496559894, 19.84760796525321780 ) ) ;
#9846=CARTESIAN_POINT ( 'NONE',  ( -10.40290173325841216, 6.376774720514426953, 27.45402280011861862 ) ) ;
#9849=CYLINDRICAL_SURFACE ( 'NONE', #31827, 12.23252173913042995 ) ;
#9859=ORIENTED_EDGE ( 'NONE', *, *, #5950, .T. ) ;
#9869=CARTESIAN_POINT ( 'NONE',  ( 30.53060340732035982, -1.477225279485574028, 19.84760796525321780 ) ) ;
#9882=VERTEX_POINT ( 'NONE', #99624 ) ;
#9899=ORIENTED_EDGE ( 'NONE', *, *, #29719, .F. ) ;
#9913=DIRECTION ( 'NONE',  ( -1.000000000000000000, 0.000000000000000000, 0.000000000000000000 ) ) ;
#9919=ORIENTED_EDGE ( 'NONE', *, *, #32964, .T. ) ;
#9923=CARTESIAN_POINT ( 'NONE',  ( 30.77956504631911017, 6.277769580494330093, 0.6965969997247714041 ) ) ;
#9942=CARTESIAN_POINT ( 'NONE',  ( 5.087148743171193033, 3.314277014504871222, -27.56324057082087364 ) ) ;
#9943=CARTESIAN_POINT ( 'NONE',  ( 30.53060340732036693, 5.234153290856875529, 0.4067587357809892556 ) ) ;
#9952=LINE ( 'NONE', #35305, #7032 ) ;
#9965=CARTESIAN_POINT ( 'NONE',  ( 13.10664265030973930, 0.3587747205144256601, -28.18129937523770678 ) ) ;
#9971=EDGE_LOOP ( 'NONE', ( #79923, #15101, #4026, #2415 ) ) ;
#9983=CARTESIAN_POINT ( 'NONE',  ( 10.27515206207115739, 5.152774720514427642, -28.04856579873300149 ) ) ;
#9984=DIRECTION ( 'NONE',  ( 0.000000000000000000, 0.000000000000000000, -1.000000000000000000 ) ) ;
#9985=VERTEX_POINT ( 'NONE', #89919 ) ;
#10013=VERTEX_POINT ( 'NONE', #20388 ) ;
#10028=EDGE_CURVE ( 'NONE', #28216, #94830, #67594, .T. ) ;
#10034=VECTOR ( 'NONE', #25118, 1000.000000000000000 ) ;
#10043=LINE ( 'NONE', #24758, #12729 ) ;
#10061=EDGE_CURVE ( 'NONE', #69079, #33824, #71749, .T. ) ;
#10068=CARTESIAN_POINT ( 'NONE',  ( 33.13288845015618023, -5.965225279485572685, -0.1650522222209214185 ) ) ;
#10083=EDGE_CURVE ( 'NONE', #4321, #19038, #16285, .T. ) ;
#10085=ORIENTED_EDGE ( 'NONE', *, *, #7411, .T. ) ;
#10087=CARTESIAN_POINT ( 'NONE',  ( -28.32169924589829080, 0.3587747205143964613, -8.244178532169451401 ) ) ;
#10098=CARTESIAN_POINT ( 'NONE',  ( 33.40725018382580913, 3.504198967030887069, -12.51830322776342008 ) ) ;
#10101=CARTESIAN_POINT ( 'NONE',  ( -4.568292318365942073, 0.3587747205144265483, 30.06720597538392425 ) ) ;
#10114=EDGE_LOOP ( 'NONE', ( #9899, #82309, #77769, #4438 ) ) ;
#10115=DIRECTION ( 'NONE',  ( 0.000000000000000000, 1.000000000000000000, -0.000000000000000000 ) ) ;
#10126=CARTESIAN_POINT ( 'NONE',  ( 32.40199294184733247, -6.475225279485576024, -12.82361242714783245 ) ) ;
#10130=CARTESIAN_POINT ( 'NONE',  ( 15.99960863614631101, 3.577630190450212577, -27.91116951066581819 ) ) ;
#10133=EDGE_CURVE ( 'NONE', #24258, #87883, #46747, .T. ) ;
#10153=ORIENTED_EDGE ( 'NONE', *, *, #94936, .T. ) ;
#10172=FACE_OUTER_BOUND ( 'NONE', #19485, .T. ) ;
#10174=LINE ( 'NONE', #85797, #69159 ) ;
#10193=VECTOR ( 'NONE', #76237, 1000.000000000000000 ) ;
#10204=ADVANCED_FACE ( 'NONE', ( #70579 ), #94413, .T. ) ;
#10205=ORIENTED_EDGE ( 'NONE', *, *, #11203, .T. ) ;
#10206=CARTESIAN_POINT ( 'NONE',  ( 29.77147767949870527, 4.540774720514427543, 26.15915692125055614 ) ) ;
#10208=LINE ( 'NONE', #63513, #49303 ) ;
#10210=DIRECTION ( 'NONE',  ( -0.000000000000000000, 1.000000000000000000, -0.000000000000000000 ) ) ;
#10218=CARTESIAN_POINT ( 'NONE',  ( -13.89275734969026388, 0.3587747205144262708, 31.02402280011862246 ) ) ;
#10223=FACE_OUTER_BOUND ( 'NONE', #45092, .T. ) ;
#10229=DIRECTION ( 'NONE',  ( -1.000000000000000000, 0.000000000000000000, -0.000000000000000000 ) ) ;
#10246=VERTEX_POINT ( 'NONE', #95916 ) ;
#10262=CYLINDRICAL_SURFACE ( 'NONE', #74467, 1.836000000000000743 ) ;
#10264=VECTOR ( 'NONE', #43421, 1000.000000000000000 ) ;
#10266=VERTEX_POINT ( 'NONE', #33518 ) ;
#10280=LINE ( 'NONE', #26513, #93312 ) ;
#10286=ORIENTED_EDGE ( 'NONE', *, *, #94882, .T. ) ;
#10294=CARTESIAN_POINT ( 'NONE',  ( -10.21384395349174490, 3.316774720514427344, 29.49402280011862487 ) ) ;
#10305=VERTEX_POINT ( 'NONE', #63492 ) ;
#10326=EDGE_CURVE ( 'NONE', #21001, #41837, #10684, .T. ) ;
#10327=VECTOR ( 'NONE', #18514, 1000.000000000000000 ) ;
#10351=CARTESIAN_POINT ( 'NONE',  ( -10.18932761084327865, 5.341047792237469949, 29.75743496038930758 ) ) ;
#10355=DIRECTION ( 'NONE',  ( 0.000000000000000000, 0.000000000000000000, -1.000000000000000000 ) ) ;
#10367=DIRECTION ( 'NONE',  ( -0.000000000000000000, -1.000000000000000000, -0.000000000000000000 ) ) ;
#10368=CARTESIAN_POINT ( 'NONE',  ( 2.449489742783179214, -16.94322527948557422, 2.499999999999999112 ) ) ;
#10384=ADVANCED_FACE ( 'NONE', ( #65997 ), #58369, .F. ) ;
#10385=EDGE_LOOP ( 'NONE', ( #15638, #75770, #94801, #53958 ) ) ;
#10393=DIRECTION ( 'NONE',  ( 0.000000000000000000, -1.000000000000000000, 0.000000000000000000 ) ) ;
#10402=LINE ( 'NONE', #56602, #79380 ) ;
#10419=CYLINDRICAL_SURFACE ( 'NONE', #66103, 1.699999999999998401 ) ;
#10426=DIRECTION ( 'NONE',  ( 0.000000000000000000, 0.000000000000000000, 1.000000000000000000 ) ) ;
#10432=LINE ( 'NONE', #96670, #74736 ) ;
#10444=CARTESIAN_POINT ( 'NONE',  ( 15.32643653063178668, 3.582999323269832725, -27.14485409495428314 ) ) ;
#10466=CARTESIAN_POINT ( 'NONE',  ( 25.83488407601165093, 4.132774720514426292, -11.31196583263648137 ) ) ;
#10488=EDGE_LOOP ( 'NONE', ( #64313, #79865, #43674, #63053, #45254, #16705, #1316, #73928, #29473, #67952, #52929 ) ) ;
#10490=ORIENTED_EDGE ( 'NONE', *, *, #27894, .T. ) ;
#10499=PLANE ( 'NONE',  #14133 ) ;
#10541=DIRECTION ( 'NONE',  ( 1.232047923278981953E-16, -1.000000000000000000, 0.000000000000000000 ) ) ;
#10555=LINE ( 'NONE', #61740, #4946 ) ;
#10566=LINE ( 'NONE', #24296, #23429 ) ;
#10573=ORIENTED_EDGE ( 'NONE', *, *, #86984, .T. ) ;
#10574=CIRCLE ( 'NONE', #67304, 28.96799999999999642 ) ;
#10582=CARTESIAN_POINT ( 'NONE',  ( 33.64447732616053344, 3.738877066258443627, -11.77943383154337376 ) ) ;
#10584=DIRECTION ( 'NONE',  ( 1.000000000000000000, -0.000000000000000000, -0.000000000000000000 ) ) ;
#10588=EDGE_CURVE ( 'NONE', #18475, #31114, #93654, .T. ) ;
#10600=VECTOR ( 'NONE', #82606, 1000.000000000000000 ) ;
#10615=EDGE_CURVE ( 'NONE', #85130, #78621, #39282, .T. ) ;
#10617=LINE ( 'NONE', #34459, #50293 ) ;
#10622=AXIS2_PLACEMENT_3D ( 'NONE', #14698, #7091, #61399 ) ;
#10635=ORIENTED_EDGE ( 'NONE', *, *, #55309, .F. ) ;
#10639=( LENGTH_UNIT ( ) NAMED_UNIT ( * ) SI_UNIT ( .MILLI., .METRE. ) );
#10649=LINE ( 'NONE', #26372, #3217 ) ;
#10671=PLANE ( 'NONE',  #30281 ) ;
#10684=LINE ( 'NONE', #17289, #31167 ) ;
#10687=CARTESIAN_POINT ( 'NONE',  ( 10.11589461582716076, 3.316774720514427344, -28.03692668899584106 ) ) ;
#10691=VECTOR ( 'NONE', #79699, 1000.000000000000000 ) ;
#10700=LINE ( 'NONE', #30650, #90070 ) ;
#10709=CARTESIAN_POINT ( 'NONE',  ( 26.73860345374794889, 5.356774720514427379, -3.111611894936215705 ) ) ;
#10715=ADVANCED_FACE ( 'NONE', ( #77422 ), #23134, .F. ) ;
#10721=ADVANCED_FACE ( 'NONE', ( #56627 ), #2837, .F. ) ;
#10730=ORIENTED_EDGE ( 'NONE', *, *, #88332, .T. ) ;
#10732=ORIENTED_EDGE ( 'NONE', *, *, #42025, .F. ) ;
#10739=CARTESIAN_POINT ( 'NONE',  ( 15.07033713866346147, 3.525255902978593703, -27.30453278895961233 ) ) ;
#10752=AXIS2_PLACEMENT_3D ( 'NONE', #38804, #87863, #41194 ) ;
#10754=ORIENTED_EDGE ( 'NONE', *, *, #10960, .F. ) ;
#10762=CARTESIAN_POINT ( 'NONE',  ( -27.96875734969026084, -6.143225279485574397, 24.50402280011861933 ) ) ;
#10787=CARTESIAN_POINT ( 'NONE',  ( 25.53193795238742325, 4.590426722874489940, -10.98904603773835476 ) ) ;
#10790=ORIENTED_EDGE ( 'NONE', *, *, #86927, .T. ) ;
#10791=CARTESIAN_POINT ( 'NONE',  ( 32.98733314340959311, 0.3587747205144265483, 2.074222136288530027 ) ) ;
#10802=ORIENTED_EDGE ( 'NONE', *, *, #96644, .T. ) ;
#10809=AXIS2_PLACEMENT_3D ( 'NONE', #54266, #99413, #85194 ) ;
#10813=VERTEX_POINT ( 'NONE', #96664 ) ;
#10823=CARTESIAN_POINT ( 'NONE',  ( 32.50838937279095120, 2.682774720514426559, -10.74666623472941218 ) ) ;
#10825=EDGE_CURVE ( 'NONE', #37448, #71104, #13423, .T. ) ;
#10830=EDGE_CURVE ( 'NONE', #22614, #72334, #89061, .T. ) ;
#10833=EDGE_LOOP ( 'NONE', ( #95535, #18876, #14621, #19864 ) ) ;
#10858=CARTESIAN_POINT ( 'NONE',  ( -10.12789510953808758, 4.109924279452578766, 30.41617935552199370 ) ) ;
#10861=AXIS2_PLACEMENT_3D ( 'NONE', #39857, #22122, #76903 ) ;
#10873=ORIENTED_EDGE ( 'NONE', *, *, #52594, .T. ) ;
#10874=DIRECTION ( 'NONE',  ( -0.000000000000000000, -1.000000000000000000, -0.000000000000000000 ) ) ;
#10880=CARTESIAN_POINT ( 'NONE',  ( -29.49875734969026198, -5.965225279485572685, 7.870022800118625206 ) ) ;
#10888=DIRECTION ( 'NONE',  ( 0.000000000000000000, -1.000000000000000000, 0.000000000000000000 ) ) ;
#10896=CARTESIAN_POINT ( 'NONE',  ( 3.421177667410919110, 6.376774720514426953, 28.69411518427638441 ) ) ;
#10900=CARTESIAN_POINT ( 'NONE',  ( -0.02075734969026145696, 6.376774720514426953, -22.78097719988138081 ) ) ;
#10919=PRODUCT_DEFINITION ( 'UNKNOWN', '', #96051, #21544 ) ;
#10934=DIRECTION ( 'NONE',  ( -0.06486421869277853025, 0.000000000000000000, 0.9978940991575085961 ) ) ;
#10951=CYLINDRICAL_SURFACE ( 'NONE', #6856, 0.8160000000000007248 ) ;
#10957=VECTOR ( 'NONE', #70467, 1000.000000000000000 ) ;
#10960=EDGE_CURVE ( 'NONE', #73137, #42999, #51005, .T. ) ;
#10961=CARTESIAN_POINT ( 'NONE',  ( 14.43441819135840376, 3.316774720514426456, -28.36222020317694970 ) ) ;
#10979=DIRECTION ( 'NONE',  ( 0.000000000000000000, -1.000000000000000000, 0.000000000000000000 ) ) ;
#10983=ORIENTED_EDGE ( 'NONE', *, *, #97084, .F. ) ;
#10990=CARTESIAN_POINT ( 'NONE',  ( 13.91401389203221406, 3.316774720514426456, 158.0376437107427137 ) ) ;
#11016=EDGE_CURVE ( 'NONE', #57584, #76588, #45389, .T. ) ;
#11026=CARTESIAN_POINT ( 'NONE',  ( 5.109298100548420152, 3.316774720514426456, -27.55941679637948383 ) ) ;
#11029=ORIENTED_EDGE ( 'NONE', *, *, #78604, .F. ) ;
#11034=CARTESIAN_POINT ( 'NONE',  ( -24.90875734969025501, 6.376774720514426953, 26.43402280011862615 ) ) ;
#11045=VECTOR ( 'NONE', #79963, 1000.000000000000114 ) ;
#11050=VERTEX_POINT ( 'NONE', #46878 ) ;
#11051=LINE ( 'NONE', #63362, #75684 ) ;
#11077=FACE_OUTER_BOUND ( 'NONE', #91033, .T. ) ;
#11093=CIRCLE ( 'NONE', #74327, 27.94799999999999685 ) ;
#11107=VECTOR ( 'NONE', #16071, 1000.000000000000000 ) ;
#11143=DIRECTION ( 'NONE',  ( 0.000000000000000000, -1.000000000000000000, 0.000000000000000000 ) ) ;
#11146=ORIENTED_EDGE ( 'NONE', *, *, #45361, .F. ) ;
#11148=DIRECTION ( 'NONE',  ( -0.000000000000000000, 1.000000000000000000, -0.000000000000000000 ) ) ;
#11158=VECTOR ( 'NONE', #5740, 1000.000000000000000 ) ;
#11166=CYLINDRICAL_SURFACE ( 'NONE', #36809, 3.500000000000000000 ) ;
#11184=DIRECTION ( 'NONE',  ( 0.000000000000000000, 0.000000000000000000, 1.000000000000000000 ) ) ;
#11187=FACE_BOUND ( 'NONE', #74900, .T. ) ;
#11192=LINE ( 'NONE', #20281, #33486 ) ;
#11197=DIRECTION ( 'NONE',  ( -0.000000000000000000, -1.000000000000000000, -0.000000000000000000 ) ) ;
#11203=EDGE_CURVE ( 'NONE', #80239, #96754, #714, .T. ) ;
#11208=DIRECTION ( 'NONE',  ( -1.000000000000000000, -1.232047923278981953E-16, 0.000000000000000000 ) ) ;
#11214=FACE_OUTER_BOUND ( 'NONE', #19629, .T. ) ;
#11223=CARTESIAN_POINT ( 'NONE',  ( 14.97568007497113385, 3.504021928054863899, -28.39450375387846748 ) ) ;
#11228=ORIENTED_EDGE ( 'NONE', *, *, #79879, .F. ) ;
#11230=CARTESIAN_POINT ( 'NONE',  ( 31.63187483939985256, 3.931892516571728446, 27.18445229901795557 ) ) ;
#11234=CARTESIAN_POINT ( 'NONE',  ( 15.32643653063177958, 3.577630190450218350, -27.14485409495429380 ) ) ;
#11246=CARTESIAN_POINT ( 'NONE',  ( -10.58858228176428717, -5.965225279485594001, -27.03148018517017093 ) ) ;
#11250=DIRECTION ( 'NONE',  ( 0.000000000000000000, 0.000000000000000000, 1.000000000000000000 ) ) ;
#11262=CARTESIAN_POINT ( 'NONE',  ( 29.77147767949874435, 6.376774720514426953, 26.15915692125051706 ) ) ;
#11267=ORIENTED_EDGE ( 'NONE', *, *, #6109, .F. ) ;
#11268=ADVANCED_FACE ( 'NONE', ( #23508, #63113 ), #32642, .T. ) ;
#11275=DIRECTION ( 'NONE',  ( -0.09721092304694055330, 0.000000000000000000, 0.9952638024365006997 ) ) ;
#11280=CARTESIAN_POINT ( 'NONE',  ( 25.03920237757594691, 5.025550379011072266, -9.721825256066050969 ) ) ;
#11283=ADVANCED_FACE ( 'NONE', ( #55492 ), #86432, .T. ) ;
#11284=VERTEX_POINT ( 'NONE', #25536 ) ;
#11290=DIRECTION ( 'NONE',  ( 0.000000000000000000, 1.000000000000000000, 0.000000000000000000 ) ) ;
#11309=CARTESIAN_POINT ( 'NONE',  ( 27.53860345374936713, 4.772774720514425972, -5.064153531141387918E-12 ) ) ;
#11315=AXIS2_PLACEMENT_3D ( 'NONE', #29543, #15311, #36663 ) ;
#11330=DIRECTION ( 'NONE',  ( -0.000000000000000000, 1.000000000000000000, -0.000000000000000000 ) ) ;
#11338=MANIFOLD_SOLID_BREP ( 'Kes-Ekstr\X2\00fc\X0\zyon27', #80877 ) ;
#11341=LINE ( 'NONE', #72250, #19814 ) ;
#11343=ORIENTED_EDGE ( 'NONE', *, *, #81141, .F. ) ;
#11346=ORIENTED_EDGE ( 'NONE', *, *, #17394, .F. ) ;
#11348=ADVANCED_FACE ( 'NONE', ( #61869 ), #7568, .F. ) ;
#11356=CARTESIAN_POINT ( 'NONE',  ( -10.36589631659242627, 6.376774720514426065, 27.85486277704324110 ) ) ;
#11363=DIRECTION ( 'NONE',  ( -0.1311553622875919756, -6.845827386180409975E-16, -0.9913618264504692190 ) ) ;
#11364=DIRECTION ( 'NONE',  ( 0.000000000000000000, -1.000000000000000000, 0.000000000000000000 ) ) ;
#11365=CARTESIAN_POINT ( 'NONE',  ( 0.000000000000000000, 1.826774720514426464, 0.000000000000000000 ) ) ;
#11416=DIRECTION ( 'NONE',  ( 0.000000000000000000, -1.000000000000000000, 0.000000000000000000 ) ) ;
#11427=DIRECTION ( 'NONE',  ( 0.000000000000000000, -1.000000000000000000, 0.000000000000000000 ) ) ;
#11430=CARTESIAN_POINT ( 'NONE',  ( -65.05438548721848235, 5.356774720514425603, 27.45402280011862572 ) ) ;
#11451=EDGE_CURVE ( 'NONE', #55557, #77754, #97981, .T. ) ;
#11455=( GEOMETRIC_REPRESENTATION_CONTEXT ( 3 ) GLOBAL_UNCERTAINTY_ASSIGNED_CONTEXT ( ( #11456 ) ) GLOBAL_UNIT_ASSIGNED_CONTEXT ( ( #10639, #9637, #41601 ) ) REPRESENTATION_CONTEXT ( 'NONE', 'WORKASPACE' ) );
#11456=UNCERTAINTY_MEASURE_WITH_UNIT (LENGTH_MEASURE( 1.000000000000000082E-05 ), #10639, 'distance_accuracy_value', 'NONE');
#11474=CARTESIAN_POINT ( 'NONE',  ( -25.92875734969026169, 3.316774720514426456, 26.43402280011862615 ) ) ;
#11495=ORIENTED_EDGE ( 'NONE', *, *, #31472, .T. ) ;
#11496=DIRECTION ( 'NONE',  ( -0.000000000000000000, 1.000000000000000000, -0.000000000000000000 ) ) ;
#11508=DIRECTION ( 'NONE',  ( -0.000000000000000000, 1.000000000000000000, -0.000000000000000000 ) ) ;
#11523=EDGE_CURVE ( 'NONE', #5853, #21581, #95308, .T. ) ;
#11538=CARTESIAN_POINT ( 'NONE',  ( 3.176458874063931681, 0.3587747205143967943, -28.85257003503889806 ) ) ;
#11542=DIRECTION ( 'NONE',  ( 0.000000000000000000, 0.000000000000000000, -1.000000000000000000 ) ) ;
#11549=FACE_OUTER_BOUND ( 'NONE', #22566, .T. ) ;
#11556=CARTESIAN_POINT ( 'NONE',  ( 3.421177667410916001, -5.965225279485572685, 28.69411518427638441 ) ) ;
#11565=DIRECTION ( 'NONE',  ( 0.000000000000000000, 0.000000000000000000, 1.000000000000000000 ) ) ;
#11570=CARTESIAN_POINT ( 'NONE',  ( 16.04662828278931741, 3.608091531752042780, -27.86986495919489215 ) ) ;
#11575=ORIENTED_EDGE ( 'NONE', *, *, #32926, .T. ) ;
#11576=EDGE_CURVE ( 'NONE', #65436, #31334, #41079, .T. ) ;
#11597=LINE ( 'NONE', #27828, #48496 ) ;
#11608=VERTEX_POINT ( 'NONE', #79072 ) ;
#11610=CYLINDRICAL_SURFACE ( 'NONE', #64450, 4.300000000000000711 ) ;
#11628=EDGE_CURVE ( 'NONE', #49235, #88649, #10566, .T. ) ;
#11638=EDGE_CURVE ( 'NONE', #82392, #82023, #13192, .T. ) ;
#11639=ORIENTED_EDGE ( 'NONE', *, *, #47190, .T. ) ;
#11648=DIRECTION ( 'NONE',  ( -0.000000000000000000, -1.000000000000000000, -0.000000000000000000 ) ) ;
#11650=DIRECTION ( 'NONE',  ( 0.000000000000000000, 0.000000000000000000, 1.000000000000000000 ) ) ;
#11676=VERTEX_POINT ( 'NONE', #72983 ) ;
#11683=CARTESIAN_POINT ( 'NONE',  ( 1.305682803664691249, -5.965225279485572685, 29.57950906855421991 ) ) ;
#11689=CARTESIAN_POINT ( 'NONE',  ( 7.553089130262996775, 6.316227684668181297, -25.84264253713260828 ) ) ;
#11697=DIRECTION ( 'NONE',  ( -4.251773225433346808E-15, 0.000000000000000000, 1.000000000000000000 ) ) ;
#11709=DIRECTION ( 'NONE',  ( -1.000000000000000000, 0.000000000000000000, 0.000000000000000000 ) ) ;
#11713=LINE ( 'NONE', #66041, #93882 ) ;
#11734=ORIENTED_EDGE ( 'NONE', *, *, #98456, .F. ) ;
#11742=LINE ( 'NONE', #96484, #48687 ) ;
#11765=ORIENTED_EDGE ( 'NONE', *, *, #27573, .F. ) ;
#11773=DIRECTION ( 'NONE',  ( 0.000000000000000000, -1.000000000000000000, 0.000000000000000000 ) ) ;
#11797=EDGE_LOOP ( 'NONE', ( #38353, #95631, #77279, #57961 ) ) ;
#11809=CARTESIAN_POINT ( 'NONE',  ( 32.59332756141815679, 0.6027747205144262654, -11.41404606144462086 ) ) ;
#11824=EDGE_LOOP ( 'NONE', ( #26752, #48864, #94096, #11346 ) ) ;
#11830=DIRECTION ( 'NONE',  ( -1.000000000000000000, 0.000000000000000000, -0.000000000000000000 ) ) ;
#11857=CARTESIAN_POINT ( 'NONE',  ( -0.02075734969026423599, -5.965225279485572685, -28.54397719988136828 ) ) ;
#11859=DIRECTION ( 'NONE',  ( -0.000000000000000000, -1.000000000000000000, -0.000000000000000000 ) ) ;
#11862=DIRECTION ( 'NONE',  ( -0.000000000000000000, 1.000000000000000000, -0.000000000000000000 ) ) ;
#11871=DIRECTION ( 'NONE',  ( -0.000000000000000000, -1.000000000000000000, -0.000000000000000000 ) ) ;
#11890=EDGE_LOOP ( 'NONE', ( #75611, #59678 ) ) ;
#11894=AXIS2_PLACEMENT_3D ( 'NONE', #55990, #31123, #17408 ) ;
#11904=LINE ( 'NONE', #67708, #40809 ) ;
#11915=CARTESIAN_POINT ( 'NONE',  ( 31.55507366846311967, 4.132774720514426292, -2.076992067079099336 ) ) ;
#11917=ORIENTED_EDGE ( 'NONE', *, *, #99818, .F. ) ;
#11924=CARTESIAN_POINT ( 'NONE',  ( 10.73283225829863952, 3.316774720511335595, -27.03068772560423838 ) ) ;
#11928=VECTOR ( 'NONE', #74382, 1000.000000000000000 ) ;
#11932=CARTESIAN_POINT ( 'NONE',  ( 12.16765770914787304, -5.965225279485572685, -27.57618308014988173 ) ) ;
#11941=CARTESIAN_POINT ( 'NONE',  ( 5.088854283150510582, 3.311779300275201177, -27.56292346345011524 ) ) ;
#11955=AXIS2_PLACEMENT_3D ( 'NONE', #3467, #3960, #51628 ) ;
#11960=CARTESIAN_POINT ( 'NONE',  ( 30.60862754225505000, 4.127879075750807480, 27.06827100787837992 ) ) ;
#11973=CARTESIAN_POINT ( 'NONE',  ( 13.91401389203221406, -5.965225279485572685, 158.0376437107427137 ) ) ;
#11991=DIRECTION ( 'NONE',  ( -0.03244919754393515293, 0.000000000000000000, 0.9994733861282923959 ) ) ;
#11993=CARTESIAN_POINT ( 'NONE',  ( 14.56700794487394290, 4.079493581517789735, -28.22524715676654239 ) ) ;
#11995=AXIS2_PLACEMENT_3D ( 'NONE', #55922, #64552, #1123 ) ;
#12001=ADVANCED_FACE ( 'NONE', ( #94679 ), #46512, .F. ) ;
#12010=FACE_OUTER_BOUND ( 'NONE', #21465, .T. ) ;
#12012=CARTESIAN_POINT ( 'NONE',  ( -28.98875734969026041, 0.3587747205144262708, 15.62202280011862321 ) ) ;
#12021=VERTEX_POINT ( 'NONE', #77441 ) ;
#12026=ORIENTED_EDGE ( 'NONE', *, *, #46684, .F. ) ;
#12049=VECTOR ( 'NONE', #29031, 1000.000000000000000 ) ;
#12051=DIRECTION ( 'NONE',  ( -0.6392559695863496705, -6.845827386180411947E-16, -0.7689940216596069522 ) ) ;
#12056=ORIENTED_EDGE ( 'NONE', *, *, #28018, .T. ) ;
#12063=CYLINDRICAL_SURFACE ( 'NONE', #62014, 11.85241003308276042 ) ;
#12067=CARTESIAN_POINT ( 'NONE',  ( 9.051621769697627329, -6.475225279485570695, -27.04979394446680274 ) ) ;
#12087=ADVANCED_FACE ( 'NONE', ( #58141 ), #54703, .T. ) ;
#12088=FACE_OUTER_BOUND ( 'NONE', #15753, .T. ) ;
#12098=ORIENTED_EDGE ( 'NONE', *, *, #15189, .T. ) ;
#12145=LINE ( 'NONE', #6037, #19003 ) ;
#12149=CARTESIAN_POINT ( 'NONE',  ( 282.9764569301858046, 4.540774720514427543, 20.79159422840526616 ) ) ;
#12170=DIRECTION ( 'NONE',  ( 0.000000000000000000, 0.000000000000000000, 1.000000000000000000 ) ) ;
#12181=CARTESIAN_POINT ( 'NONE',  ( 282.9764569301858046, 4.540774720514427543, 20.79159422840526616 ) ) ;
#12186=CARTESIAN_POINT ( 'NONE',  ( 13.91401389203221406, 3.316774720514426456, 158.0376437107427137 ) ) ;
#12198=LINE ( 'NONE', #28424, #30513 ) ;
#12208=LINE ( 'NONE', #12708, #95474 ) ;
#12211=ORIENTED_EDGE ( 'NONE', *, *, #21123, .T. ) ;
#12215=CARTESIAN_POINT ( 'NONE',  ( 29.74624769612771402, 6.376774720514427841, 26.55905195464798396 ) ) ;
#12242=ADVANCED_FACE ( 'NONE', ( #34792 ), #84445, .F. ) ;
#12260=DIRECTION ( 'NONE',  ( 0.9952638024365005887, 0.000000000000000000, 0.09721092304694053943 ) ) ;
#12272=VERTEX_POINT ( 'NONE', #29164 ) ;
#12288=CARTESIAN_POINT ( 'NONE',  ( 31.74473449900405697, 4.976825198871215328, -4.259190951192157293 ) ) ;
#12299=ORIENTED_EDGE ( 'NONE', *, *, #95504, .T. ) ;
#12310=DIRECTION ( 'NONE',  ( 0.000000000000000000, 0.000000000000000000, -1.000000000000000000 ) ) ;
#12315=VECTOR ( 'NONE', #92675, 1000.000000000000000 ) ;
#12322=CARTESIAN_POINT ( 'NONE',  ( -28.98875734969026041, -5.965225279485572685, 26.43402280011862615 ) ) ;
#12324=VECTOR ( 'NONE', #69759, 1000.000000000000000 ) ;
#12362=FACE_OUTER_BOUND ( 'NONE', #20979, .T. ) ;
#12370=CYLINDRICAL_SURFACE ( 'NONE', #61511, 251.9358649670780892 ) ;
#12371=DIRECTION ( 'NONE',  ( -1.387778780781446464E-15, 0.000000000000000000, -1.000000000000000000 ) ) ;
#12390=CARTESIAN_POINT ( 'NONE',  ( -20.27875734969026311, 3.456774720514426136, 24.00402280011862288 ) ) ;
#12403=EDGE_CURVE ( 'NONE', #82488, #16105, #41279, .T. ) ;
#12414=LINE ( 'NONE', #36266, #50640 ) ;
#12418=VECTOR ( 'NONE', #28188, 1000.000000000000000 ) ;
#12423=ORIENTED_EDGE ( 'NONE', *, *, #94859, .F. ) ;
#12441=EDGE_CURVE ( 'NONE', #80312, #3302, #80335, .T. ) ;
#12446=VECTOR ( 'NONE', #64582, 1000.000000000000000 ) ;
#12454=CARTESIAN_POINT ( 'NONE',  ( 31.71875899258513698, 3.424184405370887863, -3.672337713816452354 ) ) ;
#12460=CARTESIAN_POINT ( 'NONE',  ( 30.58729439590573662, 5.356774720514427379, 26.14186284044631492 ) ) ;
#12465=VECTOR ( 'NONE', #70062, 1000.000000000000114 ) ;
#12466=EDGE_CURVE ( 'NONE', #86336, #19038, #50895, .T. ) ;
#12479=AXIS2_PLACEMENT_3D ( 'NONE', #100177, #70762, #54536 ) ;
#12480=FACE_OUTER_BOUND ( 'NONE', #99720, .T. ) ;
#12482=ORIENTED_EDGE ( 'NONE', *, *, #70155, .F. ) ;
#12484=DIRECTION ( 'NONE',  ( 0.000000000000000000, 1.000000000000000000, -0.000000000000000000 ) ) ;
#12496=ORIENTED_EDGE ( 'NONE', *, *, #87032, .T. ) ;
#12534=CARTESIAN_POINT ( 'NONE',  ( 29.57907552799942863, 6.376774720514426953, 29.21818156447040948 ) ) ;
#12543=PLANE ( 'NONE',  #80973 ) ;
#12551=AXIS2_PLACEMENT_3D ( 'NONE', #94230, #9501, #40462 ) ;
#12558=VECTOR ( 'NONE', #58837, 1000.000000000000000 ) ;
#12572=CARTESIAN_POINT ( 'NONE',  ( 7.462166178408539352, -5.965225279485572685, -27.67315496249664974 ) ) ;
#12574=CARTESIAN_POINT ( 'NONE',  ( 7.858420481369514654, -6.475225279485573360, -27.14867965659404092 ) ) ;
#12576=LINE ( 'NONE', #41544, #75572 ) ;
#12577=VERTEX_POINT ( 'NONE', #99531 ) ;
#12578=CARTESIAN_POINT ( 'NONE',  ( -29.49875734969025842, -5.965225279485572685, 17.86602280011862476 ) ) ;
#12582=VERTEX_POINT ( 'NONE', #6201 ) ;
#12596=DIRECTION ( 'NONE',  ( -0.1593164160933055740, 0.000000000000000000, 0.9872275723272646575 ) ) ;
#12600=VERTEX_POINT ( 'NONE', #61504 ) ;
#12610=ORIENTED_EDGE ( 'NONE', *, *, #33632, .T. ) ;
#12613=DIRECTION ( 'NONE',  ( -1.226388327005079762E-16, 0.000000000000000000, 1.000000000000000000 ) ) ;
#12646=ORIENTED_EDGE ( 'NONE', *, *, #68929, .T. ) ;
#12648=CARTESIAN_POINT ( 'NONE',  ( 17.51792015816173986, -5.965225279485572685, 29.01255224319336889 ) ) ;
#12657=LINE ( 'NONE', #45126, #31956 ) ;
#12661=EDGE_CURVE ( 'NONE', #64249, #35854, #60784, .T. ) ;
#12667=DIRECTION ( 'NONE',  ( 0.000000000000000000, 0.000000000000000000, 1.000000000000000000 ) ) ;
#12677=CARTESIAN_POINT ( 'NONE',  ( 7.207151257207165429, -5.965225279485574461, -28.24477140324590252 ) ) ;
#12692=CARTESIAN_POINT ( 'NONE',  ( 33.28704981706498955, 4.441298812401576868, -11.58844794911118647 ) ) ;
#12704=PLANE ( 'NONE',  #20511 ) ;
#12705=ADVANCED_FACE ( 'NONE', ( #38648 ), #46209, .F. ) ;
#12708=CARTESIAN_POINT ( 'NONE',  ( -19.37210865224160017, -5.965225279485592225, -21.60955166348795586 ) ) ;
#12727=EDGE_LOOP ( 'NONE', ( #94505, #13987, #9221, #88334, #94414, #5990, #59959, #770 ) ) ;
#12729=VECTOR ( 'NONE', #41003, 1000.000000000000000 ) ;
#12741=VECTOR ( 'NONE', #92236, 1000.000000000000000 ) ;
#12744=VERTEX_POINT ( 'NONE', #7192 ) ;
#12754=EDGE_LOOP ( 'NONE', ( #9259, #64430, #100213 ) ) ;
#12810=ORIENTED_EDGE ( 'NONE', *, *, #47760, .T. ) ;
#12820=EDGE_CURVE ( 'NONE', #17742, #73137, #17316, .T. ) ;
#12857=ORIENTED_EDGE ( 'NONE', *, *, #11016, .F. ) ;
#12858=CARTESIAN_POINT ( 'NONE',  ( 31.64143112576189765, -5.965225279485572685, 14.03360796525321774 ) ) ;
#12869=CARTESIAN_POINT ( 'NONE',  ( -29.49875734969025842, -5.965225279485572685, 23.37402280011862743 ) ) ;
#12883=EDGE_CURVE ( 'NONE', #45125, #50697, #10574, .T. ) ;
#12887=CARTESIAN_POINT ( 'NONE',  ( 15.29947330337541445, 3.316774720514426456, -27.16854002387010780 ) ) ;
#12906=( BOUNDED_SURFACE ( )  B_SPLINE_SURFACE ( 3, 2, ( 
 ( #122, #21941, #39680 ),
 ( #76724, #78230, #7733 ),
 ( #32069, #46806, #31063 ),
 ( #6732, #37686, #22933 ) ),
 .UNSPECIFIED., .F., .F., .T. ) 
 B_SPLINE_SURFACE_WITH_KNOTS ( ( 4, 4 ),
 ( 3, 3 ),
 ( 0.0009756167707891351057, 0.001181474220861217185 ),
 ( 0.000000000000000000, 1.000000000000000000 ),
 .UNSPECIFIED. ) 
 GEOMETRIC_REPRESENTATION_ITEM ( )  RATIONAL_B_SPLINE_SURFACE ( (
 ( 1.000000000000000000, 0.8117984224361689538, 1.000000000000000000),
 ( 1.000000000000000000, 0.7811245729408042848, 1.000000000000000000),
 ( 1.000000000000000000, 0.7458076110977203133, 1.000000000000000000),
 ( 1.000000000000000000, 0.7071067811865505703, 1.000000000000000000) ) ) 
 REPRESENTATION_ITEM ( '' )  SURFACE ( )  );
#12911=DIRECTION ( 'NONE',  ( 0.000000000000000000, 1.000000000000000000, 0.000000000000000000 ) ) ;
#12915=CARTESIAN_POINT ( 'NONE',  ( -28.47875734969025885, -5.965225279485572685, -0.08597719988137125791 ) ) ;
#12929=CARTESIAN_POINT ( 'NONE',  ( 30.93860345374796594, -6.475225279485573360, 20.86760796525322093 ) ) ;
#12934=ADVANCED_FACE ( 'NONE', ( #42679 ), #4105, .T. ) ;
#12962=CARTESIAN_POINT ( 'NONE',  ( -6.914873625533462409, -5.965225279485572685, 29.95171384920748281 ) ) ;
#12969=AXIS2_PLACEMENT_3D ( 'NONE', #27882, #34504, #58839 ) ;
#12972=ORIENTED_EDGE ( 'NONE', *, *, #24897, .F. ) ;
#12975=ORIENTED_EDGE ( 'NONE', *, *, #56028, .T. ) ;
#12989=CARTESIAN_POINT ( 'NONE',  ( 282.9764569301858046, 5.356774720514427379, 20.79159422840526616 ) ) ;
#12992=CARTESIAN_POINT ( 'NONE',  ( 0.000000000000000000, 1.682774720514426114, -1.352392034746782823 ) ) ;
#13017=VECTOR ( 'NONE', #57067, 1000.000000000000000 ) ;
#13024=LINE ( 'NONE', #12534, #33831 ) ;
#13032=DIRECTION ( 'NONE',  ( -0.9952638024365005887, -0.000000000000000000, -0.09721092304694052555 ) ) ;
#13034=AXIS2_PLACEMENT_3D ( 'NONE', #38203, #147, #82028 ) ;
#13039=DIRECTION ( 'NONE',  ( 0.7512896232465891000, -1.109416176496794925E-16, 0.6599726524652351767 ) ) ;
#13081=VECTOR ( 'NONE', #75394, 1000.000000000000000 ) ;
#13098=ORIENTED_EDGE ( 'NONE', *, *, #80136, .F. ) ;
#13100=DIRECTION ( 'NONE',  ( 0.03244919754393515293, 0.000000000000000000, -0.9994733861282923959 ) ) ;
#13111=EDGE_CURVE ( 'NONE', #19685, #40707, #97444, .T. ) ;
#13119=EDGE_LOOP ( 'NONE', ( #52584, #46403, #95434, #61434 ) ) ;
#13123=CARTESIAN_POINT ( 'NONE',  ( 2.449489742783179214, 4.293056017849825601, 2.499999999999999112 ) ) ;
#13133=FACE_OUTER_BOUND ( 'NONE', #3193, .T. ) ;
#13142=CARTESIAN_POINT ( 'NONE',  ( 8.205893897551582938, -6.475225279485575136, -27.11136772256261196 ) ) ;
#13149=LINE ( 'NONE', #7048, #8673 ) ;
#13150=CARTESIAN_POINT ( 'NONE',  ( -0.02075734969026423599, 6.376774720514426953, -0.08597719988137648983 ) ) ;
#13152=DIRECTION ( 'NONE',  ( 0.000000000000000000, 0.000000000000000000, 1.000000000000000000 ) ) ;
#13166=DIRECTION ( 'NONE',  ( 0.000000000000000000, 0.000000000000000000, -1.000000000000000000 ) ) ;
#13168=ORIENTED_EDGE ( 'NONE', *, *, #63376, .F. ) ;
#13181=CARTESIAN_POINT ( 'NONE',  ( 11.59154397149680626, 4.779967012825416361, -27.71550087055790712 ) ) ;
#13192=B_SPLINE_CURVE_WITH_KNOTS ( 'NONE', 3,
 ( #41528, #34411, #58255, #65391 ),
 .UNSPECIFIED., .F., .F.,
 ( 4, 4 ),
 ( 2.218788294603013803E-07, 9.487457706522013176E-07 ),
 .UNSPECIFIED. ) ;
#13196=CYLINDRICAL_SURFACE ( 'NONE', #19477, 2.249999999999998668 ) ;
#13222=CIRCLE ( 'NONE', #91026, 84.76210982660168725 ) ;
#13233=LINE ( 'NONE', #20844, #35702 ) ;
#13234=CARTESIAN_POINT ( 'NONE',  ( 31.79364159983995464, 6.376774720514426953, -11.59305536555894278 ) ) ;
#13237=VERTEX_POINT ( 'NONE', #79598 ) ;
#13247=B_SPLINE_CURVE_WITH_KNOTS ( 'NONE', 3,
 ( #16475, #68787, #39823, #61685 ),
 .UNSPECIFIED., .F., .F.,
 ( 4, 4 ),
 ( 0.008354480413380572026, 0.009203042238611652825 ),
 .UNSPECIFIED. ) ;
#13249=ORIENTED_EDGE ( 'NONE', *, *, #61767, .F. ) ;
#13266=ORIENTED_EDGE ( 'NONE', *, *, #90693, .T. ) ;
#13277=VECTOR ( 'NONE', #44996, 1000.000000000000000 ) ;
#13385=CARTESIAN_POINT ( 'NONE',  ( 15.00349586803797486, 3.316774720514427344, -27.42854230132123305 ) ) ;
#13400=EDGE_CURVE ( 'NONE', #24140, #79832, #55784, .T. ) ;
#13415=EDGE_LOOP ( 'NONE', ( #21097, #26239, #98868, #91472 ) ) ;
#13420=CARTESIAN_POINT ( 'NONE',  ( 26.73860345374794178, -1.477225279485574028, 19.84760796525321780 ) ) ;
#13423=CIRCLE ( 'NONE', #39363, 4.300000000000000711 ) ;
#13438=CYLINDRICAL_SURFACE ( 'NONE', #42691, 0.8160000000000007248 ) ;
#13445=LINE ( 'NONE', #66775, #12418 ) ;
#13450=CARTESIAN_POINT ( 'NONE',  ( 30.61220459279984496, 3.931892516571728446, 27.21038724104498385 ) ) ;
#13453=CARTESIAN_POINT ( 'NONE',  ( 32.66876533700883556, -5.965225279485572685, -12.58926540598386445 ) ) ;
#13454=VERTEX_POINT ( 'NONE', #82960 ) ;
#13455=ORIENTED_EDGE ( 'NONE', *, *, #19438, .T. ) ;
#13456=CIRCLE ( 'NONE', #88010, 130.7884398600581335 ) ;
#13481=DIRECTION ( 'NONE',  ( 0.000000000000000000, 0.000000000000000000, -1.000000000000000000 ) ) ;
#13483=CARTESIAN_POINT ( 'NONE',  ( 31.59111626279633711, 0.3587747205144265483, 16.27760796525321751 ) ) ;
#13484=EDGE_CURVE ( 'NONE', #13594, #88430, #91572, .T. ) ;
#13489=FACE_OUTER_BOUND ( 'NONE', #24499, .T. ) ;
#13495=ORIENTED_EDGE ( 'NONE', *, *, #88785, .F. ) ;
#13502=PLANE ( 'NONE',  #64100 ) ;
#13521=VERTEX_POINT ( 'NONE', #75346 ) ;
#13528=DIRECTION ( 'NONE',  ( -1.000000000000000000, 0.000000000000000000, 0.000000000000000000 ) ) ;
#13545=AXIS2_PLACEMENT_3D ( 'NONE', #49264, #41643, #35526 ) ;
#13548=ORIENTED_EDGE ( 'NONE', *, *, #14761, .F. ) ;
#13555=EDGE_CURVE ( 'NONE', #33103, #18367, #7330, .T. ) ;
#13570=LINE ( 'NONE', #75464, #59797 ) ;
#13578=CARTESIAN_POINT ( 'NONE',  ( 29.77147767949874435, 6.376774720514426953, 26.15915692125051706 ) ) ;
#13594=VERTEX_POINT ( 'NONE', #9332 ) ;
#13604=EDGE_CURVE ( 'NONE', #63916, #79629, #56535, .T. ) ;
#13629=EDGE_LOOP ( 'NONE', ( #11765, #2061 ) ) ;
#13635=CARTESIAN_POINT ( 'NONE',  ( 5.399550031316281640, 0.3587747205144061202, -28.54570968857217395 ) ) ;
#13641=CARTESIAN_POINT ( 'NONE',  ( 14.61581676225068449, 3.316774720514424679, -27.35847991880143226 ) ) ;
#13645=VECTOR ( 'NONE', #69401, 1000.000000000000000 ) ;
#13646=CARTESIAN_POINT ( 'NONE',  ( -29.49875734969025842, -5.965225279485572685, 25.61802280011862720 ) ) ;
#13677=ORIENTED_EDGE ( 'NONE', *, *, #22221, .F. ) ;
#13695=ORIENTED_EDGE ( 'NONE', *, *, #460, .T. ) ;
#13701=CARTESIAN_POINT ( 'NONE',  ( 0.000000000000000000, -1.473225279485573802, 4.300000000000000711 ) ) ;
#13716=EDGE_CURVE ( 'NONE', #71522, #8729, #88975, .T. ) ;
#13729=ORIENTED_EDGE ( 'NONE', *, *, #95259, .T. ) ;
#13779=DIRECTION ( 'NONE',  ( -0.6599726524652352877, 0.000000000000000000, 0.7512896232465892110 ) ) ;
#13791=CARTESIAN_POINT ( 'NONE',  ( 5.471383689419965890, 0.3587747205144057872, -29.02273493113404612 ) ) ;
#13816=LINE ( 'NONE', #90953, #72397 ) ;
#13822=ORIENTED_EDGE ( 'NONE', *, *, #46423, .T. ) ;
#13838=VECTOR ( 'NONE', #50509, 1000.000000000000114 ) ;
#13866=DIRECTION ( 'NONE',  ( -0.000000000000000000, -1.000000000000000000, -0.000000000000000000 ) ) ;
#13889=ORIENTED_EDGE ( 'NONE', *, *, #52, .T. ) ;
#13890=ORIENTED_EDGE ( 'NONE', *, *, #73487, .F. ) ;
#13896=CARTESIAN_POINT ( 'NONE',  ( 33.41145047975764726, 4.538943570064879474, -12.61568413423376889 ) ) ;
#13914=ORIENTED_EDGE ( 'NONE', *, *, #63816, .T. ) ;
#13944=CARTESIAN_POINT ( 'NONE',  ( 31.10634905326439181, 4.583458114012134210, -2.800232393899708683 ) ) ;
#13949=CARTESIAN_POINT ( 'NONE',  ( 30.60993360729056079, 4.065030569019225659, 27.12046991540520580 ) ) ;
#13956=ORIENTED_EDGE ( 'NONE', *, *, #80369, .F. ) ;
#13967=EDGE_CURVE ( 'NONE', #37863, #66710, #26806, .T. ) ;
#13973=LINE ( 'NONE', #68276, #86739 ) ;
#13977=EDGE_LOOP ( 'NONE', ( #53681, #15386, #34749, #92571 ) ) ;
#13987=ORIENTED_EDGE ( 'NONE', *, *, #23244, .T. ) ;
#13992=CARTESIAN_POINT ( 'NONE',  ( -25.92875734969026524, 3.316774720514426456, -0.08597719988137648983 ) ) ;
#13994=CIRCLE ( 'NONE', #44793, 84.48086791635431325 ) ;
#14000=CARTESIAN_POINT ( 'NONE',  ( -29.49875734969025842, -5.965225279485572685, 17.86602280011862476 ) ) ;
#14021=ORIENTED_EDGE ( 'NONE', *, *, #60319, .F. ) ;
#14022=CARTESIAN_POINT ( 'NONE',  ( 32.16024265030974050, -5.965225279485572685, 16.27760796525321751 ) ) ;
#14031=CIRCLE ( 'NONE', #91831, 3.060000000000001830 ) ;
#14060=DIRECTION ( 'NONE',  ( 0.000000000000000000, -1.000000000000000000, 0.000000000000000000 ) ) ;
#14061=CIRCLE ( 'NONE', #51379, 91.74549126261076992 ) ;
#14063=ORIENTED_EDGE ( 'NONE', *, *, #82531, .F. ) ;
#14071=CARTESIAN_POINT ( 'NONE',  ( 32.56681547219513817, 5.361656835957732348, -1.802091617189351735 ) ) ;
#14089=ORIENTED_EDGE ( 'NONE', *, *, #65563, .T. ) ;
#14100=ORIENTED_EDGE ( 'NONE', *, *, #36750, .T. ) ;
#14103=CARTESIAN_POINT ( 'NONE',  ( -23.59123376470063960, 5.356774720514425603, 23.50402280011862288 ) ) ;
#14130=ORIENTED_EDGE ( 'NONE', *, *, #36172, .F. ) ;
#14133=AXIS2_PLACEMENT_3D ( 'NONE', #18118, #49084, #41974 ) ;
#14135=DIRECTION ( 'NONE',  ( -0.7512896232465891000, 0.000000000000000000, -0.6599726524652351767 ) ) ;
#14141=VECTOR ( 'NONE', #61343, 1000.000000000000000 ) ;
#14142=CARTESIAN_POINT ( 'NONE',  ( 13.80377080874918150, -6.475225279485574248, -27.21172484903264532 ) ) ;
#14188=DIRECTION ( 'NONE',  ( 0.000000000000000000, 1.000000000000000000, -1.084202172485504434E-16 ) ) ;
#14193=CYLINDRICAL_SURFACE ( 'NONE', #34960, 3.570000000000003837 ) ;
#14200=VECTOR ( 'NONE', #37209, 1000.000000000000000 ) ;
#14203=DIRECTION ( 'NONE',  ( -0.06283980576413539243, 0.000000000000000000, -0.9980236263794188822 ) ) ;
#14204=ORIENTED_EDGE ( 'NONE', *, *, #50857, .T. ) ;
#14216=ORIENTED_EDGE ( 'NONE', *, *, #88571, .T. ) ;
#14228=VERTEX_POINT ( 'NONE', #24938 ) ;
#14235=VECTOR ( 'NONE', #25254, 1000.000000000000000 ) ;
#14237=EDGE_CURVE ( 'NONE', #78402, #78496, #75412, .T. ) ;
#14240=ORIENTED_EDGE ( 'NONE', *, *, #89824, .T. ) ;
#14246=ORIENTED_EDGE ( 'NONE', *, *, #16136, .T. ) ;
#14248=VERTEX_POINT ( 'NONE', #64043 ) ;
#14261=AXIS2_PLACEMENT_3D ( 'NONE', #83048, #97787, #90181 ) ;
#14275=DIRECTION ( 'NONE',  ( -0.000000000000000000, -1.000000000000000000, -0.000000000000000000 ) ) ;
#14280=CIRCLE ( 'NONE', #79114, 3.500000000000000000 ) ;
#14281=DIRECTION ( 'NONE',  ( 0.7512896232465891000, 0.000000000000000000, 0.6599726524652351767 ) ) ;
#14288=ADVANCED_FACE ( 'NONE', ( #10223 ), #89964, .T. ) ;
#14296=VERTEX_POINT ( 'NONE', #22310 ) ;
#14299=DIRECTION ( 'NONE',  ( -0.000000000000000000, 0.000000000000000000, 1.000000000000000000 ) ) ;
#14328=PLANE ( 'NONE',  #6533 ) ;
#14334=CARTESIAN_POINT ( 'NONE',  ( 32.16024265030974050, -5.965225279485572685, 16.27760796525321751 ) ) ;
#14343=ORIENTED_EDGE ( 'NONE', *, *, #78208, .T. ) ;
#14352=PLANE ( 'NONE',  #66113 ) ;
#14360=DIRECTION ( 'NONE',  ( 0.000000000000000000, 0.000000000000000000, -1.000000000000000000 ) ) ;
#14396=CARTESIAN_POINT ( 'NONE',  ( 33.00535138976593430, 3.570691370340898452, -12.97242311383974744 ) ) ;
#14403=B_SPLINE_CURVE_WITH_KNOTS ( 'NONE', 3,
 ( #25913, #57391, #12677, #65506, #96926, #95925, #66507, #96427 ),
 .UNSPECIFIED., .F., .F.,
 ( 4, 2, 2, 4 ),
 ( 0.0001293435094372204610, 0.002876179024813956854, 0.004249596782502322069, 0.005623014540190688151 ),
 .UNSPECIFIED. ) ;
#14409=CARTESIAN_POINT ( 'NONE',  ( -0.02075734969026423599, 5.866774720514426278, 22.60902280011862686 ) ) ;
#14410=ADVANCED_FACE ( 'NONE', ( #59909 ), #14707, .F. ) ;
#14457=CARTESIAN_POINT ( 'NONE',  ( 32.60294298177596062, 6.376774720514426953, -11.48871326860665043 ) ) ;
#14460=ORIENTED_EDGE ( 'NONE', *, *, #77131, .F. ) ;
#14470=EDGE_CURVE ( 'NONE', #22648, #54228, #74610, .T. ) ;
#14476=VERTEX_POINT ( 'NONE', #99439 ) ;
#14484=CIRCLE ( 'NONE', #43681, 252.4458649670781085 ) ;
#14485=DIRECTION ( 'NONE',  ( 0.000000000000000000, 0.000000000000000000, -1.000000000000000000 ) ) ;
#14493=AXIS2_PLACEMENT_3D ( 'NONE', #74010, #20203, #51170 ) ;
#14497=ORIENTED_EDGE ( 'NONE', *, *, #10028, .T. ) ;
#14521=CARTESIAN_POINT ( 'NONE',  ( 3.421177667410919110, 0.3587747205144265483, 28.69411518427638441 ) ) ;
#14530=EDGE_CURVE ( 'NONE', #26199, #22449, #26045, .T. ) ;
#14540=EDGE_CURVE ( 'NONE', #55726, #11050, #61905, .T. ) ;
#14545=LINE ( 'NONE', #21647, #60409 ) ;
#14558=CIRCLE ( 'NONE', #50212, 28.96799999999999642 ) ;
#14561=VECTOR ( 'NONE', #11859, 1000.000000000000000 ) ;
#14567=CARTESIAN_POINT ( 'NONE',  ( 30.60113388085891017, 4.386958714992013952, 26.76092701747204927 ) ) ;
#14589=DIRECTION ( 'NONE',  ( -1.000000000000000000, -0.000000000000000000, -0.000000000000000000 ) ) ;
#14594=EDGE_CURVE ( 'NONE', #35733, #63436, #92830, .T. ) ;
#14598=ORIENTED_EDGE ( 'NONE', *, *, #47851, .F. ) ;
#14613=CARTESIAN_POINT ( 'NONE',  ( 15.52291915823239599, 3.595107466738254764, -28.22347026866548347 ) ) ;
#14621=ORIENTED_EDGE ( 'NONE', *, *, #44564, .T. ) ;
#14665=CARTESIAN_POINT ( 'NONE',  ( 22.02124265030973760, -6.143225279485574397, 16.20402280011862217 ) ) ;
#14680=PLANE ( 'NONE',  #85397 ) ;
#14683=ORIENTED_EDGE ( 'NONE', *, *, #97272, .F. ) ;
#14691=CARTESIAN_POINT ( 'NONE',  ( 30.93860345374796239, -5.965225279485572685, 26.43402280011862615 ) ) ;
#14697=VERTEX_POINT ( 'NONE', #80113 ) ;
#14698=CARTESIAN_POINT ( 'NONE',  ( 22.02124265030973760, -6.143225279485574397, 16.20402280011862217 ) ) ;
#14707=CYLINDRICAL_SURFACE ( 'NONE', #67330, 91.74549126261076992 ) ;
#14730=ORIENTED_EDGE ( 'NONE', *, *, #88150, .F. ) ;
#14732=ORIENTED_EDGE ( 'NONE', *, *, #76913, .T. ) ;
#14746=ORIENTED_EDGE ( 'NONE', *, *, #42120, .F. ) ;
#14748=VECTOR ( 'NONE', #72218, 1000.000000000000000 ) ;
#14761=EDGE_CURVE ( 'NONE', #74060, #61556, #35447, .T. ) ;
#14770=EDGE_CURVE ( 'NONE', #12582, #63531, #86722, .T. ) ;
#14775=B_SPLINE_CURVE_WITH_KNOTS ( 'NONE', 3,
 ( #54435, #45821, #85369, #53942 ),
 .UNSPECIFIED., .F., .F.,
 ( 4, 4 ),
 ( 0.007591229774494646920, 0.009012827652035957510 ),
 .UNSPECIFIED. ) ;
#14789=CARTESIAN_POINT ( 'NONE',  ( 10.68713020350585197, 3.316774720514176877, -28.05292731652309257 ) ) ;
#14803=CARTESIAN_POINT ( 'NONE',  ( 27.53860345374808105, 5.356774720496559894, 19.84760796525321780 ) ) ;
#14806=ADVANCED_FACE ( 'NONE', ( #59276 ), #35937, .F. ) ;
#14813=AXIS2_PLACEMENT_3D ( 'NONE', #67247, #91557, #98166 ) ;
#14825=EDGE_LOOP ( 'NONE', ( #15732, #18634, #54679, #60296 ) ) ;
#14826=CARTESIAN_POINT ( 'NONE',  ( 32.16024265030974050, -5.965225279485572685, 14.03360796525321774 ) ) ;
#14838=LINE ( 'NONE', #75737, #10193 ) ;
#14845=VERTEX_POINT ( 'NONE', #31316 ) ;
#14856=EDGE_CURVE ( 'NONE', #45943, #68317, #76978, .T. ) ;
#14862=FACE_OUTER_BOUND ( 'NONE', #19971, .T. ) ;
#14866=ORIENTED_EDGE ( 'NONE', *, *, #98392, .T. ) ;
#14895=CARTESIAN_POINT ( 'NONE',  ( 32.85081302853786411, 5.152774720514582185, -13.10817780685225031 ) ) ;
#14933=EDGE_CURVE ( 'NONE', #6012, #76643, #58764, .T. ) ;
#14974=VERTEX_POINT ( 'NONE', #32824 ) ;
#14988=DIRECTION ( 'NONE',  ( 0.9822594791677485837, 0.000000000000000000, -0.1875268396392986980 ) ) ;
#14990=ORIENTED_EDGE ( 'NONE', *, *, #77131, .T. ) ;
#14999=CARTESIAN_POINT ( 'NONE',  ( -4.926336369345162502, 0.3587747205143967943, -28.61095484066305161 ) ) ;
#15003=LINE ( 'NONE', #66732, #97194 ) ;
#15006=LINE ( 'NONE', #55086, #85778 ) ;
#15033=VECTOR ( 'NONE', #84439, 1000.000000000000000 ) ;
#15055=CARTESIAN_POINT ( 'NONE',  ( 30.93860345374796594, 0.6647747205144264315, 19.84760796525321780 ) ) ;
#15075=DIRECTION ( 'NONE',  ( 0.000000000000000000, -0.000000000000000000, -1.000000000000000000 ) ) ;
#15079=CARTESIAN_POINT ( 'NONE',  ( 32.15269211224249091, 4.540774720514427543, 3.401810532325273861 ) ) ;
#15101=ORIENTED_EDGE ( 'NONE', *, *, #54767, .T. ) ;
#15118=VECTOR ( 'NONE', #20425, 1000.000000000000000 ) ;
#15131=LINE ( 'NONE', #30354, #25239 ) ;
#15134=CARTESIAN_POINT ( 'NONE',  ( -26.91814428177455909, 0.3587747205144265483, 29.98490496616818746 ) ) ;
#15139=ORIENTED_EDGE ( 'NONE', *, *, #22351, .T. ) ;
#15145=DIRECTION ( 'NONE',  ( 0.000000000000000000, 0.000000000000000000, -1.000000000000000000 ) ) ;
#15155=CARTESIAN_POINT ( 'NONE',  ( 11.96746718618548577, 4.832654890647344104, -27.30666805081000348 ) ) ;
#15156=DIRECTION ( 'NONE',  ( -0.000000000000000000, 1.000000000000000000, -0.000000000000000000 ) ) ;
#15170=CARTESIAN_POINT ( 'NONE',  ( 32.45853543194704116, -5.965225279485572685, 9.169203677920338080 ) ) ;
#15189=EDGE_CURVE ( 'NONE', #71759, #4176, #33784, .T. ) ;
#15207=LINE ( 'NONE', #15708, #48638 ) ;
#15208=DIRECTION ( 'NONE',  ( -0.000000000000000000, -0.000000000000000000, 1.000000000000000000 ) ) ;
#15214=DIRECTION ( 'NONE',  ( 0.000000000000000000, 0.000000000000000000, 1.000000000000000000 ) ) ;
#15218=VERTEX_POINT ( 'NONE', #81466 ) ;
#15243=EDGE_CURVE ( 'NONE', #5514, #30477, #41889, .T. ) ;
#15249=DIRECTION ( 'NONE',  ( 0.1254312216594016538, 0.000000000000000000, 0.9921023176230513441 ) ) ;
#15254=VERTEX_POINT ( 'NONE', #65758 ) ;
#15284=ORIENTED_EDGE ( 'NONE', *, *, #49327, .F. ) ;
#15292=CARTESIAN_POINT ( 'NONE',  ( 8.655157120174900243, 3.316774720514428232, -28.10018424651253000 ) ) ;
#15304=DIRECTION ( 'NONE',  ( -0.000000000000000000, -1.000000000000000000, 0.000000000000000000 ) ) ;
#15307=AXIS2_PLACEMENT_3D ( 'NONE', #42086, #19713, #3517 ) ;
#15311=DIRECTION ( 'NONE',  ( 0.7512896232465891000, -0.000000000000000000, 0.6599726524652352877 ) ) ;
#15312=LINE ( 'NONE', #32049, #39379 ) ;
#15341=CARTESIAN_POINT ( 'NONE',  ( 31.55236408230781819, 0.6647747205144264315, 19.84760796525321780 ) ) ;
#15363=AXIS2_PLACEMENT_3D ( 'NONE', #56415, #17834, #50291 ) ;
#15367=CARTESIAN_POINT ( 'NONE',  ( -25.92875734969026524, 5.356774720514425603, 0.7300228001186309656 ) ) ;
#15386=ORIENTED_EDGE ( 'NONE', *, *, #415, .T. ) ;
#15394=CARTESIAN_POINT ( 'NONE',  ( 32.01683625711453374, 5.152774720514459617, -11.91548796314834036 ) ) ;
#15430=CARTESIAN_POINT ( 'NONE',  ( -24.90875734969025501, -5.965225279485572685, 30.51402280011862089 ) ) ;
#15435=LINE ( 'NONE', #45907, #43490 ) ;
#15439=AXIS2_PLACEMENT_3D ( 'NONE', #95960, #81733, #19816 ) ;
#15442=ORIENTED_EDGE ( 'NONE', *, *, #84505, .T. ) ;
#15463=DIRECTION ( 'NONE',  ( 0.000000000000000000, 0.000000000000000000, -1.000000000000000000 ) ) ;
#15472=ORIENTED_EDGE ( 'NONE', *, *, #32860, .T. ) ;
#15479=DIRECTION ( 'NONE',  ( 0.000000000000000000, -1.000000000000000000, 0.000000000000000000 ) ) ;
#15488=EDGE_LOOP ( 'NONE', ( #67311, #29761, #60592, #62037 ) ) ;
#15515=CARTESIAN_POINT ( 'NONE',  ( 22.81105451610979173, -6.475225279485573360, -16.21691820600746681 ) ) ;
#15517=AXIS2_PLACEMENT_3D ( 'NONE', #23231, #16629, #54217 ) ;
#15524=CARTESIAN_POINT ( 'NONE',  ( 26.73860345374794178, -1.477225279485574028, 19.84760796525321780 ) ) ;
#15527=CARTESIAN_POINT ( 'NONE',  ( 32.19706240494739546, 5.152774720514445406, -11.87117847608345933 ) ) ;
#15531=DIRECTION ( 'NONE',  ( -0.9978940991575085961, 0.000000000000000000, -0.06486421869277853025 ) ) ;
#15534=LINE ( 'NONE', #32267, #90193 ) ;
#15546=LINE ( 'NONE', #23654, #40395 ) ;
#15547=CARTESIAN_POINT ( 'NONE',  ( 27.86270917940689174, 0.3587747205144265483, 29.49402280011862487 ) ) ;
#15550=CARTESIAN_POINT ( 'NONE',  ( 27.53860345374771867, 500000.0000000000582, -9.482392034746240483 ) ) ;
#15591=ORIENTED_EDGE ( 'NONE', *, *, #91115, .F. ) ;
#15596=ORIENTED_EDGE ( 'NONE', *, *, #77312, .F. ) ;
#15610=EDGE_LOOP ( 'NONE', ( #79215, #80322, #81101, #85485 ) ) ;
#15615=VERTEX_POINT ( 'NONE', #60510 ) ;
#15625=CARTESIAN_POINT ( 'NONE',  ( 33.00535138976610483, -5.965225279485572685, -12.97242311383961422 ) ) ;
#15635=ADVANCED_FACE ( 'NONE', ( #75207 ), #44774, .F. ) ;
#15638=ORIENTED_EDGE ( 'NONE', *, *, #73953, .T. ) ;
#15639=EDGE_CURVE ( 'NONE', #95598, #43602, #5699, .T. ) ;
#15671=CARTESIAN_POINT ( 'NONE',  ( 17.51792015816173986, 0.3587747205144265483, 29.01255224319336889 ) ) ;
#15680=CARTESIAN_POINT ( 'NONE',  ( 14.02745725694894574, 2.682774720514426559, -27.25215004931931517 ) ) ;
#15704=VECTOR ( 'NONE', #39825, 1000.000000000000000 ) ;
#15708=CARTESIAN_POINT ( 'NONE',  ( 31.31283134548411340, -1.477225279485574028, -10.20862453625735711 ) ) ;
#15724=CARTESIAN_POINT ( 'NONE',  ( 22.81105451610979173, 1.682774720514426114, -18.46691820600746681 ) ) ;
#15732=ORIENTED_EDGE ( 'NONE', *, *, #88594, .F. ) ;
#15740=ORIENTED_EDGE ( 'NONE', *, *, #8761, .F. ) ;
#15747=LINE ( 'NONE', #99472, #80719 ) ;
#15749=EDGE_CURVE ( 'NONE', #60562, #10305, #49375, .T. ) ;
#15753=EDGE_LOOP ( 'NONE', ( #73047, #7359, #74876, #7755 ) ) ;
#15768=LINE ( 'NONE', #39105, #12465 ) ;
#15770=VECTOR ( 'NONE', #28975, 1000.000000000000000 ) ;
#15773=CIRCLE ( 'NONE', #80608, 91.74549126261076992 ) ;
#15784=DIRECTION ( 'NONE',  ( 0.000000000000000000, 0.000000000000000000, 1.000000000000000000 ) ) ;
#15787=CARTESIAN_POINT ( 'NONE',  ( -20.27875734969026311, -6.143225279485574397, 21.75402280011862644 ) ) ;
#15796=CARTESIAN_POINT ( 'NONE',  ( 9.313311959394031447, 3.316774720514592545, -28.06297399525112013 ) ) ;
#15798=AXIS2_PLACEMENT_3D ( 'NONE', #66811, #90125, #14485 ) ;
#15817=LINE ( 'NONE', #53402, #26692 ) ;
#15820=CARTESIAN_POINT ( 'NONE',  ( -10.16634758543296613, -5.965225279485572685, 30.00402280011862288 ) ) ;
#15825=FACE_OUTER_BOUND ( 'NONE', #80273, .T. ) ;
#15837=DIRECTION ( 'NONE',  ( 8.334928612639484546E-17, 1.000000000000000000, 7.321843366904296032E-17 ) ) ;
#15851=ORIENTED_EDGE ( 'NONE', *, *, #17001, .T. ) ;
#15857=EDGE_CURVE ( 'NONE', #5378, #20580, #10208, .T. ) ;
#15868=CARTESIAN_POINT ( 'NONE',  ( 29.73860345376319358, 1.682774720514426114, -1.352392034746782823 ) ) ;
#15882=ORIENTED_EDGE ( 'NONE', *, *, #22851, .T. ) ;
#15912=ORIENTED_EDGE ( 'NONE', *, *, #8562, .T. ) ;
#15975=CARTESIAN_POINT ( 'NONE',  ( -0.02075734969026423599, -5.965225279485572685, -0.08597719988137648983 ) ) ;
#15985=ADVANCED_FACE ( 'NONE', ( #80218 ), #95941, .T. ) ;
#15999=DIRECTION ( 'NONE',  ( 0.000000000000000000, 0.000000000000000000, -1.000000000000000000 ) ) ;
#16006=FACE_OUTER_BOUND ( 'NONE', #72944, .T. ) ;
#16017=EDGE_LOOP ( 'NONE', ( #70684, #93445, #1803, #85453 ) ) ;
#16020=EDGE_CURVE ( 'NONE', #91432, #57584, #19803, .T. ) ;
#16021=ORIENTED_EDGE ( 'NONE', *, *, #96724, .F. ) ;
#16037=CIRCLE ( 'NONE', #93839, 251.4258649670780699 ) ;
#16061=EDGE_CURVE ( 'NONE', #70795, #73934, #84087, .T. ) ;
#16068=PLANE ( 'NONE',  #96939 ) ;
#16071=DIRECTION ( 'NONE',  ( -0.000000000000000000, -1.000000000000000000, -0.000000000000000000 ) ) ;
#16074=ADVANCED_FACE ( 'NONE', ( #98421 ), #42676, .T. ) ;
#16093=CARTESIAN_POINT ( 'NONE',  ( 29.57907552799942508, 3.316774720514426456, 29.21818156447043791 ) ) ;
#16101=EDGE_CURVE ( 'NONE', #34861, #42876, #24582, .T. ) ;
#16105=VERTEX_POINT ( 'NONE', #75090 ) ;
#16122=CARTESIAN_POINT ( 'NONE',  ( -20.77875734969026311, 5.356774720514425603, 27.31649921512899937 ) ) ;
#16123=ORIENTED_EDGE ( 'NONE', *, *, #22085, .T. ) ;
#16126=FACE_OUTER_BOUND ( 'NONE', #259, .T. ) ;
#16129=EDGE_CURVE ( 'NONE', #16459, #16877, #36532, .T. ) ;
#16130=CYLINDRICAL_SURFACE ( 'NONE', #57710, 10.20000000000000107 ) ;
#16136=EDGE_CURVE ( 'NONE', #47065, #94497, #7183, .T. ) ;
#16148=CARTESIAN_POINT ( 'NONE',  ( 31.59111626279633711, -5.965225279485572685, 16.27760796525321751 ) ) ;
#16152=CARTESIAN_POINT ( 'NONE',  ( 8.462785143989153269, 3.316774720514427344, -28.02084008811334215 ) ) ;
#16157=DIRECTION ( 'NONE',  ( 0.000000000000000000, 0.000000000000000000, -1.000000000000000000 ) ) ;
#16163=DIRECTION ( 'NONE',  ( -0.000000000000000000, 1.000000000000000000, -0.000000000000000000 ) ) ;
#16164=DIRECTION ( 'NONE',  ( 0.000000000000000000, 0.000000000000000000, -1.000000000000000000 ) ) ;
#16176=ORIENTED_EDGE ( 'NONE', *, *, #89971, .T. ) ;
#16199=DIRECTION ( 'NONE',  ( 0.000000000000000000, -1.000000000000000000, 0.000000000000000000 ) ) ;
#16212=DIRECTION ( 'NONE',  ( 0.000000000000000000, -1.478457507934778393E-16, -1.000000000000000000 ) ) ;
#16229=ORIENTED_EDGE ( 'NONE', *, *, #65147, .T. ) ;
#16256=CARTESIAN_POINT ( 'NONE',  ( 31.88667425545054002, 1.682774720514426114, -9.651215965565025812 ) ) ;
#16257=ORIENTED_EDGE ( 'NONE', *, *, #88724, .F. ) ;
#16271=ORIENTED_EDGE ( 'NONE', *, *, #87761, .T. ) ;
#16281=AXIS2_PLACEMENT_3D ( 'NONE', #96619, #17504, #78886 ) ;
#16285=LINE ( 'NONE', #60485, #99255 ) ;
#16301=CARTESIAN_POINT ( 'NONE',  ( 9.313311959400177642, 6.376774720514760020, -28.06297399545715976 ) ) ;
#16307=LINE ( 'NONE', #24919, #29619 ) ;
#16315=EDGE_CURVE ( 'NONE', #75250, #50604, #64407, .T. ) ;
#16318=ORIENTED_EDGE ( 'NONE', *, *, #48812, .T. ) ;
#16342=ORIENTED_EDGE ( 'NONE', *, *, #50857, .F. ) ;
#16347=ORIENTED_EDGE ( 'NONE', *, *, #14594, .F. ) ;
#16416=CARTESIAN_POINT ( 'NONE',  ( -20.27875734969026311, -4.543225279485573864, 26.25402280011862288 ) ) ;
#16419=ADVANCED_FACE ( 'NONE', ( #95818 ), #86114, .T. ) ;
#16430=EDGE_CURVE ( 'NONE', #6678, #54547, #58275, .T. ) ;
#16435=DIRECTION ( 'NONE',  ( -0.000000000000000000, 1.000000000000000000, -0.000000000000000000 ) ) ;
#16436=EDGE_CURVE ( 'NONE', #23706, #91326, #80595, .T. ) ;
#16441=DIRECTION ( 'NONE',  ( -0.1489078231574191280, 0.000000000000000000, 0.9888510809027406534 ) ) ;
#16459=VERTEX_POINT ( 'NONE', #49664 ) ;
#16475=CARTESIAN_POINT ( 'NONE',  ( 13.59451591917074431, 3.316774720514426456, -28.23515841827053308 ) ) ;
#16511=CARTESIAN_POINT ( 'NONE',  ( 30.64697572893789967, 5.232796261063635157, 0.6042509527386027424 ) ) ;
#16523=LINE ( 'NONE', #7418, #87054 ) ;
#16524=CARTESIAN_POINT ( 'NONE',  ( 14.23870388848190771, 5.152774720514427642, -26.44223458220801248 ) ) ;
#16526=DIRECTION ( 'NONE',  ( 0.000000000000000000, -1.000000000000000000, 0.000000000000000000 ) ) ;
#16529=DIRECTION ( 'NONE',  ( -0.9685340172660600322, 0.000000000000000000, 0.2488812114211667315 ) ) ;
#16543=ADVANCED_FACE ( 'NONE', ( #59263 ), #4971, .F. ) ;
#16558=AXIS2_PLACEMENT_3D ( 'NONE', #20801, #91322, #89831 ) ;
#16567=CARTESIAN_POINT ( 'NONE',  ( 5.399550031316281640, 0.3587747205144061202, -28.54570968857217395 ) ) ;
#16570=CARTESIAN_POINT ( 'NONE',  ( -12.64432969575900323, -5.965225279485592225, -26.13179214487284696 ) ) ;
#16572=VECTOR ( 'NONE', #34651, 1000.000000000000000 ) ;
#16595=ORIENTED_EDGE ( 'NONE', *, *, #41703, .F. ) ;
#16611=ORIENTED_EDGE ( 'NONE', *, *, #95259, .F. ) ;
#16619=CARTESIAN_POINT ( 'NONE',  ( 14.76093561896379214, -5.965225279485572685, -26.55548769130089681 ) ) ;
#16620=ORIENTED_EDGE ( 'NONE', *, *, #14770, .T. ) ;
#16625=DIRECTION ( 'NONE',  ( -0.000000000000000000, -1.000000000000000000, -0.000000000000000000 ) ) ;
#16629=DIRECTION ( 'NONE',  ( 0.000000000000000000, 1.000000000000000000, -0.000000000000000000 ) ) ;
#16650=ORIENTED_EDGE ( 'NONE', *, *, #42949, .T. ) ;
#16654=ADVANCED_FACE ( 'NONE', ( #91690 ), #52645, .T. ) ;
#16655=CARTESIAN_POINT ( 'NONE',  ( 6.184520403203631389, 5.356774720514425603, -25.32021290018218451 ) ) ;
#16664=LINE ( 'NONE', #23774, #64950 ) ;
#16675=EDGE_CURVE ( 'NONE', #23980, #82488, #7455, .T. ) ;
#16705=ORIENTED_EDGE ( 'NONE', *, *, #96172, .T. ) ;
#16723=EDGE_CURVE ( 'NONE', #3684, #82958, #49046, .T. ) ;
#16730=AXIS2_PLACEMENT_3D ( 'NONE', #40284, #33672, #49414 ) ;
#16737=ORIENTED_EDGE ( 'NONE', *, *, #52560, .T. ) ;
#16779=DIRECTION ( 'NONE',  ( 0.000000000000000000, 0.000000000000000000, -1.000000000000000000 ) ) ;
#16802=ORIENTED_EDGE ( 'NONE', *, *, #75734, .T. ) ;
#16818=CARTESIAN_POINT ( 'NONE',  ( 14.76093561896379214, 3.316774720514426456, -28.39148769130088468 ) ) ;
#16825=CARTESIAN_POINT ( 'NONE',  ( -23.59123376470063960, -6.143225279485574397, 24.50402280011862288 ) ) ;
#16842=TOROIDAL_SURFACE ( 'NONE', #73576, 253.2618649670780826, 0.8159999999999999476 ) ;
#16872=LINE ( 'NONE', #15868, #74967 ) ;
#16877=VERTEX_POINT ( 'NONE', #36175 ) ;
#16892=LINE ( 'NONE', #27393, #72964 ) ;
#16902=VECTOR ( 'NONE', #18687, 1000.000000000000114 ) ;
#16910=DIRECTION ( 'NONE',  ( -0.000000000000000000, -1.000000000000000000, -0.000000000000000000 ) ) ;
#16914=CARTESIAN_POINT ( 'NONE',  ( -28.47875734969025885, -6.475225279485573360, -0.08597719988137117464 ) ) ;
#16938=LINE ( 'NONE', #76820, #39413 ) ;
#16939=EDGE_CURVE ( 'NONE', #41305, #628, #78701, .T. ) ;
#16940=DIRECTION ( 'NONE',  ( -1.000000000000000000, 0.000000000000000000, 0.000000000000000000 ) ) ;
#16942=PLANE ( 'NONE',  #7009 ) ;
#16946=EDGE_CURVE ( 'NONE', #89020, #65068, #68617, .T. ) ;
#16956=VERTEX_POINT ( 'NONE', #86342 ) ;
#16980=VERTEX_POINT ( 'NONE', #99539 ) ;
#16991=VERTEX_POINT ( 'NONE', #16825 ) ;
#17001=EDGE_CURVE ( 'NONE', #65428, #48796, #15817, .T. ) ;
#17009=VERTEX_POINT ( 'NONE', #46276 ) ;
#17015=EDGE_CURVE ( 'NONE', #31334, #38206, #88580, .T. ) ;
#17038=VERTEX_POINT ( 'NONE', #87334 ) ;
#17043=LINE ( 'NONE', #47002, #58537 ) ;
#17088=ORIENTED_EDGE ( 'NONE', *, *, #33182, .T. ) ;
#17102=ORIENTED_EDGE ( 'NONE', *, *, #3971, .T. ) ;
#17104=ORIENTED_EDGE ( 'NONE', *, *, #2706, .T. ) ;
#17120=CARTESIAN_POINT ( 'NONE',  ( -10.59832330691884117, 6.376774720514425177, -27.05373799718301697 ) ) ;
#17125=ORIENTED_EDGE ( 'NONE', *, *, #36009, .F. ) ;
#17129=CIRCLE ( 'NONE', #52771, 3.349999999999998757 ) ;
#17135=ADVANCED_FACE ( 'NONE', ( #49803 ), #80735, .T. ) ;
#17142=VERTEX_POINT ( 'NONE', #64540 ) ;
#17177=CARTESIAN_POINT ( 'NONE',  ( 30.13634516277803144, 5.269088466187364261, 19.84760796525321780 ) ) ;
#17185=EDGE_CURVE ( 'NONE', #34410, #52696, #83382, .T. ) ;
#17200=AXIS2_PLACEMENT_3D ( 'NONE', #90807, #76069, #75564 ) ;
#17204=VECTOR ( 'NONE', #28311, 1000.000000000000000 ) ;
#17213=CARTESIAN_POINT ( 'NONE',  ( 32.95803010956177559, 3.605854314291305762, -13.01399263622904812 ) ) ;
#17223=EDGE_CURVE ( 'NONE', #56438, #64548, #91330, .T. ) ;
#17236=ORIENTED_EDGE ( 'NONE', *, *, #94626, .F. ) ;
#17245=ADVANCED_FACE ( 'NONE', ( #28428 ), #59905, .F. ) ;
#17250=CIRCLE ( 'NONE', #44865, 1.699999999999998401 ) ;
#17261=VECTOR ( 'NONE', #33063, 1000.000000000000000 ) ;
#17264=ORIENTED_EDGE ( 'NONE', *, *, #75936, .F. ) ;
#17265=FACE_OUTER_BOUND ( 'NONE', #37069, .T. ) ;
#17276=EDGE_CURVE ( 'NONE', #17142, #96497, #73620, .T. ) ;
#17289=CARTESIAN_POINT ( 'NONE',  ( -65.05438548721849656, 5.356774720514425603, 23.50402280011858736 ) ) ;
#17291=DIRECTION ( 'NONE',  ( 0.000000000000000000, 1.000000000000000000, -0.000000000000000000 ) ) ;
#17294=DIRECTION ( 'NONE',  ( -0.000000000000000000, -1.000000000000000000, -0.000000000000000000 ) ) ;
#17307=CARTESIAN_POINT ( 'NONE',  ( 13.64113475014448440, 6.376774720514426953, -28.24100986136700087 ) ) ;
#17316=LINE ( 'NONE', #88340, #54334 ) ;
#17337=CARTESIAN_POINT ( 'NONE',  ( 29.58033090225963591, 3.719533051881441121, 29.19816577366266941 ) ) ;
#17342=ORIENTED_EDGE ( 'NONE', *, *, #88179, .F. ) ;
#17343=CARTESIAN_POINT ( 'NONE',  ( 0.000000000000000000, -16.94322527948557422, 0.000000000000000000 ) ) ;
#17349=DIRECTION ( 'NONE',  ( 1.000000000000000000, 0.000000000000000000, 0.000000000000000000 ) ) ;
#17356=ORIENTED_EDGE ( 'NONE', *, *, #52294, .F. ) ;
#17357=( BOUNDED_SURFACE ( )  B_SPLINE_SURFACE ( 3, 2, ( 
 ( #83456, #52026, #74356 ),
 ( #5843, #36302, #29677 ),
 ( #51531, #60152, #59648 ),
 ( #91568, #91073, #4849 ),
 ( #20561, #81974, #13944 ),
 ( #12454, #43913, #97692 ) ),
 .UNSPECIFIED., .F., .F., .F. ) 
 B_SPLINE_SURFACE_WITH_KNOTS ( ( 4, 2, 4 ),
 ( 3, 3 ),
 ( 0.04217399329892001364, 0.04576393237407583303, 0.04935387144923164549 ),
 ( 0.000000000000000000, 1.000000000000000000 ),
 .UNSPECIFIED. ) 
 GEOMETRIC_REPRESENTATION_ITEM ( )  RATIONAL_B_SPLINE_SURFACE ( (
 ( 1.000000000000000000, 0.7071067811865475727, 1.000000000000000000),
 ( 1.000000000000000000, 0.7325703083253984893, 1.000000000000000000),
 ( 1.000000000000000000, 0.7567337024450505600, 1.000000000000000000),
 ( 1.000000000000000000, 0.8025768260704856383, 1.000000000000000000),
 ( 1.000000000000000000, 0.8242588182985012280, 1.000000000000000000),
 ( 1.000000000000000000, 0.8446854842613638059, 1.000000000000000000) ) ) 
 REPRESENTATION_ITEM ( '' )  SURFACE ( )  );
#17366=DIRECTION ( 'NONE',  ( 0.000000000000000000, 1.000000000000000000, 0.000000000000000000 ) ) ;
#17394=EDGE_CURVE ( 'NONE', #92240, #95461, #69997, .T. ) ;
#17396=AXIS2_PLACEMENT_3D ( 'NONE', #29396, #75559, #66986 ) ;
#17407=VECTOR ( 'NONE', #8375, 1000.000000000000000 ) ;
#17408=DIRECTION ( 'NONE',  ( 0.000000000000000000, 0.000000000000000000, 1.000000000000000000 ) ) ;
#17417=ORIENTED_EDGE ( 'NONE', *, *, #78059, .T. ) ;
#17443=DIRECTION ( 'NONE',  ( 0.000000000000000000, 1.000000000000000000, -0.000000000000000000 ) ) ;
#17444=CARTESIAN_POINT ( 'NONE',  ( -2.768609665556980293, 0.3587747205144057872, -29.41086200512614823 ) ) ;
#17466=FACE_OUTER_BOUND ( 'NONE', #86402, .T. ) ;
#17467=DIRECTION ( 'NONE',  ( 0.000000000000000000, 0.000000000000000000, -1.000000000000000000 ) ) ;
#17470=CARTESIAN_POINT ( 'NONE',  ( 282.9764569301858046, 4.540774720514427543, 20.79159422840526616 ) ) ;
#17476=DIRECTION ( 'NONE',  ( 0.000000000000000000, 1.000000000000000000, 0.000000000000000000 ) ) ;
#17477=ORIENTED_EDGE ( 'NONE', *, *, #66629, .T. ) ;
#17484=EDGE_CURVE ( 'NONE', #26765, #55186, #24405, .T. ) ;
#17493=ORIENTED_EDGE ( 'NONE', *, *, #59986, .F. ) ;
#17494=CARTESIAN_POINT ( 'NONE',  ( -20.27875734969026311, 5.356774720514425603, 24.00402280011862288 ) ) ;
#17501=ORIENTED_EDGE ( 'NONE', *, *, #26756, .F. ) ;
#17504=DIRECTION ( 'NONE',  ( -0.000000000000000000, 1.000000000000000000, -0.000000000000000000 ) ) ;
#17523=ORIENTED_EDGE ( 'NONE', *, *, #41772, .F. ) ;
#17525=CARTESIAN_POINT ( 'NONE',  ( -2.872281323269014752, -1.473225279485573358, 1.999999999999999556 ) ) ;
#17530=DIRECTION ( 'NONE',  ( 0.000000000000000000, 0.000000000000000000, -1.000000000000000000 ) ) ;
#17558=AXIS2_PLACEMENT_3D ( 'NONE', #42681, #74601, #5094 ) ;
#17588=DIRECTION ( 'NONE',  ( -0.6451914333552788428, 0.000000000000000000, -0.7640209514960704107 ) ) ;
#17596=CARTESIAN_POINT ( 'NONE',  ( 32.65434780274890159, 3.991214330829748747, -3.988850826987774489 ) ) ;
#17601=EDGE_CURVE ( 'NONE', #70795, #22449, #97012, .T. ) ;
#17604=ORIENTED_EDGE ( 'NONE', *, *, #88779, .T. ) ;
#17615=CARTESIAN_POINT ( 'NONE',  ( 29.70906083364843653, 4.222256839740661682, 27.99786980188468277 ) ) ;
#17617=CARTESIAN_POINT ( 'NONE',  ( -65.05438548721848235, -6.475225279485573360, 29.49402280011861777 ) ) ;
#17627=CARTESIAN_POINT ( 'NONE',  ( 15.29947330337543754, 6.376774720514426953, -27.16854002387008649 ) ) ;
#17658=ORIENTED_EDGE ( 'NONE', *, *, #89411, .T. ) ;
#17667=CARTESIAN_POINT ( 'NONE',  ( -17.64648606763744354, 0.3587747205144061202, -23.04404205923973237 ) ) ;
#17674=CARTESIAN_POINT ( 'NONE',  ( 14.73162737928355170, 2.682774720514426559, -27.37940951657878941 ) ) ;
#17683=CARTESIAN_POINT ( 'NONE',  ( -29.49875734969026198, 0.3587747205144265483, 2.362022800118626531 ) ) ;
#17692=CIRCLE ( 'NONE', #19272, 129.7684398600581517 ) ;
#17699=CARTESIAN_POINT ( 'NONE',  ( 33.63243172119919677, 3.340070231344507423, -11.49682753434938043 ) ) ;
#17703=LINE ( 'NONE', #18688, #6860 ) ;
#17708=FACE_OUTER_BOUND ( 'NONE', #8706, .T. ) ;
#17734=DIRECTION ( 'NONE',  ( 0.000000000000000000, 0.000000000000000000, 1.000000000000000000 ) ) ;
#17738=VERTEX_POINT ( 'NONE', #80606 ) ;
#17742=VERTEX_POINT ( 'NONE', #3003 ) ;
#17743=CARTESIAN_POINT ( 'NONE',  ( 22.02124265030973760, -6.143225279485574397, 13.95402280011862395 ) ) ;
#17745=ORIENTED_EDGE ( 'NONE', *, *, #43289, .F. ) ;
#17747=VECTOR ( 'NONE', #92343, 1000.000000000000000 ) ;
#17760=EDGE_CURVE ( 'NONE', #19353, #11284, #5818, .T. ) ;
#17765=ORIENTED_EDGE ( 'NONE', *, *, #89088, .T. ) ;
#17779=CARTESIAN_POINT ( 'NONE',  ( -27.86046284349297864, -5.965225279485572685, -8.091963836038754465 ) ) ;
#17788=CARTESIAN_POINT ( 'NONE',  ( 0.000000000000000000, -16.94322527948557422, 0.000000000000000000 ) ) ;
#17803=FACE_OUTER_BOUND ( 'NONE', #45602, .T. ) ;
#17804=DIRECTION ( 'NONE',  ( 0.1489078231574191002, -6.845827386180410961E-16, -0.9888510809027407644 ) ) ;
#17816=CARTESIAN_POINT ( 'NONE',  ( 11.40529837385589218, 6.376774720514345240, -28.07356074678033409 ) ) ;
#17827=EDGE_CURVE ( 'NONE', #79519, #5376, #67391, .T. ) ;
#17829=VERTEX_POINT ( 'NONE', #88731 ) ;
#17834=DIRECTION ( 'NONE',  ( 0.000000000000000000, 0.000000000000000000, -1.000000000000000000 ) ) ;
#17835=CARTESIAN_POINT ( 'NONE',  ( 13.91401389203221406, 6.376774720514426953, 28.26920385068457264 ) ) ;
#17841=CARTESIAN_POINT ( 'NONE',  ( 14.74567117936177851, 4.687674228468470261, -27.80582190761142414 ) ) ;
#17845=VERTEX_POINT ( 'NONE', #96829 ) ;
#17857=DIRECTION ( 'NONE',  ( 0.000000000000000000, 1.000000000000000000, 0.000000000000000000 ) ) ;
#17881=CIRCLE ( 'NONE', #79442, 252.4458649670781085 ) ;
#17901=VERTEX_POINT ( 'NONE', #13578 ) ;
#17905=CIRCLE ( 'NONE', #35729, 1.150000000000003464 ) ;
#17906=FACE_OUTER_BOUND ( 'NONE', #70884, .T. ) ;
#17911=CARTESIAN_POINT ( 'NONE',  ( 13.91401389203221406, 6.376774720514426953, 158.0376437107427137 ) ) ;
#17946=CYLINDRICAL_SURFACE ( 'NONE', #21575, 1.149999999999998135 ) ;
#17963=DIRECTION ( 'NONE',  ( 0.000000000000000000, -1.000000000000000000, 0.000000000000000000 ) ) ;
#17983=ORIENTED_EDGE ( 'NONE', *, *, #32131, .F. ) ;
#17996=ORIENTED_EDGE ( 'NONE', *, *, #60573, .F. ) ;
#18013=CARTESIAN_POINT ( 'NONE',  ( -20.27875734969026311, -6.143225279485574397, 24.00402280011862288 ) ) ;
#18026=LINE ( 'NONE', #79419, #94335 ) ;
#18059=CARTESIAN_POINT ( 'NONE',  ( 14.61581676223891613, 3.582999323269832725, -27.35847991879931485 ) ) ;
#18079=CARTESIAN_POINT ( 'NONE',  ( 30.61643171304412903, 3.316774720514426456, 27.37433008668283207 ) ) ;
#18107=APPLICATION_CONTEXT ( 'configuration controlled 3d designs of mechanical parts and assemblies' ) ;
#18117=CARTESIAN_POINT ( 'NONE',  ( 29.71114493364435916, 4.339464138238508184, 27.93491297891351621 ) ) ;
#18118=CARTESIAN_POINT ( 'NONE',  ( 33.74607884027702909, 0.3587747205144265483, -4.999864028243830916 ) ) ;
#18134=LINE ( 'NONE', #49103, #47781 ) ;
#18150=ADVANCED_FACE ( 'NONE', ( #49555 ), #72324, .F. ) ;
#18170=VECTOR ( 'NONE', #79209, 1000.000000000000000 ) ;
#18180=FACE_OUTER_BOUND ( 'NONE', #59110, .T. ) ;
#18183=EDGE_CURVE ( 'NONE', #17742, #34210, #99805, .T. ) ;
#18192=VERTEX_POINT ( 'NONE', #52042 ) ;
#18200=CARTESIAN_POINT ( 'NONE',  ( 33.55975867735808293, 4.270419025147584868, -12.32584534477734728 ) ) ;
#18208=ADVANCED_FACE ( 'NONE', ( #41945 ), #34821, .T. ) ;
#18228=VERTEX_POINT ( 'NONE', #42448 ) ;
#18230=CARTESIAN_POINT ( 'NONE',  ( 31.93426202889373400, -5.965225279485572685, 6.907000118922836940 ) ) ;
#18237=ORIENTED_EDGE ( 'NONE', *, *, #36265, .F. ) ;
#18238=CIRCLE ( 'NONE', #74928, 2.249999999999998668 ) ;
#18242=EDGE_LOOP ( 'NONE', ( #35900, #13266, #45234, #49572, #70198 ) ) ;
#18260=VERTEX_POINT ( 'NONE', #73878 ) ;
#18293=FACE_OUTER_BOUND ( 'NONE', #45181, .T. ) ;
#18295=VECTOR ( 'NONE', #21382, 1000.000000000000000 ) ;
#18300=CARTESIAN_POINT ( 'NONE',  ( 30.00738719773716312, 4.772774720514425972, -9.049252915307087974 ) ) ;
#18305=CARTESIAN_POINT ( 'NONE',  ( -19.77875734969026311, -6.143225279485574397, 29.49402280011862487 ) ) ;
#18326=CARTESIAN_POINT ( 'NONE',  ( 27.86270917940689174, 0.3587747205144265483, 29.49402280011862487 ) ) ;
#18341=VECTOR ( 'NONE', #91246, 1000.000000000000000 ) ;
#18360=ORIENTED_EDGE ( 'NONE', *, *, #79548, .T. ) ;
#18367=VERTEX_POINT ( 'NONE', #22555 ) ;
#18400=EDGE_CURVE ( 'NONE', #48069, #43651, #68760, .T. ) ;
#18404=CARTESIAN_POINT ( 'NONE',  ( 10.46399479596398052, 2.894108053847758821, -27.03001098546561920 ) ) ;
#18444=DIRECTION ( 'NONE',  ( 0.000000000000000000, -0.000000000000000000, -1.000000000000000000 ) ) ;
#18445=LINE ( 'NONE', #66150, #36541 ) ;
#18466=DIRECTION ( 'NONE',  ( 0.000000000000000000, 0.000000000000000000, 1.000000000000000000 ) ) ;
#18475=VERTEX_POINT ( 'NONE', #25577 ) ;
#18480=CARTESIAN_POINT ( 'NONE',  ( 22.81105451610979173, -1.475225279485572916, -19.61691820600746539 ) ) ;
#18484=VERTEX_POINT ( 'NONE', #47925 ) ;
#18496=ORIENTED_EDGE ( 'NONE', *, *, #8216, .F. ) ;
#18514=DIRECTION ( 'NONE',  ( 0.000000000000000000, 0.000000000000000000, 1.000000000000000000 ) ) ;
#18520=VECTOR ( 'NONE', #85353, 1000.000000000000000 ) ;
#18526=EDGE_LOOP ( 'NONE', ( #98368, #47726, #80169, #56781 ) ) ;
#18542=AXIS2_PLACEMENT_3D ( 'NONE', #29968, #60937, #91868 ) ;
#18556=CARTESIAN_POINT ( 'NONE',  ( 14.10331789289311111, 5.152774720514426754, -26.41276880514442738 ) ) ;
#18557=CARTESIAN_POINT ( 'NONE',  ( 15.10352928271630724, 2.682774720514426559, -27.29968155418892195 ) ) ;
#18559=LINE ( 'NONE', #49533, #80420 ) ;
#18569=ADVANCED_FACE ( 'NONE', ( #71763 ), #9849, .F. ) ;
#18598=ORIENTED_EDGE ( 'NONE', *, *, #43165, .T. ) ;
#18615=EDGE_LOOP ( 'NONE', ( #44390, #13695, #2491, #33466 ) ) ;
#18625=FACE_OUTER_BOUND ( 'NONE', #1545, .T. ) ;
#18634=ORIENTED_EDGE ( 'NONE', *, *, #34263, .T. ) ;
#18649=ORIENTED_EDGE ( 'NONE', *, *, #72695, .T. ) ;
#18661=CARTESIAN_POINT ( 'NONE',  ( 5.395440699609677537, -5.965225279485594001, -28.51842087987364138 ) ) ;
#18678=DIRECTION ( 'NONE',  ( 0.000000000000000000, 0.000000000000000000, -1.000000000000000000 ) ) ;
#18681=CARTESIAN_POINT ( 'NONE',  ( 25.61870917940689196, -5.965225279485572685, 29.49402280011862487 ) ) ;
#18687=DIRECTION ( 'NONE',  ( -0.3133898629642186684, -4.164321980682960499E-15, 0.9496245541219267006 ) ) ;
#18688=CARTESIAN_POINT ( 'NONE',  ( 9.402885806365684829, -5.965225279485572685, 29.04108526060719342 ) ) ;
#18696=DIRECTION ( 'NONE',  ( 0.000000000000000000, 0.000000000000000000, -1.000000000000000000 ) ) ;
#18698=CARTESIAN_POINT ( 'NONE',  ( -25.92875734969025814, 6.376774720514426953, 30.51402280011862089 ) ) ;
#18703=VECTOR ( 'NONE', #69886, 1000.000000000000000 ) ;
#18708=ORIENTED_EDGE ( 'NONE', *, *, #2634, .F. ) ;
#18724=EDGE_CURVE ( 'NONE', #45794, #82268, #13994, .T. ) ;
#18734=DIRECTION ( 'NONE',  ( 0.000000000000000000, 1.000000000000000000, 0.000000000000000000 ) ) ;
#18747=CARTESIAN_POINT ( 'NONE',  ( -0.02075734969026423599, 0.3587747205144213303, -0.08597719988137648983 ) ) ;
#18754=LINE ( 'NONE', #63971, #85524 ) ;
#18767=ORIENTED_EDGE ( 'NONE', *, *, #6082, .T. ) ;
#18790=VECTOR ( 'NONE', #87313, 1000.000000000000000 ) ;
#18813=DIRECTION ( 'NONE',  ( 0.000000000000000000, 0.000000000000000000, -1.000000000000000000 ) ) ;
#18816=DIRECTION ( 'NONE',  ( -0.000000000000000000, -0.000000000000000000, -1.000000000000000000 ) ) ;
#18822=CARTESIAN_POINT ( 'NONE',  ( 13.91401389203221406, -6.475225279485573360, 158.0376437107427137 ) ) ;
#18825=CARTESIAN_POINT ( 'NONE',  ( 15.48350366603705552, 4.450064631497443024, -28.28653584630381701 ) ) ;
#18841=CARTESIAN_POINT ( 'NONE',  ( 15.02167523160210294, 3.508919134408378770, -27.32290745209846250 ) ) ;
#18847=ORIENTED_EDGE ( 'NONE', *, *, #86927, .F. ) ;
#18854=ORIENTED_EDGE ( 'NONE', *, *, #76878, .T. ) ;
#18855=VECTOR ( 'NONE', #91482, 1000.000000000000000 ) ;
#18870=ORIENTED_EDGE ( 'NONE', *, *, #21584, .F. ) ;
#18876=ORIENTED_EDGE ( 'NONE', *, *, #51044, .T. ) ;
#18878=ORIENTED_EDGE ( 'NONE', *, *, #13111, .F. ) ;
#18887=DIRECTION ( 'NONE',  ( -0.000000000000000000, -1.000000000000000000, -0.000000000000000000 ) ) ;
#18889=AXIS2_PLACEMENT_3D ( 'NONE', #58562, #18986, #49964 ) ;
#18892=ORIENTED_EDGE ( 'NONE', *, *, #7932, .T. ) ;
#18898=EDGE_CURVE ( 'NONE', #34410, #4424, #11192, .T. ) ;
#18935=AXIS2_PLACEMENT_3D ( 'NONE', #34633, #19884, #34134 ) ;
#18936=FACE_OUTER_BOUND ( 'NONE', #34352, .T. ) ;
#18943=DIRECTION ( 'NONE',  ( -0.000000000000000000, 0.000000000000000000, 1.000000000000000000 ) ) ;
#18960=LINE ( 'NONE', #26587, #82653 ) ;
#18962=EDGE_CURVE ( 'NONE', #6678, #10266, #13816, .T. ) ;
#18978=EDGE_CURVE ( 'NONE', #80003, #28802, #21922, .T. ) ;
#18980=ORIENTED_EDGE ( 'NONE', *, *, #46029, .T. ) ;
#18981=DIRECTION ( 'NONE',  ( -1.000000000000000000, 0.000000000000000000, -0.000000000000000000 ) ) ;
#18986=DIRECTION ( 'NONE',  ( 0.7512896232465888779, 8.688531644690855961E-16, 0.6599726524652355097 ) ) ;
#19001=DIRECTION ( 'NONE',  ( 1.251281512149627050E-16, 0.000000000000000000, -1.000000000000000000 ) ) ;
#19003=VECTOR ( 'NONE', #11648, 1000.000000000000000 ) ;
#19013=DIRECTION ( 'NONE',  ( -1.000000000000000000, -0.000000000000000000, -0.000000000000000000 ) ) ;
#19025=ORIENTED_EDGE ( 'NONE', *, *, #78208, .F. ) ;
#19031=CARTESIAN_POINT ( 'NONE',  ( 1.175186991919848989, -5.965225279485572685, 28.89597625626659649 ) ) ;
#19038=VERTEX_POINT ( 'NONE', #61015 ) ;
#19040=CIRCLE ( 'NONE', #1157, 3.349999999999998757 ) ;
#19054=CARTESIAN_POINT ( 'NONE',  ( 12.88745205064171273, 3.316774720517230435, -28.14312002837575477 ) ) ;
#19060=DIRECTION ( 'NONE',  ( -0.000000000000000000, -1.000000000000000000, -0.000000000000000000 ) ) ;
#19079=DIRECTION ( 'NONE',  ( 0.000000000000000000, 0.000000000000000000, -1.000000000000000000 ) ) ;
#19085=CYLINDRICAL_SURFACE ( 'NONE', #82159, 3.060000000000000053 ) ;
#19102=ADVANCED_FACE ( 'NONE', ( #55913 ), #9209, .T. ) ;
#19105=CIRCLE ( 'NONE', #80679, 1.836000000000000743 ) ;
#19124=LINE ( 'NONE', #50585, #28423 ) ;
#19139=AXIS2_PLACEMENT_3D ( 'NONE', #19363, #55945, #80268 ) ;
#19140=EDGE_CURVE ( 'NONE', #40087, #91590, #71125, .T. ) ;
#19168=DIRECTION ( 'NONE',  ( 0.000000000000000000, -1.478457507934778393E-16, -1.000000000000000000 ) ) ;
#19177=EDGE_CURVE ( 'NONE', #51486, #52686, #9145, .T. ) ;
#19214=ORIENTED_EDGE ( 'NONE', *, *, #98707, .F. ) ;
#19222=PLANE ( 'NONE',  #88206 ) ;
#19223=CARTESIAN_POINT ( 'NONE',  ( 29.80070917940689412, -6.475225279485573360, 27.39560796525321607 ) ) ;
#19225=ADVANCED_FACE ( 'NONE', ( #27455 ), #57913, .F. ) ;
#19235=ORIENTED_EDGE ( 'NONE', *, *, #19438, .F. ) ;
#19237=ORIENTED_EDGE ( 'NONE', *, *, #44663, .T. ) ;
#19239=ORIENTED_EDGE ( 'NONE', *, *, #63421, .F. ) ;
#19250=EDGE_LOOP ( 'NONE', ( #92920, #97836, #92029, #45523 ) ) ;
#19268=CARTESIAN_POINT ( 'NONE',  ( -23.24941632505786870, 6.376774720514426953, 27.45402280011862572 ) ) ;
#19272=AXIS2_PLACEMENT_3D ( 'NONE', #88959, #11330, #74227 ) ;
#19295=ADVANCED_FACE ( 'NONE', ( #96454 ), #12704, .F. ) ;
#19306=CIRCLE ( 'NONE', #85729, 129.7684398600581517 ) ;
#19335=CARTESIAN_POINT ( 'NONE',  ( 31.61557479013512761, 6.410763075590563354, 26.52166531862750531 ) ) ;
#19336=ORIENTED_EDGE ( 'NONE', *, *, #55821, .T. ) ;
#19337=AXIS2_PLACEMENT_3D ( 'NONE', #66198, #5263, #97119 ) ;
#19339=ADVANCED_FACE ( 'NONE', ( #28430 ), #61406, .F. ) ;
#19341=AXIS2_PLACEMENT_3D ( 'NONE', #100044, #84843, #60534 ) ;
#19353=VERTEX_POINT ( 'NONE', #13701 ) ;
#19363=CARTESIAN_POINT ( 'NONE',  ( 0.000000000000000000, 1.826774720514426464, 0.000000000000000000 ) ) ;
#19386=ORIENTED_EDGE ( 'NONE', *, *, #55786, .F. ) ;
#19387=CARTESIAN_POINT ( 'NONE',  ( -13.89275734969026388, -5.965225279485572685, 31.02402280011862246 ) ) ;
#19388=LINE ( 'NONE', #57480, #21616 ) ;
#19405=VECTOR ( 'NONE', #34840, 1000.000000000000000 ) ;
#19412=AXIS2_PLACEMENT_3D ( 'NONE', #25506, #48860, #81293 ) ;
#19420=AXIS2_PLACEMENT_3D ( 'NONE', #77201, #90450, #69103 ) ;
#19438=EDGE_CURVE ( 'NONE', #84636, #31830, #14061, .T. ) ;
#19452=EDGE_CURVE ( 'NONE', #80644, #74508, #79729, .T. ) ;
#19458=DIRECTION ( 'NONE',  ( -1.607395343451207646E-13, 0.000000000000000000, -1.000000000000000000 ) ) ;
#19459=DIRECTION ( 'NONE',  ( -0.000000000000000000, 1.000000000000000000, -0.000000000000000000 ) ) ;
#19464=CARTESIAN_POINT ( 'NONE',  ( 11.22434917415779054, 4.132774715458839232, -26.87660878605755599 ) ) ;
#19471=ORIENTED_EDGE ( 'NONE', *, *, #44281, .F. ) ;
#19472=CARTESIAN_POINT ( 'NONE',  ( 11.98973536156539943, 2.682774720514426559, -26.26140391504922178 ) ) ;
#19474=PLANE ( 'NONE',  #58479 ) ;
#19477=AXIS2_PLACEMENT_3D ( 'NONE', #98433, #35564, #59906 ) ;
#19485=EDGE_LOOP ( 'NONE', ( #57440, #60577, #65356, #92175, #61421, #904, #67312, #41126, #12056, #91928, #89631, #20094, #49599, #26550, #89544, #99507, #72265, #59669 ) ) ;
#19494=ORIENTED_EDGE ( 'NONE', *, *, #16136, .F. ) ;
#19546=LINE ( 'NONE', #50506, #45078 ) ;
#19547=CARTESIAN_POINT ( 'NONE',  ( -0.02075734969026423599, -6.475225279485573360, -28.03397719988137382 ) ) ;
#19554=CARTESIAN_POINT ( 'NONE',  ( 14.85834502026402681, 3.582999323269832725, -27.37203305628894867 ) ) ;
#19569=EDGE_LOOP ( 'NONE', ( #75489, #89761, #93747 ) ) ;
#19579=LINE ( 'NONE', #27208, #89182 ) ;
#19595=ORIENTED_EDGE ( 'NONE', *, *, #86883, .T. ) ;
#19596=VERTEX_POINT ( 'NONE', #32948 ) ;
#19609=ORIENTED_EDGE ( 'NONE', *, *, #4660, .F. ) ;
#19625=CARTESIAN_POINT ( 'NONE',  ( 10.01577673925062584, 3.316774720514425567, -27.02510548822787584 ) ) ;
#19629=EDGE_LOOP ( 'NONE', ( #31384, #73804, #38041, #19494 ) ) ;
#19632=CARTESIAN_POINT ( 'NONE',  ( 5.265981236333619456E-16, 1.826774720514426464, -4.300000000000000711 ) ) ;
#19655=ADVANCED_FACE ( 'NONE', ( #78591 ), #65916, .F. ) ;
#19669=CARTESIAN_POINT ( 'NONE',  ( 33.12653832968937451, 0.3587747205144265483, -7.315055336576590683 ) ) ;
#19683=DIRECTION ( 'NONE',  ( -0.5630016722799275897, -4.164321980682959710E-15, 0.8264557562326038109 ) ) ;
#19685=VERTEX_POINT ( 'NONE', #26330 ) ;
#19699=CARTESIAN_POINT ( 'NONE',  ( -19.77875734969026311, -6.143225279485574397, 27.35402280011862430 ) ) ;
#19700=DIRECTION ( 'NONE',  ( 0.000000000000000000, 0.000000000000000000, -1.000000000000000000 ) ) ;
#19703=ORIENTED_EDGE ( 'NONE', *, *, #59636, .T. ) ;
#19713=DIRECTION ( 'NONE',  ( 1.000000000000000000, 0.000000000000000000, 0.000000000000000000 ) ) ;
#19723=ADVANCED_FACE ( 'NONE', ( #12088 ), #33942, .T. ) ;
#19728=DIRECTION ( 'NONE',  ( 4.251773225433346808E-15, 0.000000000000000000, -1.000000000000000000 ) ) ;
#19745=CARTESIAN_POINT ( 'NONE',  ( 10.46399479596396453, 2.682774720514426559, -27.03001098546561920 ) ) ;
#19748=CARTESIAN_POINT ( 'NONE',  ( -0.02075734969026423599, 5.866774720514426278, 22.60902280011862686 ) ) ;
#19749=ORIENTED_EDGE ( 'NONE', *, *, #92027, .T. ) ;
#19785=LINE ( 'NONE', #58869, #74952 ) ;
#19803=LINE ( 'NONE', #4102, #83309 ) ;
#19804=CARTESIAN_POINT ( 'NONE',  ( 27.53860345374771867, -1.477225279485574028, -9.482392034746240483 ) ) ;
#19814=VECTOR ( 'NONE', #97071, 1000.000000000000000 ) ;
#19816=DIRECTION ( 'NONE',  ( 0.000000000000000000, 3.055962005780221396E-15, -1.000000000000000000 ) ) ;
#19819=ORIENTED_EDGE ( 'NONE', *, *, #70735, .F. ) ;
#19823=CARTESIAN_POINT ( 'NONE',  ( 31.62401270459618630, 4.290926300276496796, 26.86768354919275836 ) ) ;
#19858=ORIENTED_EDGE ( 'NONE', *, *, #45998, .F. ) ;
#19864=ORIENTED_EDGE ( 'NONE', *, *, #75366, .T. ) ;
#19872=CARTESIAN_POINT ( 'NONE',  ( 29.73860345376319358, 4.772774720514425972, -8.849814207987163783 ) ) ;
#19884=DIRECTION ( 'NONE',  ( 0.000000000000000000, -1.000000000000000000, 0.000000000000000000 ) ) ;
#19944=ORIENTED_EDGE ( 'NONE', *, *, #93302, .T. ) ;
#19958=CARTESIAN_POINT ( 'NONE',  ( 10.86264265030973952, -5.965225279485574461, -27.62597719988137612 ) ) ;
#19967=DIRECTION ( 'NONE',  ( 0.000000000000000000, -1.000000000000000000, 0.000000000000000000 ) ) ;
#19971=EDGE_LOOP ( 'NONE', ( #43586, #26968, #80985, #81512 ) ) ;
#19984=ADVANCED_FACE ( 'NONE', ( #95720 ), #19085, .T. ) ;
#19990=CARTESIAN_POINT ( 'NONE',  ( 30.09341516180546350, 2.682774720514426559, -11.39311774897855756 ) ) ;
#19994=LINE ( 'NONE', #27622, #6898 ) ;
#20019=ORIENTED_EDGE ( 'NONE', *, *, #59986, .T. ) ;
#20029=( BOUNDED_SURFACE ( )  B_SPLINE_SURFACE ( 3, 2, ( 
 ( #10961, #65281, #32793 ),
 ( #63774, #73366, #95196 ),
 ( #3862, #79965, #33797 ),
 ( #65774, #2356, #33287 ) ),
 .UNSPECIFIED., .F., .F., .T. ) 
 B_SPLINE_SURFACE_WITH_KNOTS ( ( 4, 4 ),
 ( 3, 3 ),
 ( 0.004439845973569162343, 0.004703938444645663561 ),
 ( 0.000000000000000000, 1.000000000000000000 ),
 .UNSPECIFIED. ) 
 GEOMETRIC_REPRESENTATION_ITEM ( )  RATIONAL_B_SPLINE_SURFACE ( (
 ( 1.000000000000000000, 0.9005394799515968884, 1.000000000000000000),
 ( 1.000000000000000000, 0.9005352985759393913, 1.000000000000000000),
 ( 1.000000000000000000, 0.8990570573199260229, 1.000000000000000000),
 ( 1.000000000000000000, 0.8962098481621323387, 1.000000000000000000) ) ) 
 REPRESENTATION_ITEM ( '' )  SURFACE ( )  );
#20042=VERTEX_POINT ( 'NONE', #4874 ) ;
#20058=CARTESIAN_POINT ( 'NONE',  ( 15.22325621495362391, 2.682774720514426559, -27.23549315679322547 ) ) ;
#20067=CARTESIAN_POINT ( 'NONE',  ( -24.90875734969025501, 0.3587747205144265483, 26.43402280011862615 ) ) ;
#20068=CIRCLE ( 'NONE', #52453, 3.060000000000000053 ) ;
#20072=CARTESIAN_POINT ( 'NONE',  ( 30.62809631291915835, 4.628857374213141362, 27.84496821199607908 ) ) ;
#20090=EDGE_CURVE ( 'NONE', #97596, #51332, #75363, .T. ) ;
#20094=ORIENTED_EDGE ( 'NONE', *, *, #59473, .T. ) ;
#20097=VERTEX_POINT ( 'NONE', #27712 ) ;
#20098=ORIENTED_EDGE ( 'NONE', *, *, #17015, .T. ) ;
#20102=FACE_OUTER_BOUND ( 'NONE', #73227, .T. ) ;
#20106=ORIENTED_EDGE ( 'NONE', *, *, #60001, .F. ) ;
#20115=VECTOR ( 'NONE', #8361, 1000.000000000000000 ) ;
#20127=FACE_OUTER_BOUND ( 'NONE', #84014, .T. ) ;
#20136=ORIENTED_EDGE ( 'NONE', *, *, #35385, .T. ) ;
#20147=ORIENTED_EDGE ( 'NONE', *, *, #86883, .F. ) ;
#20149=FACE_OUTER_BOUND ( 'NONE', #52712, .T. ) ;
#20160=EDGE_CURVE ( 'NONE', #92435, #31493, #75615, .T. ) ;
#20183=ORIENTED_EDGE ( 'NONE', *, *, #91792, .T. ) ;
#20196=VECTOR ( 'NONE', #59117, 1000.000000000000000 ) ;
#20203=DIRECTION ( 'NONE',  ( -0.000000000000000000, -1.000000000000000000, 0.000000000000000000 ) ) ;
#20213=EDGE_CURVE ( 'NONE', #41039, #48956, #46526, .T. ) ;
#20232=CARTESIAN_POINT ( 'NONE',  ( 31.84105487026623393, 5.152774720514427642, -11.95870468328481806 ) ) ;
#20237=AXIS2_PLACEMENT_3D ( 'NONE', #81147, #3534, #66450 ) ;
#20243=DIRECTION ( 'NONE',  ( -0.000000000000000000, 1.000000000000000000, -0.000000000000000000 ) ) ;
#20257=CARTESIAN_POINT ( 'NONE',  ( 7.805843057017202824, -6.475225279485576024, -27.15467198446602026 ) ) ;
#20264=CARTESIAN_POINT ( 'NONE',  ( 0.000000000000000000, 1.826774720514426464, 0.000000000000000000 ) ) ;
#20281=CARTESIAN_POINT ( 'NONE',  ( 22.81105451610979173, -1.475225279485572916, -17.31691820600746823 ) ) ;
#20303=AXIS2_PLACEMENT_3D ( 'NONE', #33613, #56968, #73674 ) ;
#20305=ORIENTED_EDGE ( 'NONE', *, *, #62145, .F. ) ;
#20317=EDGE_CURVE ( 'NONE', #57723, #9882, #33562, .T. ) ;
#20323=CARTESIAN_POINT ( 'NONE',  ( 15.00444628775324141, 3.502673593626820736, -27.32858455744129245 ) ) ;
#20328=EDGE_CURVE ( 'NONE', #17038, #10813, #61096, .T. ) ;
#20359=EDGE_LOOP ( 'NONE', ( #2018, #21520, #88287, #14866 ) ) ;
#20369=AXIS2_PLACEMENT_3D ( 'NONE', #85683, #16163, #71471 ) ;
#20378=ORIENTED_EDGE ( 'NONE', *, *, #60037, .F. ) ;
#20381=FACE_OUTER_BOUND ( 'NONE', #64710, .T. ) ;
#20387=ADVANCED_FACE ( 'NONE', ( #58053 ), #95096, .T. ) ;
#20388=CARTESIAN_POINT ( 'NONE',  ( 28.87399897812681004, 1.682774720514426114, -12.57761096169975445 ) ) ;
#20425=DIRECTION ( 'NONE',  ( 0.000000000000000000, 1.000000000000000000, 0.000000000000000000 ) ) ;
#20429=FACE_OUTER_BOUND ( 'NONE', #47502, .T. ) ;
#20434=CARTESIAN_POINT ( 'NONE',  ( 30.53060340732035982, 4.132774720517318201, 19.84760796525321780 ) ) ;
#20454=EDGE_CURVE ( 'NONE', #25992, #23706, #89481, .T. ) ;
#20481=DIRECTION ( 'NONE',  ( 0.000000000000000000, 0.000000000000000000, -1.000000000000000000 ) ) ;
#20504=VECTOR ( 'NONE', #43647, 1000.000000000000000 ) ;
#20511=AXIS2_PLACEMENT_3D ( 'NONE', #58411, #95452, #74608 ) ;
#20512=CARTESIAN_POINT ( 'NONE',  ( 31.33322533232960083, 4.132774720514427180, -3.827970713771306155 ) ) ;
#20521=CARTESIAN_POINT ( 'NONE',  ( 8.476323908354110870, 5.356774720514068555, -27.09030197689322961 ) ) ;
#20523=AXIS2_PLACEMENT_3D ( 'NONE', #49169, #58271, #96321 ) ;
#20542=CARTESIAN_POINT ( 'NONE',  ( 12.16765770914787304, -6.475225279485573360, -27.57618308014988173 ) ) ;
#20547=EDGE_CURVE ( 'NONE', #52686, #31493, #63939, .T. ) ;
#20561=CARTESIAN_POINT ( 'NONE',  ( 31.60906425211781823, 3.844812497472038793, -2.545713913898462799 ) ) ;
#20565=CARTESIAN_POINT ( 'NONE',  ( 30.61752088227329693, 5.013017886559611114, 27.44065105897852419 ) ) ;
#20569=VERTEX_POINT ( 'NONE', #2518 ) ;
#20580=VERTEX_POINT ( 'NONE', #30060 ) ;
#20581=CARTESIAN_POINT ( 'NONE',  ( -4.568292318365942073, -5.965225279485572685, 30.06720597538392425 ) ) ;
#20584=AXIS2_PLACEMENT_3D ( 'NONE', #45177, #98434, #37553 ) ;
#20593=ORIENTED_EDGE ( 'NONE', *, *, #65273, .T. ) ;
#20613=ORIENTED_EDGE ( 'NONE', *, *, #11203, .F. ) ;
#20619=ORIENTED_EDGE ( 'NONE', *, *, #92745, .T. ) ;
#20621=( BOUNDED_SURFACE ( )  B_SPLINE_SURFACE ( 3, 2, ( 
 ( #81421, #13385, #12887 ),
 ( #66221, #97140, #97631 ),
 ( #44365, #49990, #43367 ),
 ( #67707, #90521, #27137 ) ),
 .UNSPECIFIED., .F., .F., .T. ) 
 B_SPLINE_SURFACE_WITH_KNOTS ( ( 4, 4 ),
 ( 3, 3 ),
 ( 0.004439845973569162343, 0.004703938444645663561 ),
 ( 0.000000000000000000, 1.000000000000000000 ),
 .UNSPECIFIED. ) 
 GEOMETRIC_REPRESENTATION_ITEM ( )  RATIONAL_B_SPLINE_SURFACE ( (
 ( 1.000000000000000000, 0.9005394799515968884, 1.000000000000000000),
 ( 1.000000000000000000, 0.9005352985759397244, 1.000000000000000000),
 ( 1.000000000000000000, 0.8990570573199264670, 1.000000000000000000),
 ( 1.000000000000000000, 0.8962098481621324497, 1.000000000000000000) ) ) 
 REPRESENTATION_ITEM ( '' )  SURFACE ( )  );
#20634=AXIS2_PLACEMENT_3D ( 'NONE', #93649, #8425, #6925 ) ;
#20647=CARTESIAN_POINT ( 'NONE',  ( 13.99288689683290166, -5.965225279485572685, -28.28242551218217926 ) ) ;
#20656=DIRECTION ( 'NONE',  ( 0.000000000000000000, 0.000000000000000000, -1.000000000000000000 ) ) ;
#20659=CARTESIAN_POINT ( 'NONE',  ( 4.712727796232553779, 3.316774720514426456, -25.55789472434992859 ) ) ;
#20660=EDGE_CURVE ( 'NONE', #36444, #49834, #63431, .T. ) ;
#20661=AXIS2_PLACEMENT_3D ( 'NONE', #77036, #36989, #69441 ) ;
#20662=ADVANCED_FACE ( 'NONE', ( #9617 ), #2021, .T. ) ;
#20668=EDGE_CURVE ( 'NONE', #18228, #74261, #96855, .T. ) ;
#20681=ADVANCED_FACE ( 'NONE', ( #27348 ), #11610, .T. ) ;
#20682=EDGE_LOOP ( 'NONE', ( #94008, #80211, #93881, #14021 ) ) ;
#20687=ORIENTED_EDGE ( 'NONE', *, *, #36706, .T. ) ;
#20699=DIRECTION ( 'NONE',  ( 0.000000000000000000, 0.000000000000000000, 1.000000000000000000 ) ) ;
#20722=ORIENTED_EDGE ( 'NONE', *, *, #33366, .F. ) ;
#20755=CARTESIAN_POINT ( 'NONE',  ( 10.62437663934349530, 3.316774720514425567, -27.03002426119959978 ) ) ;
#20774=DIRECTION ( 'NONE',  ( -1.000000000000000000, 0.000000000000000000, -0.000000000000000000 ) ) ;
#20775=EDGE_CURVE ( 'NONE', #39091, #36941, #75692, .T. ) ;
#20780=EDGE_CURVE ( 'NONE', #62896, #88037, #51186, .T. ) ;
#20786=EDGE_CURVE ( 'NONE', #41305, #54228, #59575, .T. ) ;
#20793=DIRECTION ( 'NONE',  ( 0.000000000000000000, 1.000000000000000000, 0.000000000000000000 ) ) ;
#20798=CARTESIAN_POINT ( 'NONE',  ( 31.63524360068765162, 3.637569336689931543, 27.31569296206930630 ) ) ;
#20800=VECTOR ( 'NONE', #46775, 1000.000000000000000 ) ;
#20801=CARTESIAN_POINT ( 'NONE',  ( 13.91401389203221406, -5.965225279485572685, 158.0376437107427137 ) ) ;
#20806=FACE_OUTER_BOUND ( 'NONE', #22152, .T. ) ;
#20810=CARTESIAN_POINT ( 'NONE',  ( -0.02075734969026423599, 5.356774720514425603, -0.08597719988137648983 ) ) ;
#20813=CARTESIAN_POINT ( 'NONE',  ( -53.01255352321339842, 4.132774720514426292, 35.59556822165056644 ) ) ;
#20817=CARTESIAN_POINT ( 'NONE',  ( 6.184520403203634942, 6.376774720514426953, -25.32021290018218451 ) ) ;
#20820=ORIENTED_EDGE ( 'NONE', *, *, #665, .T. ) ;
#20830=ORIENTED_EDGE ( 'NONE', *, *, #34131, .F. ) ;
#20831=ORIENTED_EDGE ( 'NONE', *, *, #23185, .F. ) ;
#20836=DIRECTION ( 'NONE',  ( 0.000000000000000000, 1.000000000000000000, 0.000000000000000000 ) ) ;
#20844=CARTESIAN_POINT ( 'NONE',  ( -20.27875734969026311, -4.543225279485573864, 21.75402280011862644 ) ) ;
#20845=CYLINDRICAL_SURFACE ( 'NONE', #71446, 1.836000000000000743 ) ;
#20861=VERTEX_POINT ( 'NONE', #91234 ) ;
#20868=EDGE_LOOP ( 'NONE', ( #60796, #3785 ) ) ;
#20897=DIRECTION ( 'NONE',  ( 0.000000000000000000, 0.000000000000000000, -1.000000000000000000 ) ) ;
#20925=VECTOR ( 'NONE', #35228, 1000.000000000000000 ) ;
#20928=CIRCLE ( 'NONE', #24418, 2.249999999999998668 ) ;
#20936=ORIENTED_EDGE ( 'NONE', *, *, #27894, .F. ) ;
#20939=ORIENTED_EDGE ( 'NONE', *, *, #18724, .F. ) ;
#20945=DIRECTION ( 'NONE',  ( 0.000000000000000000, 1.000000000000000000, 0.000000000000000000 ) ) ;
#20976=DIRECTION ( 'NONE',  ( -0.000000000000000000, -1.000000000000000000, -0.000000000000000000 ) ) ;
#20979=EDGE_LOOP ( 'NONE', ( #41321, #68396, #86285, #42218, #47435, #72615, #45694, #4285, #24846, #92494, #75487 ) ) ;
#20980=AXIS2_PLACEMENT_3D ( 'NONE', #48914, #11830, #18943 ) ;
#20983=ORIENTED_EDGE ( 'NONE', *, *, #47760, .F. ) ;
#20984=ORIENTED_EDGE ( 'NONE', *, *, #75467, .F. ) ;
#20988=DIRECTION ( 'NONE',  ( 0.000000000000000000, -1.000000000000000000, 0.000000000000000000 ) ) ;
#20997=ORIENTED_EDGE ( 'NONE', *, *, #92733, .T. ) ;
#20999=FACE_OUTER_BOUND ( 'NONE', #19250, .T. ) ;
#21001=VERTEX_POINT ( 'NONE', #14103 ) ;
#21003=CIRCLE ( 'NONE', #97204, 129.7684398600581517 ) ;
#21010=CARTESIAN_POINT ( 'NONE',  ( 32.16024265030974050, -5.965225279485572685, 16.27760796525321751 ) ) ;
#21018=DIRECTION ( 'NONE',  ( 0.000000000000000000, 0.000000000000000000, -1.000000000000000000 ) ) ;
#21022=CARTESIAN_POINT ( 'NONE',  ( 11.25623914429021788, 5.356774720514424715, -27.04805245727492036 ) ) ;
#21034=EDGE_CURVE ( 'NONE', #33683, #74588, #386, .T. ) ;
#21035=EDGE_CURVE ( 'NONE', #25854, #97022, #1187, .T. ) ;
#21054=CARTESIAN_POINT ( 'NONE',  ( 11.62916340711181284, 0.3587747205144265483, 28.75961759920349792 ) ) ;
#21059=EDGE_LOOP ( 'NONE', ( #48443, #5707, #30816, #45453 ) ) ;
#21065=DIRECTION ( 'NONE',  ( -0.000000000000000000, 1.000000000000000000, -0.000000000000000000 ) ) ;
#21069=EDGE_CURVE ( 'NONE', #4176, #60428, #32844, .T. ) ;
#21093=CARTESIAN_POINT ( 'NONE',  ( 0.000000000000000000, -6.943225279485572443, 0.000000000000000000 ) ) ;
#21097=ORIENTED_EDGE ( 'NONE', *, *, #31906, .T. ) ;
#21100=PLANE ( 'NONE',  #1084 ) ;
#21122=EDGE_CURVE ( 'NONE', #71932, #25228, #61172, .T. ) ;
#21123=EDGE_CURVE ( 'NONE', #64548, #24863, #1900, .T. ) ;
#21126=ORIENTED_EDGE ( 'NONE', *, *, #85164, .F. ) ;
#21135=DIRECTION ( 'NONE',  ( 0.000000000000000000, -1.000000000000000000, 0.000000000000000000 ) ) ;
#21137=ADVANCED_FACE ( 'NONE', ( #87634 ), #10499, .F. ) ;
#21154=VECTOR ( 'NONE', #31395, 1000.000000000000000 ) ;
#21170=DIRECTION ( 'NONE',  ( -1.000000000000000000, 0.000000000000000000, 0.000000000000000000 ) ) ;
#21174=ORIENTED_EDGE ( 'NONE', *, *, #87828, .F. ) ;
#21176=CARTESIAN_POINT ( 'NONE',  ( 5.949073730962466833, -6.475225279485573360, -27.94053387008862188 ) ) ;
#21207=ORIENTED_EDGE ( 'NONE', *, *, #94814, .F. ) ;
#21221=DIRECTION ( 'NONE',  ( 0.000000000000000000, 0.000000000000000000, -1.000000000000000000 ) ) ;
#21222=ORIENTED_EDGE ( 'NONE', *, *, #97697, .T. ) ;
#21247=CARTESIAN_POINT ( 'NONE',  ( 5.314386400780318986, 0.3587747205143965723, -28.55951656536880989 ) ) ;
#21253=CARTESIAN_POINT ( 'NONE',  ( 5.097264368844749427, -6.475225279485576024, -27.56135813788841560 ) ) ;
#21257=EDGE_CURVE ( 'NONE', #82699, #33683, #96794, .T. ) ;
#21269=CARTESIAN_POINT ( 'NONE',  ( -29.49875734969026198, 0.3587747205144262708, 0.1180228001186258285 ) ) ;
#21272=DIRECTION ( 'NONE',  ( 0.000000000000000000, 0.000000000000000000, -1.000000000000000000 ) ) ;
#21286=CARTESIAN_POINT ( 'NONE',  ( -28.49194798280534968, 0.3587747205144265483, 28.38521343323375490 ) ) ;
#21312=CARTESIAN_POINT ( 'NONE',  ( 30.54440242517687665, 0.2147811518489142757, 23.45430928465146891 ) ) ;
#21314=AXIS2_PLACEMENT_3D ( 'NONE', #288, #39352, #84024 ) ;
#21337=ORIENTED_EDGE ( 'NONE', *, *, #6609, .F. ) ;
#21343=EDGE_CURVE ( 'NONE', #83129, #11050, #30715, .T. ) ;
#21348=EDGE_CURVE ( 'NONE', #37593, #94215, #30364, .T. ) ;
#21354=EDGE_CURVE ( 'NONE', #17901, #34861, #100013, .T. ) ;
#21358=ORIENTED_EDGE ( 'NONE', *, *, #5776, .T. ) ;
#21362=ORIENTED_EDGE ( 'NONE', *, *, #28364, .T. ) ;
#21374=DIRECTION ( 'NONE',  ( 0.000000000000000000, 0.000000000000000000, -1.000000000000000000 ) ) ;
#21382=DIRECTION ( 'NONE',  ( 1.000000000000000000, -0.000000000000000000, -0.000000000000000000 ) ) ;
#21392=DIRECTION ( 'NONE',  ( 0.000000000000000000, 0.000000000000000000, -1.000000000000000000 ) ) ;
#21397=LINE ( 'NONE', #98527, #90966 ) ;
#21402=EDGE_CURVE ( 'NONE', #72334, #81022, #91687, .T. ) ;
#21403=ORIENTED_EDGE ( 'NONE', *, *, #44768, .F. ) ;
#21404=CARTESIAN_POINT ( 'NONE',  ( -27.96875734969026084, -6.475225279485573360, 0.7300228001186309656 ) ) ;
#21417=CIRCLE ( 'NONE', #356, 3.500000000000000000 ) ;
#21423=CARTESIAN_POINT ( 'NONE',  ( 3.180076745125955284, 6.376774720514426953, -28.87659520466658236 ) ) ;
#21432=CARTESIAN_POINT ( 'NONE',  ( 21.29813515305326632, 4.383221189982441146, -16.78466049732684695 ) ) ;
#21435=LINE ( 'NONE', #91960, #89028 ) ;
#21454=LINE ( 'NONE', #23444, #72952 ) ;
#21465=EDGE_LOOP ( 'NONE', ( #51799, #37599, #68815, #32602, #24064, #43567 ) ) ;
#21466=LINE ( 'NONE', #37217, #80920 ) ;
#21479=CARTESIAN_POINT ( 'NONE',  ( -19.80875734969026425, -5.965225279485572685, 31.02402280011862246 ) ) ;
#21486=DIRECTION ( 'NONE',  ( 0.000000000000000000, -1.000000000000000000, 0.000000000000000000 ) ) ;
#21491=DIRECTION ( 'NONE',  ( 0.000000000000000000, 0.000000000000000000, -1.000000000000000000 ) ) ;
#21496=ORIENTED_EDGE ( 'NONE', *, *, #42343, .T. ) ;
#21509=FACE_OUTER_BOUND ( 'NONE', #83911, .T. ) ;
#21510=AXIS2_PLACEMENT_3D ( 'NONE', #397, #38958, #30345 ) ;
#21512=LINE ( 'NONE', #75306, #57263 ) ;
#21516=ADVANCED_FACE ( 'NONE', ( #57072 ), #64192, .F. ) ;
#21520=ORIENTED_EDGE ( 'NONE', *, *, #100223, .F. ) ;
#21542=B_SPLINE_CURVE_WITH_KNOTS ( 'NONE', 3,
 ( #60033, #75719, #30049, #61025, #21432, #28564, #76222, #37179, #37672, #6220 ),
 .UNSPECIFIED., .F., .F.,
 ( 4, 2, 2, 2, 4 ),
 ( 0.0003558180612557550128, 0.001068662273289818030, 0.001781506485323880885, 0.002494350697357944173, 0.003207194909392007028 ),
 .UNSPECIFIED. ) ;
#21544=DESIGN_CONTEXT ( 'detailed design', #18107, 'design' ) ;
#21575=AXIS2_PLACEMENT_3D ( 'NONE', #25556, #40779, #71741 ) ;
#21581=VERTEX_POINT ( 'NONE', #2780 ) ;
#21584=EDGE_CURVE ( 'NONE', #88881, #62896, #88007, .T. ) ;
#21599=EDGE_CURVE ( 'NONE', #13237, #60950, #25091, .T. ) ;
#21600=VERTEX_POINT ( 'NONE', #80890 ) ;
#21608=CARTESIAN_POINT ( 'NONE',  ( 29.73860345376319358, 1.682774720514426114, 3.721136469884293236E-15 ) ) ;
#21616=VECTOR ( 'NONE', #28009, 1000.000000000000000 ) ;
#21621=AXIS2_PLACEMENT_3D ( 'NONE', #40448, #55182, #63297 ) ;
#21633=DIRECTION ( 'NONE',  ( 8.334928612639484546E-17, 1.000000000000000000, 7.321843366904296032E-17 ) ) ;
#21647=CARTESIAN_POINT ( 'NONE',  ( -32.30247028140506416, -5.965225279485572685, 27.60502002861223048 ) ) ;
#21662=CARTESIAN_POINT ( 'NONE',  ( 7.462166178408539352, -6.475225279485573360, -27.67315496249664974 ) ) ;
#21663=LINE ( 'NONE', #68365, #67004 ) ;
#21667=ADVANCED_FACE ( 'NONE', ( #60062 ), #14352, .F. ) ;
#21671=EDGE_CURVE ( 'NONE', #22324, #35733, #81887, .T. ) ;
#21672=CARTESIAN_POINT ( 'NONE',  ( 11.62916340711181284, 0.3587747205144265483, 28.75961759920349792 ) ) ;
#21674=VECTOR ( 'NONE', #63925, 1000.000000000000000 ) ;
#21676=CARTESIAN_POINT ( 'NONE',  ( 32.68381218857752657, 4.917472161913310380, -3.063707678755810182 ) ) ;
#21682=CIRCLE ( 'NONE', #65488, 1.149999999999998135 ) ;
#21688=B_SPLINE_CURVE_WITH_KNOTS ( 'NONE', 3,
 ( #5431, #83547, #20647, #22136 ),
 .UNSPECIFIED., .F., .F.,
 ( 4, 4 ),
 ( 0.007875538328797549587, 0.009214210883376282302 ),
 .UNSPECIFIED. ) ;
#21714=DIRECTION ( 'NONE',  ( -0.000000000000000000, 1.000000000000000000, -0.000000000000000000 ) ) ;
#21718=CARTESIAN_POINT ( 'NONE',  ( -19.77875734969026311, 5.356774720514425603, 0.7300228001186309656 ) ) ;
#21743=CARTESIAN_POINT ( 'NONE',  ( 5.271800844963591359, 0.3587747205143965168, -28.56638892015329745 ) ) ;
#21746=DIRECTION ( 'NONE',  ( -0.6599726524652352877, 0.000000000000000000, 0.7512896232465889890 ) ) ;
#21755=DIRECTION ( 'NONE',  ( 0.000000000000000000, 1.000000000000000000, 0.000000000000000000 ) ) ;
#21756=CARTESIAN_POINT ( 'NONE',  ( 12.78578435864683449, 3.995361385602315796, -28.02483137475221397 ) ) ;
#21803=ADVANCED_FACE ( 'NONE', ( #31079 ), #77243, .F. ) ;
#21819=AXIS2_PLACEMENT_3D ( 'NONE', #88006, #27609, #58072 ) ;
#21820=ORIENTED_EDGE ( 'NONE', *, *, #62068, .T. ) ;
#21865=LINE ( 'NONE', #6156, #52833 ) ;
#21899=LINE ( 'NONE', #6195, #92137 ) ;
#21918=VECTOR ( 'NONE', #100158, 1000.000000000000000 ) ;
#21922=LINE ( 'NONE', #21423, #41618 ) ;
#21933=FACE_OUTER_BOUND ( 'NONE', #35361, .T. ) ;
#21941=CARTESIAN_POINT ( 'NONE',  ( 15.63775912259811918, 4.567193422985928564, -28.22903731538494299 ) ) ;
#21948=AXIS2_PLACEMENT_3D ( 'NONE', #68443, #29874, #91763 ) ;
#21955=AXIS2_PLACEMENT_3D ( 'NONE', #68386, #52657, #67393 ) ;
#21960=DIRECTION ( 'NONE',  ( 0.000000000000000000, -1.000000000000000000, 0.000000000000000000 ) ) ;
#21972=ORIENTED_EDGE ( 'NONE', *, *, #77043, .F. ) ;
#21981=CARTESIAN_POINT ( 'NONE',  ( 15.97264540888996365, -5.965225279485572685, -27.93485543958161443 ) ) ;
#21987=ORIENTED_EDGE ( 'NONE', *, *, #58412, .T. ) ;
#22003=VERTEX_POINT ( 'NONE', #94988 ) ;
#22006=EDGE_LOOP ( 'NONE', ( #12026, #39312, #67665, #3154 ) ) ;
#22011=EDGE_CURVE ( 'NONE', #97904, #18367, #64073, .T. ) ;
#22032=DIRECTION ( 'NONE',  ( -0.000000000000000000, -1.000000000000000000, 0.000000000000000000 ) ) ;
#22054=CARTESIAN_POINT ( 'NONE',  ( 27.53860345374808105, -1.477225279485574028, -1.352392034746782823 ) ) ;
#22056=ADVANCED_FACE ( 'NONE', ( #87884, #9753 ), #81265, .F. ) ;
#22074=ORIENTED_EDGE ( 'NONE', *, *, #91799, .T. ) ;
#22085=EDGE_CURVE ( 'NONE', #39655, #36906, #80774, .T. ) ;
#22093=ORIENTED_EDGE ( 'NONE', *, *, #28603, .F. ) ;
#22115=ORIENTED_EDGE ( 'NONE', *, *, #93302, .F. ) ;
#22122=DIRECTION ( 'NONE',  ( -0.000000000000000000, 1.000000000000000000, -0.000000000000000000 ) ) ;
#22133=DIRECTION ( 'NONE',  ( -1.000000000000000000, 8.334928612639484546E-17, 0.000000000000000000 ) ) ;
#22136=CARTESIAN_POINT ( 'NONE',  ( 14.43441819135929727, -5.965225279485572685, -28.36222020317710246 ) ) ;
#22140=AXIS2_PLACEMENT_3D ( 'NONE', #52352, #84282, #77163 ) ;
#22152=EDGE_LOOP ( 'NONE', ( #98797, #27094, #28196, #38787 ) ) ;
#22157=CARTESIAN_POINT ( 'NONE',  ( 15.97264540888995299, 3.316774720514426456, -27.93485543958162154 ) ) ;
#22172=CARTESIAN_POINT ( 'NONE',  ( -29.49875734969026198, -5.965225279485572685, 10.11402280011862587 ) ) ;
#22174=AXIS2_PLACEMENT_3D ( 'NONE', #50332, #88389, #42240 ) ;
#22176=VECTOR ( 'NONE', #16625, 1000.000000000000000 ) ;
#22209=DIRECTION ( 'NONE',  ( 0.000000000000000000, 0.000000000000000000, 1.000000000000000000 ) ) ;
#22212=ORIENTED_EDGE ( 'NONE', *, *, #89532, .F. ) ;
#22221=EDGE_CURVE ( 'NONE', #89963, #8495, #62916, .T. ) ;
#22247=CARTESIAN_POINT ( 'NONE',  ( 13.80377080874918150, 3.316774720514426900, -27.21172484903264532 ) ) ;
#22254=CYLINDRICAL_SURFACE ( 'NONE', #69539, 28.96799999999999642 ) ;
#22271=VERTEX_POINT ( 'NONE', #50827 ) ;
#22310=CARTESIAN_POINT ( 'NONE',  ( 10.95759398273795249, 4.132774720514426292, -26.86884997114579932 ) ) ;
#22313=VECTOR ( 'NONE', #71470, 999.9999999999998863 ) ;
#22315=ORIENTED_EDGE ( 'NONE', *, *, #85406, .T. ) ;
#22324=VERTEX_POINT ( 'NONE', #39083 ) ;
#22330=DIRECTION ( 'NONE',  ( 0.000000000000000000, -0.000000000000000000, -1.000000000000000000 ) ) ;
#22345=DIRECTION ( 'NONE',  ( -0.000000000000000000, 0.000000000000000000, 1.000000000000000000 ) ) ;
#22347=VERTEX_POINT ( 'NONE', #22838 ) ;
#22350=ORIENTED_EDGE ( 'NONE', *, *, #67688, .F. ) ;
#22351=EDGE_CURVE ( 'NONE', #23980, #37481, #15747, .T. ) ;
#22365=EDGE_CURVE ( 'NONE', #37863, #82958, #33459, .T. ) ;
#22375=AXIS2_PLACEMENT_3D ( 'NONE', #48040, #75479, #61290 ) ;
#22384=AXIS2_PLACEMENT_3D ( 'NONE', #37043, #45660, #29422 ) ;
#22393=EDGE_CURVE ( 'NONE', #49971, #14697, #94372, .T. ) ;
#22400=ORIENTED_EDGE ( 'NONE', *, *, #6109, .T. ) ;
#22402=LINE ( 'NONE', #53385, #6929 ) ;
#22403=DIRECTION ( 'NONE',  ( 0.000000000000000000, 0.000000000000000000, 1.000000000000000000 ) ) ;
#22404=CARTESIAN_POINT ( 'NONE',  ( 31.79364159983995464, -5.965225279485572685, -11.59305536555894278 ) ) ;
#22423=CARTESIAN_POINT ( 'NONE',  ( 30.09341516180546350, -1.477225279485574028, -11.39311774897855756 ) ) ;
#22449=VERTEX_POINT ( 'NONE', #86263 ) ;
#22450=DIRECTION ( 'NONE',  ( 0.000000000000000000, 1.000000000000000000, -0.000000000000000000 ) ) ;
#22483=ORIENTED_EDGE ( 'NONE', *, *, #38947, .F. ) ;
#22486=CARTESIAN_POINT ( 'NONE',  ( -28.84663072490566194, -5.965225279485572685, 28.73989617533406715 ) ) ;
#22498=LINE ( 'NONE', #53491, #65385 ) ;
#22501=ORIENTED_EDGE ( 'NONE', *, *, #90567, .F. ) ;
#22528=DIRECTION ( 'NONE',  ( 0.000000000000000000, 0.000000000000000000, -1.000000000000000000 ) ) ;
#22534=ADVANCED_FACE ( 'NONE', ( #46534, #37920 ), #94193, .T. ) ;
#22539=ADVANCED_FACE ( 'NONE', ( #86088 ), #62779, .T. ) ;
#22541=VECTOR ( 'NONE', #76688, 1000.000000000000000 ) ;
#22549=ORIENTED_EDGE ( 'NONE', *, *, #2599, .T. ) ;
#22555=CARTESIAN_POINT ( 'NONE',  ( -13.89275734969026388, 0.3587747205144262708, 30.51402280011862089 ) ) ;
#22556=DIRECTION ( 'NONE',  ( 0.000000000000000000, -0.000000000000000000, -1.000000000000000000 ) ) ;
#22561=CARTESIAN_POINT ( 'NONE',  ( 32.66876533700882845, -6.475225279485573360, -12.58926540598385557 ) ) ;
#22563=ORIENTED_EDGE ( 'NONE', *, *, #58382, .F. ) ;
#22566=EDGE_LOOP ( 'NONE', ( #18708, #80365, #36868, #73643 ) ) ;
#22569=AXIS2_PLACEMENT_3D ( 'NONE', #5381, #65809, #96729 ) ;
#22577=CIRCLE ( 'NONE', #71212, 8.452410033082761842 ) ;
#22588=VECTOR ( 'NONE', #61409, 1000.000000000000000 ) ;
#22596=VERTEX_POINT ( 'NONE', #54653 ) ;
#22597=DIRECTION ( 'NONE',  ( -1.000000000000000000, 0.000000000000000000, -0.000000000000000000 ) ) ;
#22609=ADVANCED_FACE ( 'NONE', ( #8965 ), #16068, .T. ) ;
#22611=VERTEX_POINT ( 'NONE', #16567 ) ;
#22614=VERTEX_POINT ( 'NONE', #38916 ) ;
#22625=ORIENTED_EDGE ( 'NONE', *, *, #78404, .F. ) ;
#22627=CARTESIAN_POINT ( 'NONE',  ( -24.90875734969025501, 6.376774720514426953, 27.45402280011862572 ) ) ;
#22629=PLANE ( 'NONE',  #24684 ) ;
#22648=VERTEX_POINT ( 'NONE', #76964 ) ;
#22660=AXIS2_PLACEMENT_3D ( 'NONE', #20810, #98939, #76096 ) ;
#22664=CARTESIAN_POINT ( 'NONE',  ( 30.61643171304413613, 3.478988201194511909, 27.37433008668280365 ) ) ;
#22675=CARTESIAN_POINT ( 'NONE',  ( 30.53060340732035982, -6.475225279485573360, 20.86760796525322093 ) ) ;
#22676=CARTESIAN_POINT ( 'NONE',  ( 32.54161589056530346, 4.044086941844335925, -1.517980283019001453 ) ) ;
#22683=PLANE ( 'NONE',  #73852 ) ;
#22705=DIRECTION ( 'NONE',  ( -0.000000000000000000, 1.000000000000000000, -0.000000000000000000 ) ) ;
#22708=VERTEX_POINT ( 'NONE', #98053 ) ;
#22755=CARTESIAN_POINT ( 'NONE',  ( 30.53060340732035982, 4.905668307171742626, 14.33114642260468585 ) ) ;
#22769=VERTEX_POINT ( 'NONE', #12322 ) ;
#22773=DIRECTION ( 'NONE',  ( -0.000000000000000000, -0.000000000000000000, -1.000000000000000000 ) ) ;
#22782=VECTOR ( 'NONE', #41861, 1000.000000000000000 ) ;
#22792=FACE_OUTER_BOUND ( 'NONE', #7862, .T. ) ;
#22796=CIRCLE ( 'NONE', #53622, 2.499999999999998668 ) ;
#22800=CARTESIAN_POINT ( 'NONE',  ( 0.000000000000000000, 4.132774720514426292, 0.000000000000000000 ) ) ;
#22806=ADVANCED_FACE ( 'NONE', ( #20429 ), #71014, .F. ) ;
#22807=CARTESIAN_POINT ( 'NONE',  ( -28.98875734969026041, 0.3587747205144265483, 25.61802280011862720 ) ) ;
#22821=ORIENTED_EDGE ( 'NONE', *, *, #21584, .T. ) ;
#22832=EDGE_CURVE ( 'NONE', #4626, #22347, #9014, .T. ) ;
#22833=CARTESIAN_POINT ( 'NONE',  ( 32.88562546571908740, 6.376774720514426953, -5.083907541707153754 ) ) ;
#22838=CARTESIAN_POINT ( 'NONE',  ( 20.57455539870835537, 4.132774720514415634, -18.22080502500613974 ) ) ;
#22851=EDGE_CURVE ( 'NONE', #82017, #67705, #45062, .T. ) ;
#22859=EDGE_LOOP ( 'NONE', ( #48601, #61946, #89391, #52412 ) ) ;
#22864=DIRECTION ( 'NONE',  ( 0.000000000000000000, 0.000000000000000000, 1.000000000000000000 ) ) ;
#22865=VECTOR ( 'NONE', #59870, 1000.000000000000114 ) ;
#22885=ORIENTED_EDGE ( 'NONE', *, *, #91593, .T. ) ;
#22886=CARTESIAN_POINT ( 'NONE',  ( 6.783277368979140576, 6.376774720515100192, -28.31678455572487252 ) ) ;
#22891=ORIENTED_EDGE ( 'NONE', *, *, #60573, .T. ) ;
#22897=FACE_OUTER_BOUND ( 'NONE', #89160, .T. ) ;
#22903=FACE_OUTER_BOUND ( 'NONE', #39313, .T. ) ;
#22906=DIRECTION ( 'NONE',  ( 1.000000000000000000, -0.000000000000000000, -0.000000000000000000 ) ) ;
#22916=CARTESIAN_POINT ( 'NONE',  ( -0.02075734969026423599, -6.475225279485573360, -28.54397719988136828 ) ) ;
#22917=ADVANCED_FACE ( 'NONE', ( #47060 ), #79993, .T. ) ;
#22933=CARTESIAN_POINT ( 'NONE',  ( 16.15056352287345476, 3.622774720514426949, -27.77856273171767398 ) ) ;
#22935=CARTESIAN_POINT ( 'NONE',  ( 22.33191539159816585, 3.407774720514426647, -16.26852658953824360 ) ) ;
#22938=DIRECTION ( 'NONE',  ( 0.2488812114211666759, 0.000000000000000000, 0.9685340172660599212 ) ) ;
#22947=ADVANCED_FACE ( 'NONE', ( #12480 ), #43448, .T. ) ;
#22951=CARTESIAN_POINT ( 'NONE',  ( 27.86270917940689174, 6.376774720514426953, 29.02104833056109001 ) ) ;
#22955=ORIENTED_EDGE ( 'NONE', *, *, #31456, .T. ) ;
#22960=ORIENTED_EDGE ( 'NONE', *, *, #85156, .T. ) ;
#22977=VERTEX_POINT ( 'NONE', #58172 ) ;
#22978=CARTESIAN_POINT ( 'NONE',  ( 25.43734433117264615, 5.179209770121858902, -8.122553904655967827 ) ) ;
#23015=DIRECTION ( 'NONE',  ( 0.000000000000000000, 0.000000000000000000, 1.000000000000000000 ) ) ;
#23034=B_SPLINE_CURVE_WITH_KNOTS ( 'NONE', 3,
 ( #37541, #68491, #35800, #1988, #32427, #63907, #33930, #72003 ),
 .UNSPECIFIED., .F., .F.,
 ( 4, 2, 2, 4 ),
 ( 0.003348119353445774479, 0.004405762884006169181, 0.005463406414566563882, 0.007578693475687353284 ),
 .UNSPECIFIED. ) ;
#23039=EDGE_CURVE ( 'NONE', #32574, #50853, #91099, .T. ) ;
#23041=DIRECTION ( 'NONE',  ( -0.000000000000000000, 1.000000000000000000, -0.000000000000000000 ) ) ;
#23080=CARTESIAN_POINT ( 'NONE',  ( -10.37843575862113887, 5.356774720514426491, 27.71903885537846435 ) ) ;
#23096=VECTOR ( 'NONE', #25151, 1000.000000000000000 ) ;
#23125=ORIENTED_EDGE ( 'NONE', *, *, #79879, .T. ) ;
#23129=FACE_OUTER_BOUND ( 'NONE', #56042, .T. ) ;
#23131=CARTESIAN_POINT ( 'NONE',  ( 15.14080536460164517, 5.152774720514427642, -26.62908960815038384 ) ) ;
#23134=PLANE ( 'NONE',  #73348 ) ;
#23139=PLANE ( 'NONE',  #77918 ) ;
#23149=ORIENTED_EDGE ( 'NONE', *, *, #87032, .F. ) ;
#23163=CARTESIAN_POINT ( 'NONE',  ( 30.61558314414154580, 3.638221654638376990, 27.34201279177319321 ) ) ;
#23176=EDGE_CURVE ( 'NONE', #83405, #79593, #5739, .T. ) ;
#23185=EDGE_CURVE ( 'NONE', #55229, #68279, #39777, .T. ) ;
#23222=LINE ( 'NONE', #21718, #97725 ) ;
#23225=ORIENTED_EDGE ( 'NONE', *, *, #23244, .F. ) ;
#23226=EDGE_LOOP ( 'NONE', ( #70016, #95979, #67933, #13168 ) ) ;
#23231=CARTESIAN_POINT ( 'NONE',  ( 13.91401389203221406, 3.316774720514426456, 158.0376437107427137 ) ) ;
#23244=EDGE_CURVE ( 'NONE', #69079, #74508, #70261, .T. ) ;
#23258=CARTESIAN_POINT ( 'NONE',  ( 13.35520464978777788, 3.511397109468809674, -28.20545335007043164 ) ) ;
#23260=DIRECTION ( 'NONE',  ( -0.000000000000000000, -1.000000000000000000, -0.000000000000000000 ) ) ;
#23264=DIRECTION ( 'NONE',  ( -0.1875268396392987258, -0.000000000000000000, -0.9822594791677485837 ) ) ;
#23286=AXIS2_PLACEMENT_3D ( 'NONE', #32829, #64304, #1883 ) ;
#23294=EDGE_CURVE ( 'NONE', #96621, #27652, #70765, .T. ) ;
#23308=EDGE_CURVE ( 'NONE', #62785, #61654, #57999, .T. ) ;
#23314=DIRECTION ( 'NONE',  ( 0.9980236263794188822, 0.000000000000000000, -0.06283980576413539243 ) ) ;
#23324=DIRECTION ( 'NONE',  ( 6.030048488936326810E-14, 0.000000000000000000, -1.000000000000000000 ) ) ;
#23333=CARTESIAN_POINT ( 'NONE',  ( -65.05438548721849656, 5.356774720514425603, 24.50402280011859091 ) ) ;
#23347=EDGE_CURVE ( 'NONE', #57513, #33445, #48934, .T. ) ;
#23349=PLANE ( 'NONE',  #45281 ) ;
#23364=VERTEX_POINT ( 'NONE', #42825 ) ;
#23380=ORIENTED_EDGE ( 'NONE', *, *, #39012, .T. ) ;
#23391=CARTESIAN_POINT ( 'NONE',  ( 8.616046215355789073, 6.376774720514426065, -25.03514012577542758 ) ) ;
#23392=VECTOR ( 'NONE', #45655, 1000.000000000000000 ) ;
#23412=CARTESIAN_POINT ( 'NONE',  ( 29.73860345376319358, 5.356653621633795659, 18.57591161935199153 ) ) ;
#23413=CARTESIAN_POINT ( 'NONE',  ( 32.53135143123563466, 0.3587747205144265483, 6.926385399448451885 ) ) ;
#23429=VECTOR ( 'NONE', #87699, 1000.000000000000000 ) ;
#23435=LINE ( 'NONE', #93461, #49316 ) ;
#23436=EDGE_LOOP ( 'NONE', ( #84410, #90331, #75992, #56922 ) ) ;
#23444=CARTESIAN_POINT ( 'NONE',  ( -27.61845239340658154, -5.965225279485594001, -10.37513603161905351 ) ) ;
#23452=DIRECTION ( 'NONE',  ( -0.9952638024365005887, 0.000000000000000000, -0.09721092304694053943 ) ) ;
#23456=ORIENTED_EDGE ( 'NONE', *, *, #45420, .T. ) ;
#23462=EDGE_LOOP ( 'NONE', ( #13677, #8859, #6994, #57675 ) ) ;
#23463=VECTOR ( 'NONE', #15208, 1000.000000000000000 ) ;
#23469=VERTEX_POINT ( 'NONE', #14334 ) ;
#23480=ORIENTED_EDGE ( 'NONE', *, *, #95490, .T. ) ;
#23508=FACE_BOUND ( 'NONE', #40067, .T. ) ;
#23532=DIRECTION ( 'NONE',  ( 2.313651251573820309E-16, -1.000000000000000000, 8.068660792749117443E-16 ) ) ;
#23552=CIRCLE ( 'NONE', #59221, 28.96799999999999287 ) ;
#23554=ORIENTED_EDGE ( 'NONE', *, *, #42120, .T. ) ;
#23569=DIRECTION ( 'NONE',  ( -0.000000000000000000, -1.000000000000000000, 0.000000000000000000 ) ) ;
#23574=EDGE_LOOP ( 'NONE', ( #64434, #85695 ) ) ;
#23592=VECTOR ( 'NONE', #23041, 1000.000000000000000 ) ;
#23597=VERTEX_POINT ( 'NONE', #3023 ) ;
#23605=LINE ( 'NONE', #282, #3229 ) ;
#23612=EDGE_LOOP ( 'NONE', ( #39454, #99369, #22821, #67410 ) ) ;
#23627=VECTOR ( 'NONE', #96336, 1000.000000000000000 ) ;
#23630=DIRECTION ( 'NONE',  ( 1.286817348990133408E-16, 0.000000000000000000, -1.000000000000000000 ) ) ;
#23635=DIRECTION ( 'NONE',  ( 0.000000000000000000, -0.000000000000000000, -1.000000000000000000 ) ) ;
#23638=CARTESIAN_POINT ( 'NONE',  ( 5.085443162053245203, 3.316774720514426456, -27.56355752155217331 ) ) ;
#23644=LINE ( 'NONE', #71341, #62540 ) ;
#23647=LINE ( 'NONE', #38381, #89325 ) ;
#23654=CARTESIAN_POINT ( 'NONE',  ( 19.72776355195876619, 6.376774720514426953, 28.39950002376592764 ) ) ;
#23656=LINE ( 'NONE', #94174, #65128 ) ;
#23691=VERTEX_POINT ( 'NONE', #97844 ) ;
#23696=DIRECTION ( 'NONE',  ( 0.000000000000000000, -1.000000000000000000, -0.000000000000000000 ) ) ;
#23698=DIRECTION ( 'NONE',  ( 0.000000000000000000, -0.000000000000000000, 1.000000000000000000 ) ) ;
#23700=EDGE_LOOP ( 'NONE', ( #26979, #59168, #99518, #69319, #83363 ) ) ;
#23703=VERTEX_POINT ( 'NONE', #57814 ) ;
#23704=VECTOR ( 'NONE', #94852, 1000.000000000000000 ) ;
#23706=VERTEX_POINT ( 'NONE', #5502 ) ;
#23707=VECTOR ( 'NONE', #9371, 1000.000000000000000 ) ;
#23715=ORIENTED_EDGE ( 'NONE', *, *, #47259, .F. ) ;
#23733=ORIENTED_EDGE ( 'NONE', *, *, #33286, .T. ) ;
#23735=LINE ( 'NONE', #55716, #89926 ) ;
#23740=CARTESIAN_POINT ( 'NONE',  ( 33.69795529655567634, -5.515143950957555496, 14.99689261510125249 ) ) ;
#23774=CARTESIAN_POINT ( 'NONE',  ( 30.53060340732035982, 2.682774720514426559, 19.84760796525321780 ) ) ;
#23795=ORIENTED_EDGE ( 'NONE', *, *, #23294, .F. ) ;
#23798=DIRECTION ( 'NONE',  ( 2.327730190238734579E-16, 1.000000000000000000, -8.064610422320895277E-16 ) ) ;
#23802=CARTESIAN_POINT ( 'NONE',  ( 13.91401389203221406, -6.475225279485573360, 158.0376437107427137 ) ) ;
#23815=ORIENTED_EDGE ( 'NONE', *, *, #5552, .F. ) ;
#23816=DIRECTION ( 'NONE',  ( -0.000000000000000000, 1.000000000000000000, -0.000000000000000000 ) ) ;
#23819=AXIS2_PLACEMENT_3D ( 'NONE', #26522, #57486, #65605 ) ;
#23821=EDGE_CURVE ( 'NONE', #42999, #63531, #90240, .T. ) ;
#23831=VECTOR ( 'NONE', #62972, 1000.000000000000000 ) ;
#23842=VERTEX_POINT ( 'NONE', #36953 ) ;
#23847=VECTOR ( 'NONE', #75039, 1000.000000000000114 ) ;
#23874=CARTESIAN_POINT ( 'NONE',  ( 22.81105451610979173, 500000.0000000000582, -16.21691820600746681 ) ) ;
#23889=DIRECTION ( 'NONE',  ( 0.000000000000000000, 1.000000000000000000, 0.000000000000000000 ) ) ;
#23892=B_SPLINE_CURVE_WITH_KNOTS ( 'NONE', 3,
 ( #9846, #11356, #41307, #1745, #34697, #40307, #63663, #10351, #88486, #26075, #72267, #71761, #10858, #72767, #3262, #48425 ),
 .UNSPECIFIED., .F., .F.,
 ( 4, 2, 2, 2, 2, 2, 2, 4 ),
 ( -2.611475609838436325E-05, 0.001181507984664241897, 0.001785319355045555511, 0.002389130725426869776, 0.002992942095808183173, 0.003596753466189497005, 0.004200564836570811270, 0.004804376206952124667 ),
 .UNSPECIFIED. ) ;
#23896=DIRECTION ( 'NONE',  ( 0.6599726524652347326, 0.000000000000000000, -0.7512896232465895441 ) ) ;
#23911=CARTESIAN_POINT ( 'NONE',  ( 6.055070916906798217, 3.316774720512750019, -28.43998667593618990 ) ) ;
#23912=VECTOR ( 'NONE', #85119, 1000.000000000000000 ) ;
#23915=CARTESIAN_POINT ( 'NONE',  ( 5.471383689419962337, -5.965225279485594001, -29.02273493113403902 ) ) ;
#23928=VERTEX_POINT ( 'NONE', #91236 ) ;
#23933=DIRECTION ( 'NONE',  ( 1.251281512149627050E-16, 0.000000000000000000, -1.000000000000000000 ) ) ;
#23958=EDGE_LOOP ( 'NONE', ( #77385, #4302, #77578, #90133 ) ) ;
#23980=VERTEX_POINT ( 'NONE', #7003 ) ;
#24000=TOROIDAL_SURFACE ( 'NONE', #9453, 3.060000000000000053, 2.040000000000000036 ) ;
#24007=EDGE_CURVE ( 'NONE', #48956, #58117, #77498, .T. ) ;
#24010=DIRECTION ( 'NONE',  ( -0.4009304992412300317, -6.845827386180410961E-16, -0.9161084732596779245 ) ) ;
#24063=ORIENTED_EDGE ( 'NONE', *, *, #69313, .F. ) ;
#24064=ORIENTED_EDGE ( 'NONE', *, *, #9242, .F. ) ;
#24080=CARTESIAN_POINT ( 'NONE',  ( 26.73860345374794178, 5.356774720496559894, 19.84760796525321780 ) ) ;
#24098=EDGE_LOOP ( 'NONE', ( #17501, #16347, #67797, #505, #47329, #48228, #21222, #93094, #11228, #4886, #4110, #65430, #75382, #899, #64412, #23715, #74323, #38940, #21174, #40933 ) ) ;
#24120=ORIENTED_EDGE ( 'NONE', *, *, #94579, .F. ) ;
#24125=AXIS2_PLACEMENT_3D ( 'NONE', #54025, #47401, #70737 ) ;
#24140=VERTEX_POINT ( 'NONE', #56200 ) ;
#24141=DIRECTION ( 'NONE',  ( 0.000000000000000000, 0.000000000000000000, -1.000000000000000000 ) ) ;
#24148=DIRECTION ( 'NONE',  ( 0.6599726524652352877, -0.000000000000000000, -0.7512896232465891000 ) ) ;
#24153=CARTESIAN_POINT ( 'NONE',  ( -29.49875734969025842, 0.3587747205144262708, 15.62202280011862321 ) ) ;
#24163=CARTESIAN_POINT ( 'NONE',  ( -0.02075734969026423599, -5.965225279485572685, -0.08597719988137648983 ) ) ;
#24168=CARTESIAN_POINT ( 'NONE',  ( 15.99960863614631101, 3.577630190450212577, -27.91116951066581819 ) ) ;
#24187=LINE ( 'NONE', #7458, #11107 ) ;
#24203=EDGE_CURVE ( 'NONE', #5126, #38206, #4353, .T. ) ;
#24208=CARTESIAN_POINT ( 'NONE',  ( 5.271800844963591359, 6.376774720514426953, -28.56638892015329745 ) ) ;
#24210=EDGE_LOOP ( 'NONE', ( #8945, #39371 ) ) ;
#24239=ORIENTED_EDGE ( 'NONE', *, *, #9502, .F. ) ;
#24257=CYLINDRICAL_SURFACE ( 'NONE', #76508, 2.499999999999998668 ) ;
#24258=VERTEX_POINT ( 'NONE', #99219 ) ;
#24265=DIRECTION ( 'NONE',  ( -0.6392559695863496705, 0.000000000000000000, -0.7689940216596069522 ) ) ;
#24270=CARTESIAN_POINT ( 'NONE',  ( 5.271800844830267785, 3.316774720514427344, -28.56638892017480913 ) ) ;
#24278=ADVANCED_FACE ( 'NONE', ( #13489 ), #21100, .T. ) ;
#24295=ORIENTED_EDGE ( 'NONE', *, *, #35385, .F. ) ;
#24296=CARTESIAN_POINT ( 'NONE',  ( -11.64875734969026233, -5.965225279485572685, 31.02402280011862246 ) ) ;
#24307=VERTEX_POINT ( 'NONE', #84998 ) ;
#24315=ORIENTED_EDGE ( 'NONE', *, *, #79919, .F. ) ;
#24327=DIRECTION ( 'NONE',  ( -0.7071067811865474617, 0.000000000000000000, -0.7071067811865476838 ) ) ;
#24331=AXIS2_PLACEMENT_3D ( 'NONE', #38688, #22450, #76244 ) ;
#24351=VERTEX_POINT ( 'NONE', #93107 ) ;
#24354=EDGE_LOOP ( 'NONE', ( #65632, #6672, #91876, #44693, #38808, #82771 ) ) ;
#24367=CARTESIAN_POINT ( 'NONE',  ( -29.49875734969025842, 0.3587747205144265483, 25.61802280011862720 ) ) ;
#24387=EDGE_CURVE ( 'NONE', #49834, #95734, #62685, .T. ) ;
#24404=CARTESIAN_POINT ( 'NONE',  ( 32.16024265030974050, -5.965225279485572685, 14.03360796525321774 ) ) ;
#24405=B_SPLINE_CURVE_WITH_KNOTS ( 'NONE', 3,
 ( #85725, #92827, #76097, #7597 ),
 .UNSPECIFIED., .F., .F.,
 ( 4, 4 ),
 ( 0.000000000000000000, 1.000000000000000000 ),
 .UNSPECIFIED. ) ;
#24417=CARTESIAN_POINT ( 'NONE',  ( 10.16119454606143435, 6.376774720514261752, -28.04611093484508899 ) ) ;
#24418=AXIS2_PLACEMENT_3D ( 'NONE', #54908, #94462, #71133 ) ;
#24423=CARTESIAN_POINT ( 'NONE',  ( -24.90875734969025501, -5.965225279485572685, 26.43402280011862615 ) ) ;
#24441=EDGE_CURVE ( 'NONE', #93762, #20861, #1280, .T. ) ;
#24444=CARTESIAN_POINT ( 'NONE',  ( 31.63587494018430135, 3.477878053198200536, 27.33969830395653844 ) ) ;
#24460=DIRECTION ( 'NONE',  ( -1.000000000000000000, 9.637352644315600173E-17, 0.000000000000000000 ) ) ;
#24464=ORIENTED_EDGE ( 'NONE', *, *, #94814, .T. ) ;
#24466=ORIENTED_EDGE ( 'NONE', *, *, #36971, .T. ) ;
#24480=CIRCLE ( 'NONE', #60146, 1.149999999999998135 ) ;
#24484=DIRECTION ( 'NONE',  ( -0.1254312216594016538, -0.000000000000000000, -0.9921023176230513441 ) ) ;
#24499=EDGE_LOOP ( 'NONE', ( #54364, #16271, #3231, #90270 ) ) ;
#24561=DIRECTION ( 'NONE',  ( -0.1311553622875919756, -6.845827386180409975E-16, -0.9913618264504692190 ) ) ;
#24582=B_SPLINE_CURVE_WITH_KNOTS ( 'NONE', 3,
 ( #59383, #43661, #57902, #27439, #36038, #58397, #90325, #20798, #82708, #44157 ),
 .UNSPECIFIED., .F., .F.,
 ( 4, 2, 2, 2, 4 ),
 ( 0.000000000000000000, 0.0004823517777971119314, 0.0009647035555942238627, 0.001447055333391335848, 0.001929407111188447725 ),
 .UNSPECIFIED. ) ;
#24585=FACE_OUTER_BOUND ( 'NONE', #30022, .T. ) ;
#24587=EDGE_CURVE ( 'NONE', #44056, #88744, #99917, .T. ) ;
#24600=ORIENTED_EDGE ( 'NONE', *, *, #83561, .F. ) ;
#24625=CYLINDRICAL_SURFACE ( 'NONE', #2758, 130.7884398600581335 ) ;
#24638=FACE_OUTER_BOUND ( 'NONE', #81648, .T. ) ;
#24642=ORIENTED_EDGE ( 'NONE', *, *, #63607, .T. ) ;
#24645=CARTESIAN_POINT ( 'NONE',  ( -53.01255352321339842, -1.477225279485574028, 35.59556822165056644 ) ) ;
#24657=PLANE ( 'NONE',  #58726 ) ;
#24679=DIRECTION ( 'NONE',  ( 0.000000000000000000, -1.000000000000000000, 0.000000000000000000 ) ) ;
#24683=VERTEX_POINT ( 'NONE', #51944 ) ;
#24684=AXIS2_PLACEMENT_3D ( 'NONE', #54118, #85038, #78424 ) ;
#24701=ORIENTED_EDGE ( 'NONE', *, *, #78652, .F. ) ;
#24716=CARTESIAN_POINT ( 'NONE',  ( 29.70566059910618861, 3.975162330554212531, 28.10075438475601928 ) ) ;
#24721=EDGE_LOOP ( 'NONE', ( #57330, #55034, #242, #66702 ) ) ;
#24758=CARTESIAN_POINT ( 'NONE',  ( 27.53860345374808105, 3.356774720514427379, 1.647607965253217621 ) ) ;
#24797=CARTESIAN_POINT ( 'NONE',  ( -29.49875734969025842, 0.3587747205144265483, 25.61802280011862720 ) ) ;
#24801=CARTESIAN_POINT ( 'NONE',  ( 33.41263754283357912, 3.496799131921995762, -12.47286811689047070 ) ) ;
#24821=DIRECTION ( 'NONE',  ( -0.2488812114211667037, -0.000000000000000000, -0.9685340172660599212 ) ) ;
#24835=DIRECTION ( 'NONE',  ( 1.000000000000000000, 0.000000000000000000, 0.000000000000000000 ) ) ;
#24841=VERTEX_POINT ( 'NONE', #97491 ) ;
#24846=ORIENTED_EDGE ( 'NONE', *, *, #30956, .F. ) ;
#24854=DIRECTION ( 'NONE',  ( 1.000000000000000000, 0.000000000000000000, 0.000000000000000000 ) ) ;
#24863=VERTEX_POINT ( 'NONE', #79763 ) ;
#24866=CARTESIAN_POINT ( 'NONE',  ( -29.49875734969026198, 0.3587747205144265483, 2.362022800118626531 ) ) ;
#24875=FACE_OUTER_BOUND ( 'NONE', #24957, .T. ) ;
#24894=EDGE_CURVE ( 'NONE', #15218, #98626, #57955, .T. ) ;
#24897=EDGE_CURVE ( 'NONE', #80644, #33824, #81270, .T. ) ;
#24910=FACE_OUTER_BOUND ( 'NONE', #59213, .T. ) ;
#24919=CARTESIAN_POINT ( 'NONE',  ( 26.73860345374794178, -1.477225279485574028, 19.84760796525321780 ) ) ;
#24923=AXIS2_PLACEMENT_3D ( 'NONE', #3955, #2964, #33896 ) ;
#24938=CARTESIAN_POINT ( 'NONE',  ( -27.15721599100127648, 0.3587747205144061757, -10.22292133548836723 ) ) ;
#24943=AXIS2_PLACEMENT_3D ( 'NONE', #74134, #3632, #57929 ) ;
#24948=FACE_OUTER_BOUND ( 'NONE', #82882, .T. ) ;
#24957=EDGE_LOOP ( 'NONE', ( #80030, #2189, #95079, #10732 ) ) ;
#24963=ORIENTED_EDGE ( 'NONE', *, *, #57246, .T. ) ;
#24977=FACE_OUTER_BOUND ( 'NONE', #50314, .T. ) ;
#24998=VERTEX_POINT ( 'NONE', #3168 ) ;
#25005=CARTESIAN_POINT ( 'NONE',  ( 10.46399479596398052, 3.316774720514422903, -27.03001098546561209 ) ) ;
#25031=CARTESIAN_POINT ( 'NONE',  ( 30.54125281784916268, 0.6647747205144264315, 23.11160796525322070 ) ) ;
#25085=LINE ( 'NONE', #72283, #13017 ) ;
#25088=CIRCLE ( 'NONE', #81815, 28.45799999999999486 ) ;
#25091=LINE ( 'NONE', #80391, #33702 ) ;
#25097=CARTESIAN_POINT ( 'NONE',  ( 22.81105451610979173, 1.682774720514426114, -18.46691820600746681 ) ) ;
#25103=EDGE_LOOP ( 'NONE', ( #83362, #2233, #29512, #1262, #40235, #36696, #44638, #3742, #52030, #57453, #29138, #36867, #44598, #91313, #52391, #41182, #66960, #80024, #67666, #90642, #37959, #7740, #26360, #94768 ) ) ;
#25118=DIRECTION ( 'NONE',  ( -0.000000000000000000, -1.000000000000000000, -0.000000000000000000 ) ) ;
#25130=EDGE_CURVE ( 'NONE', #84112, #34210, #36790, .T. ) ;
#25139=CARTESIAN_POINT ( 'NONE',  ( 31.62300803125484094, 5.234178280976530928, -3.660617518925037395 ) ) ;
#25140=EDGE_CURVE ( 'NONE', #82652, #95350, #99967, .T. ) ;
#25149=EDGE_CURVE ( 'NONE', #84636, #85130, #7643, .T. ) ;
#25151=DIRECTION ( 'NONE',  ( -0.000000000000000000, -1.000000000000000000, -0.000000000000000000 ) ) ;
#25164=DIRECTION ( 'NONE',  ( 0.000000000000000000, -1.000000000000000000, 0.000000000000000000 ) ) ;
#25172=LINE ( 'NONE', #90445, #3014 ) ;
#25186=DIRECTION ( 'NONE',  ( 0.000000000000000000, 1.000000000000000000, 0.000000000000000000 ) ) ;
#25192=DIRECTION ( 'NONE',  ( 0.000000000000000000, 1.000000000000000000, -0.000000000000000000 ) ) ;
#25219=ORIENTED_EDGE ( 'NONE', *, *, #48552, .T. ) ;
#25228=VERTEX_POINT ( 'NONE', #25365 ) ;
#25239=VECTOR ( 'NONE', #70430, 1000.000000000000000 ) ;
#25252=ORIENTED_EDGE ( 'NONE', *, *, #82765, .T. ) ;
#25254=DIRECTION ( 'NONE',  ( -0.000000000000000000, 1.000000000000000000, 0.000000000000000000 ) ) ;
#25267=FACE_OUTER_BOUND ( 'NONE', #49707, .T. ) ;
#25275=LINE ( 'NONE', #86677, #75775 ) ;
#25279=CARTESIAN_POINT ( 'NONE',  ( 30.32108885906865936, 6.376774720514426953, 3.274824222184972822 ) ) ;
#25306=CARTESIAN_POINT ( 'NONE',  ( 33.57588617459661151, 3.431642488465076912, -12.05779067269562255 ) ) ;
#25310=CIRCLE ( 'NONE', #82034, 1.149999999999998135 ) ;
#25314=EDGE_LOOP ( 'NONE', ( #15139, #88715, #32927, #56188 ) ) ;
#25333=ORIENTED_EDGE ( 'NONE', *, *, #82139, .T. ) ;
#25344=EDGE_LOOP ( 'NONE', ( #99719, #69659, #54603, #73911 ) ) ;
#25365=CARTESIAN_POINT ( 'NONE',  ( 31.55236408230781819, -5.965225279485572685, 19.84760796525321780 ) ) ;
#25373=AXIS2_PLACEMENT_3D ( 'NONE', #4618, #11709, #49805 ) ;
#25377=FACE_OUTER_BOUND ( 'NONE', #70024, .T. ) ;
#25391=AXIS2_PLACEMENT_3D ( 'NONE', #10791, #27520, #74189 ) ;
#25409=FACE_BOUND ( 'NONE', #74733, .T. ) ;
#25410=DIRECTION ( 'NONE',  ( -1.334402673828313586E-16, 0.000000000000000000, 1.000000000000000000 ) ) ;
#25416=CARTESIAN_POINT ( 'NONE',  ( 5.109298100548420152, 3.316774720514426456, -27.55941679637948383 ) ) ;
#25444=CARTESIAN_POINT ( 'NONE',  ( 15.37486457892693181, 3.577890193782808037, -28.28298033016838886 ) ) ;
#25454=CARTESIAN_POINT ( 'NONE',  ( -2.449489742783178770, -16.94322527948557422, 2.499999999999999556 ) ) ;
#25475=DIRECTION ( 'NONE',  ( -0.000000000000000000, -0.000000000000000000, -1.000000000000000000 ) ) ;
#25476=AXIS2_PLACEMENT_3D ( 'NONE', #39717, #87399, #62573 ) ;
#25482=PLANE ( 'NONE',  #22174 ) ;
#25484=CARTESIAN_POINT ( 'NONE',  ( -41.32836283488544638, -2.803225279485573207, 39.26872235229541985 ) ) ;
#25489=ORIENTED_EDGE ( 'NONE', *, *, #60319, .T. ) ;
#25491=EDGE_LOOP ( 'NONE', ( #98125, #49992, #1724, #28686 ) ) ;
#25506=CARTESIAN_POINT ( 'NONE',  ( 27.53860345374771867, 2.682774720514426559, -9.482392034746240483 ) ) ;
#25510=AXIS2_PLACEMENT_3D ( 'NONE', #70581, #17291, #15784 ) ;
#25514=LINE ( 'NONE', #8790, #42684 ) ;
#25520=CARTESIAN_POINT ( 'NONE',  ( 29.73860345376320424, 4.772779586519632744, -4.021226786694506394 ) ) ;
#25529=DIRECTION ( 'NONE',  ( 1.000000000000000000, -2.464095846557964090E-17, 0.000000000000000000 ) ) ;
#25536=CARTESIAN_POINT ( 'NONE',  ( 5.265981236333619456E-16, -1.473225279485573802, -4.300000000000000711 ) ) ;
#25556=CARTESIAN_POINT ( 'NONE',  ( -20.27875734969026311, 3.456774720514426136, 24.00402280011862288 ) ) ;
#25558=CARTESIAN_POINT ( 'NONE',  ( -6.741682653110981249, -5.965225279485572685, 30.62569541381301619 ) ) ;
#25571=CIRCLE ( 'NONE', #9418, 3.349999999999998757 ) ;
#25577=CARTESIAN_POINT ( 'NONE',  ( 15.58962545129234911, 1.684774720514426560, -26.91365498785467025 ) ) ;
#25597=DIRECTION ( 'NONE',  ( 0.000000000000000000, 1.000000000000000000, 0.000000000000000000 ) ) ;
#25601=PLANE ( 'NONE',  #59151 ) ;
#25602=DIRECTION ( 'NONE',  ( -0.000000000000000000, -1.000000000000000000, -0.000000000000000000 ) ) ;
#25611=DIRECTION ( 'NONE',  ( 0.000000000000000000, -0.000000000000000000, -1.000000000000000000 ) ) ;
#25616=ORIENTED_EDGE ( 'NONE', *, *, #65667, .T. ) ;
#25650=VECTOR ( 'NONE', #1092, 1000.000000000000114 ) ;
#25657=CARTESIAN_POINT ( 'NONE',  ( 5.184553252003285984, -5.965225279485572685, -28.06387035751381731 ) ) ;
#25669=AXIS2_PLACEMENT_3D ( 'NONE', #60895, #84707, #90330 ) ;
#25670=DIRECTION ( 'NONE',  ( 0.000000000000000000, -1.000000000000000000, 0.000000000000000000 ) ) ;
#25671=CYLINDRICAL_SURFACE ( 'NONE', #89363, 2.249999999999998668 ) ;
#25684=CARTESIAN_POINT ( 'NONE',  ( 32.16024265030974050, -5.965225279485572685, 14.03360796525321774 ) ) ;
#25695=PLANE ( 'NONE',  #82495 ) ;
#25708=LINE ( 'NONE', #24208, #73498 ) ;
#25726=CIRCLE ( 'NONE', #9574, 2.040000000000000036 ) ;
#25735=EDGE_CURVE ( 'NONE', #16980, #12582, #78924, .T. ) ;
#25736=B_SPLINE_CURVE_WITH_KNOTS ( 'NONE', 3,
 ( #96032, #71703, #33130, #25520, #56493 ),
 .UNSPECIFIED., .F., .F.,
 ( 4, 1, 4 ),
 ( 0.09110967255127218334, 0.09110974468632360157, 0.09110981682137500592 ),
 .UNSPECIFIED. ) ;
#25751=DIRECTION ( 'NONE',  ( 0.000000000000000000, 0.000000000000000000, 1.000000000000000000 ) ) ;
#25771=ORIENTED_EDGE ( 'NONE', *, *, #36471, .F. ) ;
#25791=VECTOR ( 'NONE', #77839, 1000.000000000000000 ) ;
#25801=VECTOR ( 'NONE', #52446, 1000.000000000000000 ) ;
#25803=DIRECTION ( 'NONE',  ( 0.000000000000000000, 0.000000000000000000, -1.000000000000000000 ) ) ;
#25805=AXIS2_PLACEMENT_3D ( 'NONE', #91335, #45675, #15214 ) ;
#25852=LINE ( 'NONE', #10126, #41488 ) ;
#25854=VERTEX_POINT ( 'NONE', #64600 ) ;
#25856=VECTOR ( 'NONE', #69778, 1000.000000000000000 ) ;
#25862=EDGE_CURVE ( 'NONE', #17845, #83405, #61136, .T. ) ;
#25877=CARTESIAN_POINT ( 'NONE',  ( -28.98875734969026041, -5.965225279485572685, 23.37402280011862743 ) ) ;
#25888=CARTESIAN_POINT ( 'NONE',  ( 29.73860345376316872, 5.356774720514427379, 17.30421508979850387 ) ) ;
#25910=FACE_OUTER_BOUND ( 'NONE', #26228, .T. ) ;
#25912=ORIENTED_EDGE ( 'NONE', *, *, #29263, .F. ) ;
#25913=CARTESIAN_POINT ( 'NONE',  ( 5.399550031317769339, -5.965225279485594001, -28.54570968858208246 ) ) ;
#25939=AXIS2_PLACEMENT_3D ( 'NONE', #16619, #30852, #69417 ) ;
#25953=DIRECTION ( 'NONE',  ( 1.700709290173338723E-14, 0.000000000000000000, 1.000000000000000000 ) ) ;
#25976=EDGE_CURVE ( 'NONE', #74588, #91432, #49775, .T. ) ;
#25978=ORIENTED_EDGE ( 'NONE', *, *, #28875, .F. ) ;
#25984=DIRECTION ( 'NONE',  ( 0.000000000000000000, 0.000000000000000000, -1.000000000000000000 ) ) ;
#25986=DIRECTION ( 'NONE',  ( -0.000000000000000000, -1.000000000000000000, -0.000000000000000000 ) ) ;
#25992=VERTEX_POINT ( 'NONE', #43732 ) ;
#26025=FACE_OUTER_BOUND ( 'NONE', #91994, .T. ) ;
#26045=B_SPLINE_CURVE_WITH_KNOTS ( 'NONE', 3,
 ( #84723, #69002, #17213, #92331 ),
 .UNSPECIFIED., .F., .F.,
 ( 4, 4 ),
 ( 1.788112030672749005E-18, 0.0002127494369525745788 ),
 .UNSPECIFIED. ) ;
#26051=ADVANCED_FACE ( 'NONE', ( #66597 ), #97509, .F. ) ;
#26052=PLANE ( 'NONE',  #16730 ) ;
#26075=CARTESIAN_POINT ( 'NONE',  ( -10.15655021453082263, 4.851073166933324465, 30.10912256999369774 ) ) ;
#26087=CYLINDRICAL_SURFACE ( 'NONE', #97888, 6.000000000000000888 ) ;
#26117=CARTESIAN_POINT ( 'NONE',  ( 27.53860345374808105, 5.356774720514427379, 1.647607965253217399 ) ) ;
#26139=CARTESIAN_POINT ( 'NONE',  ( 31.53822845103994865, 4.132774720514425404, -2.786383594989611634 ) ) ;
#26140=LINE ( 'NONE', #2819, #29503 ) ;
#26161=DIRECTION ( 'NONE',  ( 0.000000000000000000, 1.000000000000000000, 0.000000000000000000 ) ) ;
#26165=LINE ( 'NONE', #26674, #28843 ) ;
#26184=FACE_OUTER_BOUND ( 'NONE', #44448, .T. ) ;
#26185=CARTESIAN_POINT ( 'NONE',  ( 15.92621150404962371, -5.965225279485572685, -27.29681269571043245 ) ) ;
#26187=B_SPLINE_CURVE_WITH_KNOTS ( 'NONE', 3,
 ( #36694, #29074, #60049, #90976, #83356, #6235 ),
 .UNSPECIFIED., .F., .F.,
 ( 4, 2, 4 ),
 ( 0.000000000000000000, 0.0005049716539041804782, 0.001009943307808368112 ),
 .UNSPECIFIED. ) ;
#26190=AXIS2_PLACEMENT_3D ( 'NONE', #99611, #87787, #49242 ) ;
#26197=FACE_OUTER_BOUND ( 'NONE', #79200, .T. ) ;
#26199=VERTEX_POINT ( 'NONE', #70557 ) ;
#26211=CARTESIAN_POINT ( 'NONE',  ( 32.40823333110732563, 4.442403080972329832, -4.096588619916003537 ) ) ;
#26218=ORIENTED_EDGE ( 'NONE', *, *, #78973, .F. ) ;
#26226=CARTESIAN_POINT ( 'NONE',  ( 14.45468597507895225, 3.471643246632551527, -28.36588305008992705 ) ) ;
#26228=EDGE_LOOP ( 'NONE', ( #32723, #44568, #25771, #34490 ) ) ;
#26229=CARTESIAN_POINT ( 'NONE',  ( -4.568292318365942073, -5.965225279485572685, 30.06720597538392425 ) ) ;
#26239=ORIENTED_EDGE ( 'NONE', *, *, #54512, .T. ) ;
#26260=ORIENTED_EDGE ( 'NONE', *, *, #84192, .F. ) ;
#26263=AXIS2_PLACEMENT_3D ( 'NONE', #32248, #7405, #7913 ) ;
#26280=CARTESIAN_POINT ( 'NONE',  ( 32.50838937279095120, 0.6027747205144262654, -10.74666623472941218 ) ) ;
#26306=VECTOR ( 'NONE', #55151, 1000.000000000000000 ) ;
#26307=ORIENTED_EDGE ( 'NONE', *, *, #85164, .T. ) ;
#26316=CARTESIAN_POINT ( 'NONE',  ( 33.24104357593923709, 3.536202174476160920, -12.73333860248705740 ) ) ;
#26330=CARTESIAN_POINT ( 'NONE',  ( 30.77564450787170003, 1.682774720514426114, -9.689394075852828081 ) ) ;
#26337=ORIENTED_EDGE ( 'NONE', *, *, #93757, .T. ) ;
#26340=VERTEX_POINT ( 'NONE', #41351 ) ;
#26358=EDGE_CURVE ( 'NONE', #87883, #39840, #57952, .T. ) ;
#26360=ORIENTED_EDGE ( 'NONE', *, *, #68378, .T. ) ;
#26368=CARTESIAN_POINT ( 'NONE',  ( 32.53135143123563466, -5.965225279485572685, 6.926385399448451885 ) ) ;
#26372=CARTESIAN_POINT ( 'NONE',  ( -23.59123376470063960, -6.143225279485574397, 23.50402280011862288 ) ) ;
#26406=FACE_OUTER_BOUND ( 'NONE', #40622, .T. ) ;
#26408=VECTOR ( 'NONE', #33261, 1000.000000000000000 ) ;
#26412=CARTESIAN_POINT ( 'NONE',  ( 13.59451591917074431, 3.316774720514426456, -28.23515841827053308 ) ) ;
#26419=LINE ( 'NONE', #18305, #45773 ) ;
#26423=DIRECTION ( 'NONE',  ( 0.000000000000000000, 0.000000000000000000, -1.000000000000000000 ) ) ;
#26429=DIRECTION ( 'NONE',  ( 0.000000000000000000, 0.000000000000000000, -1.000000000000000000 ) ) ;
#26437=CARTESIAN_POINT ( 'NONE',  ( 13.64113475014448618, 3.316774720514425567, -28.24100986136700442 ) ) ;
#26448=LINE ( 'NONE', #57412, #6178 ) ;
#26469=CARTESIAN_POINT ( 'NONE',  ( 14.98548720554672187, 3.495622884075268999, -27.33451462832999113 ) ) ;
#26470=EDGE_CURVE ( 'NONE', #38206, #97546, #36235, .T. ) ;
#26476=ORIENTED_EDGE ( 'NONE', *, *, #37996, .T. ) ;
#26513=CARTESIAN_POINT ( 'NONE',  ( 5.399550031317772891, -1.324225279485572893, -28.54570968858208246 ) ) ;
#26515=CARTESIAN_POINT ( 'NONE',  ( 25.13018594592114852, 5.151325109778972511, -8.770570395071676018 ) ) ;
#26522=CARTESIAN_POINT ( 'NONE',  ( -12.64432969575899968, 0.3587747205143967943, -26.13179214487285407 ) ) ;
#26525=CARTESIAN_POINT ( 'NONE',  ( 282.9764569301858046, -6.475225279485573360, 20.79159422840526616 ) ) ;
#26550=ORIENTED_EDGE ( 'NONE', *, *, #18400, .F. ) ;
#26587=CARTESIAN_POINT ( 'NONE',  ( 0.000000000000000000, -1.477225279485574028, -1.352392034746782823 ) ) ;
#26593=CARTESIAN_POINT ( 'NONE',  ( 6.421796364777552668, 5.356774720514453136, -25.37953985271570900 ) ) ;
#26600=ORIENTED_EDGE ( 'NONE', *, *, #12403, .T. ) ;
#26604=CARTESIAN_POINT ( 'NONE',  ( -27.61845239340658154, -5.965225279485594001, -10.37513603161905351 ) ) ;
#26639=CARTESIAN_POINT ( 'NONE',  ( 28.20688450243577705, 14.82721238576592704, -7.073367244511738150 ) ) ;
#26643=ADVANCED_FACE ( 'NONE', ( #68679 ), #37720, .F. ) ;
#26645=ORIENTED_EDGE ( 'NONE', *, *, #49793, .T. ) ;
#26657=CARTESIAN_POINT ( 'NONE',  ( 10.22011794243639038, 5.356774720516090937, -27.02313658038265132 ) ) ;
#26661=CARTESIAN_POINT ( 'NONE',  ( -0.02075734969026423599, 5.866774720514426278, -0.08597719988137648983 ) ) ;
#26669=DIRECTION ( 'NONE',  ( 0.7512896232465891000, -1.109416176496794925E-16, 0.6599726524652351767 ) ) ;
#26674=CARTESIAN_POINT ( 'NONE',  ( -12.65407072091355722, 6.376774720514426953, -26.15404995688569301 ) ) ;
#26675=DIRECTION ( 'NONE',  ( 0.6451914333552788428, 0.000000000000000000, 0.7640209514960702997 ) ) ;
#26684=CARTESIAN_POINT ( 'NONE',  ( 5.271800844963591359, 5.356774720514425603, -28.56638892015329034 ) ) ;
#26692=VECTOR ( 'NONE', #84326, 1000.000000000000114 ) ;
#26702=ORIENTED_EDGE ( 'NONE', *, *, #44166, .T. ) ;
#26748=LINE ( 'NONE', #74901, #93253 ) ;
#26749=CARTESIAN_POINT ( 'NONE',  ( 22.02124265030973760, -4.543225279485573864, 17.35402280011862786 ) ) ;
#26752=ORIENTED_EDGE ( 'NONE', *, *, #36471, .T. ) ;
#26756=EDGE_CURVE ( 'NONE', #63436, #8729, #27381, .T. ) ;
#26757=EDGE_CURVE ( 'NONE', #89963, #52986, #18754, .T. ) ;
#26758=DIRECTION ( 'NONE',  ( 0.7640209514960704107, 0.000000000000000000, -0.6451914333552789538 ) ) ;
#26765=VERTEX_POINT ( 'NONE', #19745 ) ;
#26789=LINE ( 'NONE', #81580, #94594 ) ;
#26796=DIRECTION ( 'NONE',  ( -1.889676989081488347E-15, 0.000000000000000000, -1.000000000000000000 ) ) ;
#26801=CARTESIAN_POINT ( 'NONE',  ( -0.02075734969026423599, -5.965225279485572685, -0.08597719988137648983 ) ) ;
#26806=CIRCLE ( 'NONE', #70614, 0.8160000000000007248 ) ;
#26811=EDGE_LOOP ( 'NONE', ( #7452, #2271, #5125, #8868, #87171, #7506, #43271, #64473, #41672, #31721, #90235, #16611, #2815, #47293, #62717, #36356 ) ) ;
#26816=ORIENTED_EDGE ( 'NONE', *, *, #75566, .T. ) ;
#26835=ORIENTED_EDGE ( 'NONE', *, *, #30956, .T. ) ;
#26844=FACE_OUTER_BOUND ( 'NONE', #84619, .T. ) ;
#26858=ADVANCED_FACE ( 'NONE', ( #13133 ), #90272, .F. ) ;
#26872=DIRECTION ( 'NONE',  ( 0.000000000000000000, 0.000000000000000000, -1.000000000000000000 ) ) ;
#26897=DIRECTION ( 'NONE',  ( -4.472869286569340140E-16, -1.000000000000000000, 7.102795889480464408E-16 ) ) ;
#26906=EDGE_LOOP ( 'NONE', ( #45601, #49593, #774, #1971 ) ) ;
#26930=CARTESIAN_POINT ( 'NONE',  ( 11.22265027772288093, 3.316774720514091612, -28.06709888818796017 ) ) ;
#26932=ORIENTED_EDGE ( 'NONE', *, *, #88943, .T. ) ;
#26934=CARTESIAN_POINT ( 'NONE',  ( -20.27875734969026311, -6.143225279485574397, 24.00402280011862288 ) ) ;
#26947=CARTESIAN_POINT ( 'NONE',  ( 15.01911467442486625, 4.015204461132062974, -28.37592028203548011 ) ) ;
#26953=CARTESIAN_POINT ( 'NONE',  ( 31.60706529141451426, 6.376774720514427841, 26.12024523944107557 ) ) ;
#26968=ORIENTED_EDGE ( 'NONE', *, *, #23039, .F. ) ;
#26969=VECTOR ( 'NONE', #31700, 1000.000000000000114 ) ;
#26974=CARTESIAN_POINT ( 'NONE',  ( -27.96875734969026084, -6.143225279485574397, 23.50402280011861933 ) ) ;
#26979=ORIENTED_EDGE ( 'NONE', *, *, #59066, .F. ) ;
#26984=AXIS2_PLACEMENT_3D ( 'NONE', #99781, #75458, #5958 ) ;
#27006=CARTESIAN_POINT ( 'NONE',  ( -24.90875734969025501, -5.965225279485572685, 26.43402280011862615 ) ) ;
#27016=ORIENTED_EDGE ( 'NONE', *, *, #61772, .T. ) ;
#27018=AXIS2_PLACEMENT_3D ( 'NONE', #49996, #11416, #80425 ) ;
#27034=AXIS2_PLACEMENT_3D ( 'NONE', #32529, #55888, #95432 ) ;
#27061=AXIS2_PLACEMENT_3D ( 'NONE', #26525, #1691, #57490 ) ;
#27076=DIRECTION ( 'NONE',  ( -0.000000000000000000, -0.000000000000000000, 1.000000000000000000 ) ) ;
#27078=VECTOR ( 'NONE', #55334, 1000.000000000000000 ) ;
#27085=VECTOR ( 'NONE', #35520, 1000.000000000000000 ) ;
#27094=ORIENTED_EDGE ( 'NONE', *, *, #69201, .F. ) ;
#27096=ADVANCED_FACE ( 'NONE', ( #57725 ), #71448, .F. ) ;
#27099=LINE ( 'NONE', #65686, #45510 ) ;
#27101=ORIENTED_EDGE ( 'NONE', *, *, #97455, .T. ) ;
#27124=CARTESIAN_POINT ( 'NONE',  ( -27.13414387080440093, -5.965225279485594001, -10.21530720150730254 ) ) ;
#27127=AXIS2_PLACEMENT_3D ( 'NONE', #38984, #37989, #15145 ) ;
#27137=CARTESIAN_POINT ( 'NONE',  ( 15.32675665358028283, 3.579156900695799060, -27.14457288197743878 ) ) ;
#27142=ORIENTED_EDGE ( 'NONE', *, *, #75566, .F. ) ;
#27150=( BOUNDED_SURFACE ( )  B_SPLINE_SURFACE ( 3, 2, ( 
 ( #77717, #1121, #32058 ),
 ( #93955, #55920, #85340 ),
 ( #24444, #86841, #17337 ),
 ( #69633, #79230, #9729 ),
 ( #2135, #33070, #92947 ),
 ( #80747, #81240, #88358 ),
 ( #11230, #42207, #82233 ),
 ( #3135, #73139, #74132 ),
 ( #49816, #3630, #81740 ),
 ( #2629, #65547, #64549 ),
 ( #19823, #34579, #96464 ),
 ( #65049, #4124, #89356 ),
 ( #50304, #41186, #50801 ),
 ( #41699, #95462, #72143 ),
 ( #95966, #19335, #12215 ),
 ( #33571, #26953, #4625 ) ),
 .UNSPECIFIED., .F., .F., .T. ) 
 B_SPLINE_SURFACE_WITH_KNOTS ( ( 4, 2, 2, 2, 2, 2, 2, 4 ),
 ( 3, 3 ),
 ( 5.963111948670274387E-19, 0.0002402527847056124086, 0.0004805055694112242209, 0.0007207583541168360603, 0.0009610111388224478997, 0.001201263923528059739, 0.001441516708233671470, 0.001922022277644895149 ),
 ( 0.000000000000000000, 1.000000000000000000 ),
 .UNSPECIFIED. ) 
 GEOMETRIC_REPRESENTATION_ITEM ( )  RATIONAL_B_SPLINE_SURFACE ( (
 ( 1.000000000000000000, 0.6532382444175202085, 1.000000000000000000),
 ( 1.000000000000000000, 0.6532394276814369460, 1.000000000000000000),
 ( 1.000000000000000000, 0.6536213453767286685, 1.000000000000000000),
 ( 1.000000000000000000, 0.6551141999105375424, 1.000000000000000000),
 ( 1.000000000000000000, 0.6562426621441458385, 1.000000000000000000),
 ( 1.000000000000000000, 0.6591574828660696772, 1.000000000000000000),
 ( 1.000000000000000000, 0.6609310395923536641, 1.000000000000000000),
 ( 1.000000000000000000, 0.6650742797341039347, 1.000000000000000000),
 ( 1.000000000000000000, 0.6674600455424170020, 1.000000000000000000),
 ( 1.000000000000000000, 0.6725980719960679144, 1.000000000000000000),
 ( 1.000000000000000000, 0.6753708636379929242, 1.000000000000000000),
 ( 1.000000000000000000, 0.6813027919944147914, 1.000000000000000000),
 ( 1.000000000000000000, 0.6844015431888567091, 1.000000000000000000),
 ( 1.000000000000000000, 0.6938890553659712301, 1.000000000000000000),
 ( 1.000000000000000000, 0.7006220437376852184, 1.000000000000000000),
 ( 1.000000000000000000, 0.7071067811865475727, 1.000000000000000000) ) ) 
 REPRESENTATION_ITEM ( '' )  SURFACE ( )  );
#27155=CARTESIAN_POINT ( 'NONE',  ( 9.131215498121711960, 5.356774720514425603, -25.00673578072587588 ) ) ;
#27162=DIRECTION ( 'NONE',  ( 0.000000000000000000, 0.000000000000000000, 1.000000000000000000 ) ) ;
#27165=AXIS2_PLACEMENT_3D ( 'NONE', #95927, #39635, #26423 ) ;
#27166=CARTESIAN_POINT ( 'NONE',  ( 5.949073730962466833, -5.965225279485572685, -27.94053387008862188 ) ) ;
#27169=DIRECTION ( 'NONE',  ( -0.1311553622875919756, -6.845827386180409975E-16, -0.9913618264504692190 ) ) ;
#27171=EDGE_CURVE ( 'NONE', #37175, #66086, #48110, .T. ) ;
#27173=DIRECTION ( 'NONE',  ( -0.000000000000000000, -0.000000000000000000, -1.000000000000000000 ) ) ;
#27192=EDGE_CURVE ( 'NONE', #94148, #93421, #1933, .T. ) ;
#27208=CARTESIAN_POINT ( 'NONE',  ( 21.97688922017995239, 4.772774720514425972, -18.55878510778117985 ) ) ;
#27218=ORIENTED_EDGE ( 'NONE', *, *, #17484, .F. ) ;
#27226=ORIENTED_EDGE ( 'NONE', *, *, #22851, .F. ) ;
#27251=DIRECTION ( 'NONE',  ( 0.000000000000000000, 1.000000000000000000, 0.000000000000000000 ) ) ;
#27277=DIRECTION ( 'NONE',  ( -0.9888510809027409865, -4.164321980682959710E-15, -0.1489078231574183231 ) ) ;
#27278=ORIENTED_EDGE ( 'NONE', *, *, #24894, .F. ) ;
#27280=DIRECTION ( 'NONE',  ( 0.000000000000000000, -1.000000000000000000, 0.000000000000000000 ) ) ;
#27292=LINE ( 'NONE', #34404, #5439 ) ;
#27305=LINE ( 'NONE', #96318, #25650 ) ;
#27333=CARTESIAN_POINT ( 'NONE',  ( 26.74698519091204574, 4.772774720514425972, -10.98683230472873973 ) ) ;
#27334=ORIENTED_EDGE ( 'NONE', *, *, #69193, .T. ) ;
#27339=EDGE_LOOP ( 'NONE', ( #52430, #90503 ) ) ;
#27340=EDGE_LOOP ( 'NONE', ( #94138, #36568, #72656, #55050 ) ) ;
#27348=FACE_OUTER_BOUND ( 'NONE', #80694, .T. ) ;
#27361=DIRECTION ( 'NONE',  ( 0.9888510809027408754, -5.365801633547220192E-16, 0.1489078231574191280 ) ) ;
#27367=EDGE_CURVE ( 'NONE', #36345, #64249, #19105, .T. ) ;
#27376=FACE_OUTER_BOUND ( 'NONE', #79373, .T. ) ;
#27378=EDGE_CURVE ( 'NONE', #35739, #45794, #71897, .T. ) ;
#27381=LINE ( 'NONE', #25877, #69307 ) ;
#27388=LINE ( 'NONE', #4053, #12558 ) ;
#27393=CARTESIAN_POINT ( 'NONE',  ( 0.000000000000000000, -1.477225279485574028, -1.352392034746782823 ) ) ;
#27399=VECTOR ( 'NONE', #78877, 1000.000000000000000 ) ;
#27427=DIRECTION ( 'NONE',  ( 1.000000000000000000, 3.639962309748244178E-15, 0.000000000000000000 ) ) ;
#27430=ORIENTED_EDGE ( 'NONE', *, *, #66774, .T. ) ;
#27439=CARTESIAN_POINT ( 'NONE',  ( 31.62087157062645204, 4.386438359062696080, 26.73777224682022435 ) ) ;
#27447=DIRECTION ( 'NONE',  ( 0.000000000000000000, 0.000000000000000000, -1.000000000000000000 ) ) ;
#27452=DIRECTION ( 'NONE',  ( -0.8264557562326033668, -6.845827386180409975E-16, -0.5630016722799281448 ) ) ;
#27455=FACE_OUTER_BOUND ( 'NONE', #75150, .T. ) ;
#27456=CARTESIAN_POINT ( 'NONE',  ( 14.83405752585473891, 4.881907540128495704, -27.54622755360321307 ) ) ;
#27466=CIRCLE ( 'NONE', #19337, 1.529999999999998916 ) ;
#27469=EDGE_CURVE ( 'NONE', #32299, #4321, #57821, .T. ) ;
#27476=ORIENTED_EDGE ( 'NONE', *, *, #76444, .T. ) ;
#27489=ORIENTED_EDGE ( 'NONE', *, *, #27469, .T. ) ;
#27496=ORIENTED_EDGE ( 'NONE', *, *, #8071, .F. ) ;
#27520=DIRECTION ( 'NONE',  ( 0.000000000000000000, -1.000000000000000000, 0.000000000000000000 ) ) ;
#27521=ORIENTED_EDGE ( 'NONE', *, *, #25976, .T. ) ;
#27535=DIRECTION ( 'NONE',  ( 0.000000000000000000, 1.000000000000000000, -1.084202172485504434E-16 ) ) ;
#27542=CARTESIAN_POINT ( 'NONE',  ( -29.49875734969025842, -5.965225279485572685, 15.62202280011862321 ) ) ;
#27544=AXIS2_PLACEMENT_3D ( 'NONE', #27598, #19967, #67169 ) ;
#27546=AXIS2_PLACEMENT_3D ( 'NONE', #57550, #95593, #19458 ) ;
#27569=ADVANCED_FACE ( 'NONE', ( #87034 ), #24625, .T. ) ;
#27573=EDGE_CURVE ( 'NONE', #52686, #51486, #47984, .T. ) ;
#27598=CARTESIAN_POINT ( 'NONE',  ( 31.79364159983995464, 1.682774720514426114, -11.59305536555894278 ) ) ;
#27599=ORIENTED_EDGE ( 'NONE', *, *, #10825, .T. ) ;
#27609=DIRECTION ( 'NONE',  ( -0.000000000000000000, 1.000000000000000000, -0.000000000000000000 ) ) ;
#27622=CARTESIAN_POINT ( 'NONE',  ( -27.25988310792305214, 0.3587747205144265483, 30.32664379231667695 ) ) ;
#27624=ORIENTED_EDGE ( 'NONE', *, *, #67495, .T. ) ;
#27648=EDGE_CURVE ( 'NONE', #74181, #94973, #44838, .T. ) ;
#27649=CARTESIAN_POINT ( 'NONE',  ( 30.56047832681638354, -2.297196155479634516, 24.67598410064775649 ) ) ;
#27652=VERTEX_POINT ( 'NONE', #78912 ) ;
#27656=VERTEX_POINT ( 'NONE', #3329 ) ;
#27657=CARTESIAN_POINT ( 'NONE',  ( 31.79364159983995464, -5.965225279485572685, -11.59305536555894278 ) ) ;
#27658=CARTESIAN_POINT ( 'NONE',  ( 6.948977015814011615, 5.356774720514426491, -25.20533573604597066 ) ) ;
#27670=LINE ( 'NONE', #95678, #45578 ) ;
#27687=AXIS2_PLACEMENT_3D ( 'NONE', #93405, #77174, #76667 ) ;
#27693=EDGE_CURVE ( 'NONE', #16980, #63531, #14031, .T. ) ;
#27698=CARTESIAN_POINT ( 'NONE',  ( 29.75292639967170771, 5.303223407918566501, 26.69524796275325684 ) ) ;
#27712=CARTESIAN_POINT ( 'NONE',  ( 5.399550031317769339, -5.965225279485594001, -28.54570968858208246 ) ) ;
#27757=VECTOR ( 'NONE', #5066, 1000.000000000000227 ) ;
#27766=CARTESIAN_POINT ( 'NONE',  ( -20.27875734969026311, 3.456774720514426136, 22.85402280011862430 ) ) ;
#27768=DIRECTION ( 'NONE',  ( 0.7682573101345366862, 0.000000000000000000, -0.6401411605457395515 ) ) ;
#27770=LINE ( 'NONE', #59223, #2783 ) ;
#27773=PLANE ( 'NONE',  #39787 ) ;
#27774=CARTESIAN_POINT ( 'NONE',  ( -25.92875734969025814, 6.376774720514426953, 26.43402280011862615 ) ) ;
#27809=LINE ( 'NONE', #60275, #92209 ) ;
#27828=CARTESIAN_POINT ( 'NONE',  ( 17.51792015816173986, -5.965225279485572685, 29.01255224319336889 ) ) ;
#27847=ORIENTED_EDGE ( 'NONE', *, *, #64465, .F. ) ;
#27852=AXIS2_PLACEMENT_3D ( 'NONE', #65473, #35501, #58834 ) ;
#27879=CARTESIAN_POINT ( 'NONE',  ( -2.872281323269014752, 4.293056017849825601, 1.999999999999999556 ) ) ;
#27882=CARTESIAN_POINT ( 'NONE',  ( -20.27875734969026311, -6.143225279485574397, 24.00402280011862288 ) ) ;
#27894=EDGE_CURVE ( 'NONE', #5514, #31628, #84411, .T. ) ;
#27904=LINE ( 'NONE', #76066, #61235 ) ;
#27948=CARTESIAN_POINT ( 'NONE',  ( -24.97666371003640151, -5.965225279485592225, -15.72894043976419098 ) ) ;
#27949=VERTEX_POINT ( 'NONE', #38230 ) ;
#27951=ORIENTED_EDGE ( 'NONE', *, *, #13400, .F. ) ;
#27958=DIRECTION ( 'NONE',  ( 0.000000000000000000, 0.000000000000000000, 1.000000000000000000 ) ) ;
#27962=VERTEX_POINT ( 'NONE', #62090 ) ;
#27965=ORIENTED_EDGE ( 'NONE', *, *, #2489, .T. ) ;
#27968=LINE ( 'NONE', #66058, #80297 ) ;
#27994=ORIENTED_EDGE ( 'NONE', *, *, #40262, .F. ) ;
#28007=VERTEX_POINT ( 'NONE', #30118 ) ;
#28009=DIRECTION ( 'NONE',  ( -0.000000000000000000, -1.000000000000000000, -0.000000000000000000 ) ) ;
#28011=EDGE_CURVE ( 'NONE', #70502, #94742, #61091, .T. ) ;
#28018=EDGE_CURVE ( 'NONE', #78621, #871, #48109, .T. ) ;
#28019=CARTESIAN_POINT ( 'NONE',  ( -27.25988310792305214, 0.3587747205144265483, 30.32664379231667695 ) ) ;
#28026=ORIENTED_EDGE ( 'NONE', *, *, #66322, .T. ) ;
#28044=AXIS2_PLACEMENT_3D ( 'NONE', #26801, #88707, #43532 ) ;
#28056=LINE ( 'NONE', #36167, #46752 ) ;
#28079=CARTESIAN_POINT ( 'NONE',  ( 22.65031661608460922, 2.682774720514426559, -20.71116937900381672 ) ) ;
#28084=AXIS2_PLACEMENT_3D ( 'NONE', #29294, #92681, #37910 ) ;
#28095=EDGE_LOOP ( 'NONE', ( #54788, #68274, #54726, #59953 ) ) ;
#28105=LINE ( 'NONE', #90495, #72331 ) ;
#28111=DIRECTION ( 'NONE',  ( -0.9496245541219264785, -6.845827386180410961E-16, -0.3133898629642195011 ) ) ;
#28121=ORIENTED_EDGE ( 'NONE', *, *, #92979, .T. ) ;
#28147=ADVANCED_FACE ( 'NONE', ( #17906 ), #48866, .F. ) ;
#28155=CARTESIAN_POINT ( 'NONE',  ( 5.659515148826130826, 3.316774720513238517, -27.47062408975114067 ) ) ;
#28175=CARTESIAN_POINT ( 'NONE',  ( 13.86067930680220073, 3.316774720515830666, -28.23766061184437604 ) ) ;
#28182=ADVANCED_FACE ( 'NONE', ( #20381 ), #98002, .T. ) ;
#28188=DIRECTION ( 'NONE',  ( 0.9888510809027409865, -7.885106708985486076E-16, 0.1489078231574183231 ) ) ;
#28190=VERTEX_POINT ( 'NONE', #89416 ) ;
#28192=CARTESIAN_POINT ( 'NONE',  ( 30.63935204725980554, 3.888906929512149446, 28.25823861891851507 ) ) ;
#28193=AXIS2_PLACEMENT_3D ( 'NONE', #14665, #82181, #12667 ) ;
#28196=ORIENTED_EDGE ( 'NONE', *, *, #65545, .F. ) ;
#28197=ORIENTED_EDGE ( 'NONE', *, *, #53856, .F. ) ;
#28210=ORIENTED_EDGE ( 'NONE', *, *, #69193, .F. ) ;
#28216=VERTEX_POINT ( 'NONE', #28506 ) ;
#28219=DIRECTION ( 'NONE',  ( -0.000000000000000000, 1.000000000000000000, -0.000000000000000000 ) ) ;
#28226=DIRECTION ( 'NONE',  ( -0.000000000000000000, -1.000000000000000000, 0.000000000000000000 ) ) ;
#28243=LINE ( 'NONE', #59204, #98302 ) ;
#28249=EDGE_CURVE ( 'NONE', #50681, #22596, #6008, .T. ) ;
#28257=EDGE_CURVE ( 'NONE', #10246, #58683, #78849, .T. ) ;
#28262=DIRECTION ( 'NONE',  ( 1.000000000000000000, 0.000000000000000000, 0.000000000000000000 ) ) ;
#28269=DIRECTION ( 'NONE',  ( -0.7512896232465892110, 0.000000000000000000, -0.6599726524652350657 ) ) ;
#28270=CARTESIAN_POINT ( 'NONE',  ( 33.96422015159436114, 0.3587747205144265483, -7.233236000911337449 ) ) ;
#28274=CARTESIAN_POINT ( 'NONE',  ( 32.53346577320678534, 1.682774720514426114, -11.93731717363831102 ) ) ;
#28293=CARTESIAN_POINT ( 'NONE',  ( 30.53060340732035982, -1.477225279485574028, 19.84760796525321780 ) ) ;
#28300=DIRECTION ( 'NONE',  ( 0.000000000000000000, -1.478457507934778393E-16, -1.000000000000000000 ) ) ;
#28311=DIRECTION ( 'NONE',  ( -0.000000000000000000, 1.000000000000000000, -0.000000000000000000 ) ) ;
#28324=FACE_OUTER_BOUND ( 'NONE', #95964, .T. ) ;
#28335=ORIENTED_EDGE ( 'NONE', *, *, #20160, .T. ) ;
#28364=EDGE_CURVE ( 'NONE', #95809, #76588, #10174, .T. ) ;
#28368=DIRECTION ( 'NONE',  ( 0.000000000000000000, 3.740001113483016365E-15, -1.000000000000000000 ) ) ;
#28371=ORIENTED_EDGE ( 'NONE', *, *, #7092, .T. ) ;
#28376=DIRECTION ( 'NONE',  ( 1.000000000000000000, -0.000000000000000000, -0.000000000000000000 ) ) ;
#28377=CARTESIAN_POINT ( 'NONE',  ( 9.402885806365684829, 0.3587747205144265483, 29.04108526060719342 ) ) ;
#28423=VECTOR ( 'NONE', #50097, 1000.000000000000000 ) ;
#28424=CARTESIAN_POINT ( 'NONE',  ( 33.13288845015618023, 0.3587747205144265483, -0.1650522222209214185 ) ) ;
#28428=FACE_OUTER_BOUND ( 'NONE', #78639, .T. ) ;
#28430=FACE_OUTER_BOUND ( 'NONE', #94250, .T. ) ;
#28440=EDGE_CURVE ( 'NONE', #47768, #36906, #56301, .T. ) ;
#28493=VECTOR ( 'NONE', #23264, 1000.000000000000000 ) ;
#28497=ORIENTED_EDGE ( 'NONE', *, *, #5664, .T. ) ;
#28506=CARTESIAN_POINT ( 'NONE',  ( -29.49875734969026198, 0.3587747205144265483, 10.11402280011862587 ) ) ;
#28523=EDGE_CURVE ( 'NONE', #98946, #50260, #49756, .T. ) ;
#28526=CARTESIAN_POINT ( 'NONE',  ( 10.95759398273795249, 4.132774720514426292, -26.86884997114579932 ) ) ;
#28527=CARTESIAN_POINT ( 'NONE',  ( 29.73860345376319358, 3.356774720514427379, 1.647607965253216067 ) ) ;
#28551=AXIS2_PLACEMENT_3D ( 'NONE', #42943, #72888, #65298 ) ;
#28552=ORIENTED_EDGE ( 'NONE', *, *, #75219, .F. ) ;
#28554=B_SPLINE_CURVE_WITH_KNOTS ( 'NONE', 3,
 ( #95737, #81518, #66308, #95237, #80509, #11993, #97235, #72911, #26226, #2906 ),
 .UNSPECIFIED., .F., .F.,
 ( 4, 2, 2, 2, 4 ),
 ( 0.000000000000000000, 0.0004686948575969753904, 0.0009373897151939507809, 0.001406084572790926171, 0.001874779430387901562 ),
 .UNSPECIFIED. ) ;
#28564=CARTESIAN_POINT ( 'NONE',  ( 20.98022359556508931, 4.383291743620153724, -17.13764241148466994 ) ) ;
#28603=EDGE_CURVE ( 'NONE', #9599, #14974, #74078, .T. ) ;
#28611=EDGE_CURVE ( 'NONE', #95350, #7760, #19040, .T. ) ;
#28631=VECTOR ( 'NONE', #75077, 1000.000000000000227 ) ;
#28634=EDGE_CURVE ( 'NONE', #45943, #45676, #16523, .T. ) ;
#28635=EDGE_LOOP ( 'NONE', ( #45772, #28210, #25252, #17125, #89820, #48327, #47088, #36855, #14683 ) ) ;
#28642=ORIENTED_EDGE ( 'NONE', *, *, #36009, .T. ) ;
#28643=AXIS2_PLACEMENT_3D ( 'NONE', #93752, #39475, #25751 ) ;
#28649=CARTESIAN_POINT ( 'NONE',  ( 10.77631500667670572, 5.356774720514423827, -24.99100794736120434 ) ) ;
#28654=DIRECTION ( 'NONE',  ( 0.000000000000000000, 0.000000000000000000, 1.000000000000000000 ) ) ;
#28672=CARTESIAN_POINT ( 'NONE',  ( 10.86264265030973952, -5.965225279485574461, -27.62597719988137612 ) ) ;
#28686=ORIENTED_EDGE ( 'NONE', *, *, #39215, .T. ) ;
#28689=CARTESIAN_POINT ( 'NONE',  ( 30.60441873609196151, 4.296715115238376015, 26.89749680779764773 ) ) ;
#28691=ADVANCED_FACE ( 'NONE', ( #31765 ), #53620, .F. ) ;
#28693=EDGE_CURVE ( 'NONE', #73934, #52090, #51029, .T. ) ;
#28695=EDGE_CURVE ( 'NONE', #76406, #83129, #69235, .T. ) ;
#28696=ORIENTED_EDGE ( 'NONE', *, *, #29493, .T. ) ;
#28743=ORIENTED_EDGE ( 'NONE', *, *, #64240, .T. ) ;
#28744=DIRECTION ( 'NONE',  ( 0.000000000000000000, 0.000000000000000000, -1.000000000000000000 ) ) ;
#28758=DIRECTION ( 'NONE',  ( 0.000000000000000000, 1.000000000000000000, 0.000000000000000000 ) ) ;
#28759=ADVANCED_FACE ( 'NONE', ( #47495, #46491, #46993 ), #813, .T. ) ;
#28766=ORIENTED_EDGE ( 'NONE', *, *, #70865, .F. ) ;
#28779=AXIS2_PLACEMENT_3D ( 'NONE', #55196, #100321, #71411 ) ;
#28802=VERTEX_POINT ( 'NONE', #94152 ) ;
#28806=ADVANCED_FACE ( 'NONE', ( #24638 ), #55618, .F. ) ;
#28837=ORIENTED_EDGE ( 'NONE', *, *, #1964, .F. ) ;
#28843=VECTOR ( 'NONE', #33271, 1000.000000000000000 ) ;
#28855=EDGE_LOOP ( 'NONE', ( #41857, #17765, #36330, #37223, #79399 ) ) ;
#28858=DIRECTION ( 'NONE',  ( 0.000000000000000000, 1.000000000000000000, 0.000000000000000000 ) ) ;
#28859=AXIS2_PLACEMENT_3D ( 'NONE', #50784, #49797, #27447 ) ;
#28875=EDGE_CURVE ( 'NONE', #39863, #76643, #84978, .T. ) ;
#28888=CARTESIAN_POINT ( 'NONE',  ( 12.17309066428871667, 5.143895418987112222, -26.49515656621686333 ) ) ;
#28900=EDGE_LOOP ( 'NONE', ( #77105, #86356, #77388, #59576 ) ) ;
#28914=CARTESIAN_POINT ( 'NONE',  ( 32.66876533700882845, -5.965225279485572685, -12.58926540598385557 ) ) ;
#28926=DIRECTION ( 'NONE',  ( 0.3133898629642186684, -7.885106708985488048E-16, -0.9496245541219267006 ) ) ;
#28936=EDGE_CURVE ( 'NONE', #43843, #47644, #87047, .T. ) ;
#28954=ORIENTED_EDGE ( 'NONE', *, *, #89653, .F. ) ;
#28975=DIRECTION ( 'NONE',  ( -0.000000000000000000, 1.000000000000000000, -0.000000000000000000 ) ) ;
#28977=EDGE_CURVE ( 'NONE', #86861, #79629, #15773, .T. ) ;
#29004=DIRECTION ( 'NONE',  ( 0.000000000000000000, -1.000000000000000000, 0.000000000000000000 ) ) ;
#29011=EDGE_LOOP ( 'NONE', ( #93612, #26476, #73671, #55167 ) ) ;
#29031=DIRECTION ( 'NONE',  ( -0.000000000000000000, -1.000000000000000000, -0.000000000000000000 ) ) ;
#29033=AXIS2_PLACEMENT_3D ( 'NONE', #31178, #85464, #99189 ) ;
#29041=VECTOR ( 'NONE', #70042, 1000.000000000000000 ) ;
#29056=ORIENTED_EDGE ( 'NONE', *, *, #35579, .F. ) ;
#29074=CARTESIAN_POINT ( 'NONE',  ( 31.59245846751552378, 5.049734226592146769, -4.287355462049295518 ) ) ;
#29087=ORIENTED_EDGE ( 'NONE', *, *, #51163, .F. ) ;
#29121=VECTOR ( 'NONE', #44364, 1000.000000000000000 ) ;
#29123=VECTOR ( 'NONE', #35090, 1000.000000000000000 ) ;
#29125=CIRCLE ( 'NONE', #22660, 25.90800000000000125 ) ;
#29135=ADVANCED_FACE ( 'NONE', ( #90051 ), #97166, .F. ) ;
#29138=ORIENTED_EDGE ( 'NONE', *, *, #415, .F. ) ;
#29157=CARTESIAN_POINT ( 'NONE',  ( -0.02075734969026423599, 6.376774720514426953, -29.05397719988137339 ) ) ;
#29162=DIRECTION ( 'NONE',  ( 0.000000000000000000, -1.000000000000000000, 0.000000000000000000 ) ) ;
#29164=CARTESIAN_POINT ( 'NONE',  ( 27.53860345374808105, 5.356774720496559894, -0.3523920347467610070 ) ) ;
#29170=CARTESIAN_POINT ( 'NONE',  ( -0.02075734969026423599, -6.475225279485573360, -0.08597719988137648983 ) ) ;
#29182=CARTESIAN_POINT ( 'NONE',  ( 30.59070867143730155, 4.540774708561928108, 26.30292506078689385 ) ) ;
#29183=AXIS2_PLACEMENT_3D ( 'NONE', #62043, #52935, #30580 ) ;
#29202=EDGE_LOOP ( 'NONE', ( #19025, #39102, #57087, #95517, #75275 ) ) ;
#29263=EDGE_CURVE ( 'NONE', #45940, #98622, #2840, .T. ) ;
#29264=DIRECTION ( 'NONE',  ( 0.000000000000000000, 1.000000000000000000, -0.000000000000000000 ) ) ;
#29294=CARTESIAN_POINT ( 'NONE',  ( -0.02075734969026423599, 0.3587747205144213303, -0.08597719988137648983 ) ) ;
#29296=PLANE ( 'NONE',  #36000 ) ;
#29304=VERTEX_POINT ( 'NONE', #30134 ) ;
#29305=CARTESIAN_POINT ( 'NONE',  ( 32.51008598047019404, 5.548342165039966467, -1.163674249303449315 ) ) ;
#29316=EDGE_CURVE ( 'NONE', #54573, #31114, #76793, .T. ) ;
#29327=ORIENTED_EDGE ( 'NONE', *, *, #86332, .F. ) ;
#29367=EDGE_CURVE ( 'NONE', #50535, #93762, #3705, .T. ) ;
#29373=FACE_OUTER_BOUND ( 'NONE', #77475, .T. ) ;
#29393=FACE_OUTER_BOUND ( 'NONE', #69981, .T. ) ;
#29396=CARTESIAN_POINT ( 'NONE',  ( 282.9764569301858046, 0.3587747205144265483, 20.79159422840526616 ) ) ;
#29413=DIRECTION ( 'NONE',  ( -0.000000000000000000, -1.000000000000000000, -0.000000000000000000 ) ) ;
#29418=DIRECTION ( 'NONE',  ( -0.000000000000000000, 1.000000000000000000, -0.000000000000000000 ) ) ;
#29422=DIRECTION ( 'NONE',  ( 0.000000000000000000, 0.000000000000000000, -1.000000000000000000 ) ) ;
#29435=CARTESIAN_POINT ( 'NONE',  ( 22.02124265030973760, -4.543225279485573864, 13.95402280011862395 ) ) ;
#29453=ORIENTED_EDGE ( 'NONE', *, *, #83778, .T. ) ;
#29473=ORIENTED_EDGE ( 'NONE', *, *, #91163, .T. ) ;
#29487=ORIENTED_EDGE ( 'NONE', *, *, #88267, .F. ) ;
#29493=EDGE_CURVE ( 'NONE', #45709, #65428, #75521, .T. ) ;
#29503=VECTOR ( 'NONE', #49497, 1000.000000000000000 ) ;
#29512=ORIENTED_EDGE ( 'NONE', *, *, #56915, .F. ) ;
#29543=CARTESIAN_POINT ( 'NONE',  ( -15.82668884360736961, -6.475225279485576024, 42.07822029717483758 ) ) ;
#29573=ORIENTED_EDGE ( 'NONE', *, *, #96413, .F. ) ;
#29579=EDGE_LOOP ( 'NONE', ( #71040, #97651, #21496, #5904 ) ) ;
#29586=DIRECTION ( 'NONE',  ( 4.015954566446630556E-15, -1.000000000000000000, 1.297050502119899750E-15 ) ) ;
#29619=VECTOR ( 'NONE', #47271, 1000.000000000000000 ) ;
#29638=EDGE_CURVE ( 'NONE', #67705, #43651, #96831, .T. ) ;
#29647=ORIENTED_EDGE ( 'NONE', *, *, #67688, .T. ) ;
#29651=CARTESIAN_POINT ( 'NONE',  ( 282.9764569301858046, 0.3587747205144265483, 20.79159422840526616 ) ) ;
#29677=CARTESIAN_POINT ( 'NONE',  ( 30.46555845599590029, 5.356774720514427379, 2.040766579062852415 ) ) ;
#29683=CARTESIAN_POINT ( 'NONE',  ( 30.63256949310621735, 4.401217678701063285, 28.01131607762999565 ) ) ;
#29686=FACE_OUTER_BOUND ( 'NONE', #71253, .T. ) ;
#29697=ORIENTED_EDGE ( 'NONE', *, *, #92934, .F. ) ;
#29708=DIRECTION ( 'NONE',  ( 1.000000000000000000, 0.000000000000000000, 0.000000000000000000 ) ) ;
#29711=AXIS2_PLACEMENT_3D ( 'NONE', #64998, #4071, #42151 ) ;
#29719=EDGE_CURVE ( 'NONE', #18192, #36941, #59877, .T. ) ;
#29725=CARTESIAN_POINT ( 'NONE',  ( 3.509873074917118085, 0.3587747205144265483, 29.15869884040363758 ) ) ;
#29742=EDGE_CURVE ( 'NONE', #28007, #58159, #36516, .T. ) ;
#29748=DIRECTION ( 'NONE',  ( 0.000000000000000000, -1.000000000000000000, 0.000000000000000000 ) ) ;
#29750=CIRCLE ( 'NONE', #23286, 252.4458649670781085 ) ;
#29761=ORIENTED_EDGE ( 'NONE', *, *, #37889, .T. ) ;
#29766=DIRECTION ( 'NONE',  ( 0.000000000000000000, 0.000000000000000000, 1.000000000000000000 ) ) ;
#29798=CYLINDRICAL_SURFACE ( 'NONE', #26984, 130.2784398600581710 ) ;
#29831=LINE ( 'NONE', #84117, #76188 ) ;
#29873=CARTESIAN_POINT ( 'NONE',  ( 14.76093561896379214, -5.965225279485572685, -28.39148769130089889 ) ) ;
#29874=DIRECTION ( 'NONE',  ( 0.000000000000000000, 1.000000000000000000, -0.000000000000000000 ) ) ;
#29893=PLANE ( 'NONE',  #6537 ) ;
#29894=CARTESIAN_POINT ( 'NONE',  ( -0.02075734969026423599, 6.376774720514426953, -0.08597719988137648983 ) ) ;
#29941=EDGE_CURVE ( 'NONE', #55186, #52365, #58222, .T. ) ;
#29954=ORIENTED_EDGE ( 'NONE', *, *, #11638, .T. ) ;
#29963=ORIENTED_EDGE ( 'NONE', *, *, #12883, .F. ) ;
#29968=CARTESIAN_POINT ( 'NONE',  ( 22.81105451610979173, 1.684774720501991396, -18.46691820600746681 ) ) ;
#29969=DIRECTION ( 'NONE',  ( 0.000000000000000000, -1.000000000000000000, -0.000000000000000000 ) ) ;
#29971=DIRECTION ( 'NONE',  ( -0.000000000000000000, -1.000000000000000000, 0.000000000000000000 ) ) ;
#29976=AXIS2_PLACEMENT_3D ( 'NONE', #15550, #25164, #31279 ) ;
#30005=ORIENTED_EDGE ( 'NONE', *, *, #40993, .T. ) ;
#30022=EDGE_LOOP ( 'NONE', ( #5021, #49349, #45687, #54336 ) ) ;
#30027=LINE ( 'NONE', #38644, #22541 ) ;
#30033=ORIENTED_EDGE ( 'NONE', *, *, #10061, .T. ) ;
#30049=CARTESIAN_POINT ( 'NONE',  ( 21.89332223281681067, 4.278632354317016606, -16.39935597170616788 ) ) ;
#30053=ORIENTED_EDGE ( 'NONE', *, *, #90033, .F. ) ;
#30058=EDGE_CURVE ( 'NONE', #31628, #43602, #78776, .T. ) ;
#30060=CARTESIAN_POINT ( 'NONE',  ( -22.05275734969026047, 0.3587747205144262708, 30.51402280011862089 ) ) ;
#30096=EDGE_LOOP ( 'NONE', ( #98184, #57163, #33085, #59770 ) ) ;
#30118=CARTESIAN_POINT ( 'NONE',  ( 1.408343819019456028E-16, -6.943225279485572443, 1.149999999999999911 ) ) ;
#30120=CARTESIAN_POINT ( 'NONE',  ( -27.25988310792305214, -5.965225279485572685, 30.32664379231667695 ) ) ;
#30131=EDGE_CURVE ( 'NONE', #94426, #14476, #279, .T. ) ;
#30134=CARTESIAN_POINT ( 'NONE',  ( 0.000000000000000000, -16.94322527948557422, 3.500000000000000000 ) ) ;
#30154=CIRCLE ( 'NONE', #36606, 12.23252173913042995 ) ;
#30179=CARTESIAN_POINT ( 'NONE',  ( -24.97666371003640151, -5.965225279485592225, -15.72894043976419098 ) ) ;
#30197=CARTESIAN_POINT ( 'NONE',  ( 13.91401389203221406, 3.316774720514426456, 27.24920385068457662 ) ) ;
#30203=EDGE_CURVE ( 'NONE', #61556, #42618, #48026, .T. ) ;
#30215=CARTESIAN_POINT ( 'NONE',  ( 33.96422015159436114, 0.3587747205144265483, -7.233236000911337449 ) ) ;
#30218=CARTESIAN_POINT ( 'NONE',  ( 32.16024265030974050, 0.3587747205144265483, 14.03360796525321774 ) ) ;
#30224=CIRCLE ( 'NONE', #91787, 11.85241003308275864 ) ;
#30229=DIRECTION ( 'NONE',  ( -0.000000000000000000, 1.000000000000000000, -0.000000000000000000 ) ) ;
#30253=VECTOR ( 'NONE', #79884, 1000.000000000000114 ) ;
#30262=CARTESIAN_POINT ( 'NONE',  ( 30.53060340732036693, 4.132774720514426292, -5.153186819891554471 ) ) ;
#30271=LINE ( 'NONE', #99283, #33876 ) ;
#30276=DIRECTION ( 'NONE',  ( 1.000000000000000000, 0.000000000000000000, 0.000000000000000000 ) ) ;
#30281=AXIS2_PLACEMENT_3D ( 'NONE', #41633, #57368, #72575 ) ;
#30282=LINE ( 'NONE', #28293, #89611 ) ;
#30301=FACE_OUTER_BOUND ( 'NONE', #41948, .T. ) ;
#30315=EDGE_CURVE ( 'NONE', #47577, #77487, #75928, .T. ) ;
#30340=ORIENTED_EDGE ( 'NONE', *, *, #19140, .T. ) ;
#30345=DIRECTION ( 'NONE',  ( 1.000000000000000000, 3.639832272653110612E-15, 0.000000000000000000 ) ) ;
#30354=CARTESIAN_POINT ( 'NONE',  ( 30.53060340732035982, -1.477225279485574028, 19.84760796525321780 ) ) ;
#30364=CIRCLE ( 'NONE', #72537, 28.96799999999999287 ) ;
#30367=ADVANCED_FACE ( 'NONE', ( #7421 ), #67847, .F. ) ;
#30379=ORIENTED_EDGE ( 'NONE', *, *, #48812, .F. ) ;
#30392=EDGE_CURVE ( 'NONE', #94978, #79832, #74926, .T. ) ;
#30393=DIRECTION ( 'NONE',  ( 0.6392559695863496705, 0.000000000000000000, 0.7689940216596069522 ) ) ;
#30397=EDGE_CURVE ( 'NONE', #63837, #24351, #21688, .T. ) ;
#30408=ADVANCED_FACE ( 'NONE', ( #53120 ), #86034, .F. ) ;
#30420=CARTESIAN_POINT ( 'NONE',  ( 33.74607884027702909, 0.3587747205144265483, -4.999864028243830916 ) ) ;
#30439=AXIS2_PLACEMENT_3D ( 'NONE', #92976, #77740, #92476 ) ;
#30454=EDGE_CURVE ( 'NONE', #88744, #45969, #35019, .T. ) ;
#30477=VERTEX_POINT ( 'NONE', #23638 ) ;
#30494=CARTESIAN_POINT ( 'NONE',  ( 31.13513474936814163, 4.540774720514427543, 3.331262582247520143 ) ) ;
#30496=DIRECTION ( 'NONE',  ( -0.000000000000000000, -0.000000000000000000, 1.000000000000000000 ) ) ;
#30503=AXIS2_PLACEMENT_3D ( 'NONE', #61771, #70369, #92690 ) ;
#30513=VECTOR ( 'NONE', #4613, 1000.000000000000114 ) ;
#30532=CARTESIAN_POINT ( 'NONE',  ( 27.53860345374808105, 1.682774720514426114, 0.000000000000000000 ) ) ;
#30540=CARTESIAN_POINT ( 'NONE',  ( 26.73860345374794534, 5.058662225110310828, -7.113848178280766099 ) ) ;
#30545=DIRECTION ( 'NONE',  ( -0.000000000000000000, -1.000000000000000000, -0.000000000000000000 ) ) ;
#30552=ORIENTED_EDGE ( 'NONE', *, *, #82441, .T. ) ;
#30567=EDGE_CURVE ( 'NONE', #8495, #13454, #90052, .T. ) ;
#30572=LINE ( 'NONE', #22935, #59019 ) ;
#30579=ORIENTED_EDGE ( 'NONE', *, *, #17394, .T. ) ;
#30580=DIRECTION ( 'NONE',  ( 0.9980236263794188822, 0.000000000000000000, -0.06283980576413537855 ) ) ;
#30587=PLANE ( 'NONE',  #95060 ) ;
#30612=CARTESIAN_POINT ( 'NONE',  ( 25.90623483695386042, 5.165022820506127488, -7.573688418739351391 ) ) ;
#30633=VECTOR ( 'NONE', #97207, 1000.000000000000000 ) ;
#30650=CARTESIAN_POINT ( 'NONE',  ( 22.81105451610979173, 500000.0000000000582, -20.71691820600746681 ) ) ;
#30670=DIRECTION ( 'NONE',  ( -0.6599726524652352877, 0.000000000000000000, 0.7512896232465891000 ) ) ;
#30677=CARTESIAN_POINT ( 'NONE',  ( -11.64875734969026233, 0.3587747205144265483, 30.51402280011862089 ) ) ;
#30705=EDGE_LOOP ( 'NONE', ( #67233, #16620, #68042 ) ) ;
#30714=CIRCLE ( 'NONE', #69617, 2.040000000000000036 ) ;
#30715=LINE ( 'NONE', #62681, #17407 ) ;
#30724=AXIS2_PLACEMENT_3D ( 'NONE', #22423, #8728, #54402 ) ;
#30729=CIRCLE ( 'NONE', #61523, 2.249999999999998668 ) ;
#30759=PLANE ( 'NONE',  #53894 ) ;
#30762=CARTESIAN_POINT ( 'NONE',  ( 13.32458981842495049, 5.152774720514427642, -26.34181586963115507 ) ) ;
#30788=LINE ( 'NONE', #8949, #12315 ) ;
#30795=AXIS2_PLACEMENT_3D ( 'NONE', #80371, #33699, #56553 ) ;
#30808=CARTESIAN_POINT ( 'NONE',  ( 31.68302997424993350, 5.121054483180515149, -3.958552486145202831 ) ) ;
#30816=ORIENTED_EDGE ( 'NONE', *, *, #28364, .F. ) ;
#30831=ORIENTED_EDGE ( 'NONE', *, *, #17276, .F. ) ;
#30832=ORIENTED_EDGE ( 'NONE', *, *, #14237, .F. ) ;
#30850=DIRECTION ( 'NONE',  ( 1.251281512149627050E-16, 0.000000000000000000, -1.000000000000000000 ) ) ;
#30851=ORIENTED_EDGE ( 'NONE', *, *, #27367, .F. ) ;
#30852=DIRECTION ( 'NONE',  ( 0.000000000000000000, -1.000000000000000000, 0.000000000000000000 ) ) ;
#30854=VERTEX_POINT ( 'NONE', #66125 ) ;
#30859=FACE_OUTER_BOUND ( 'NONE', #63304, .T. ) ;
#30884=CARTESIAN_POINT ( 'NONE',  ( 13.43165536947796213, -5.965225279485592225, -28.18099828186571187 ) ) ;
#30897=PLANE ( 'NONE',  #80630 ) ;
#30898=DIRECTION ( 'NONE',  ( -0.000000000000000000, -1.000000000000000000, -0.000000000000000000 ) ) ;
#30901=EDGE_LOOP ( 'NONE', ( #17523, #84630, #95962, #90163 ) ) ;
#30935=AXIS2_PLACEMENT_3D ( 'NONE', #56194, #4397, #65322 ) ;
#30942=ORIENTED_EDGE ( 'NONE', *, *, #11628, .T. ) ;
#30949=CARTESIAN_POINT ( 'NONE',  ( 31.93426202889373400, 0.3587747205144265483, 6.907000118922838716 ) ) ;
#30956=EDGE_CURVE ( 'NONE', #48956, #79545, #95043, .T. ) ;
#30960=CARTESIAN_POINT ( 'NONE',  ( 22.81105451610979173, 1.682774720514426114, -18.46691820600746681 ) ) ;
#30993=DIRECTION ( 'NONE',  ( 0.000000000000000000, -1.000000000000000000, 0.000000000000000000 ) ) ;
#31028=LINE ( 'NONE', #92921, #64579 ) ;
#31038=ORIENTED_EDGE ( 'NONE', *, *, #53564, .T. ) ;
#31052=ORIENTED_EDGE ( 'NONE', *, *, #77510, .F. ) ;
#31063=CARTESIAN_POINT ( 'NONE',  ( 16.09828331921172051, 3.622774695106080411, -27.82448843548682049 ) ) ;
#31079=FACE_OUTER_BOUND ( 'NONE', #66083, .T. ) ;
#31093=FACE_OUTER_BOUND ( 'NONE', #67074, .T. ) ;
#31114=VERTEX_POINT ( 'NONE', #60987 ) ;
#31123=DIRECTION ( 'NONE',  ( 1.000000000000000000, 0.000000000000000000, -0.000000000000000000 ) ) ;
#31131=EDGE_CURVE ( 'NONE', #69074, #9599, #8573, .T. ) ;
#31145=LINE ( 'NONE', #61116, #36154 ) ;
#31158=CARTESIAN_POINT ( 'NONE',  ( -27.96875734969026084, 3.316774720514426456, 23.50402280011861933 ) ) ;
#31167=VECTOR ( 'NONE', #55367, 1000.000000000000000 ) ;
#31176=ORIENTED_EDGE ( 'NONE', *, *, #52088, .T. ) ;
#31178=CARTESIAN_POINT ( 'NONE',  ( 282.9764569301858046, 6.376774720514426953, 20.79159422840526616 ) ) ;
#31192=LINE ( 'NONE', #24080, #54307 ) ;
#31205=DIRECTION ( 'NONE',  ( -0.000000000000000000, 1.000000000000000000, -0.000000000000000000 ) ) ;
#31215=DIRECTION ( 'NONE',  ( 0.000000000000000000, -1.478457507934778393E-16, -1.000000000000000000 ) ) ;
#31224=FACE_OUTER_BOUND ( 'NONE', #22859, .T. ) ;
#31227=ORIENTED_EDGE ( 'NONE', *, *, #62556, .T. ) ;
#31229=DIRECTION ( 'NONE',  ( 1.000000000000000000, -0.000000000000000000, -0.000000000000000000 ) ) ;
#31231=VECTOR ( 'NONE', #56226, 1000.000000000000000 ) ;
#31232=CARTESIAN_POINT ( 'NONE',  ( 27.53860345374784657, 4.772774720514425972, -8.321925749325748356 ) ) ;
#31245=AXIS2_PLACEMENT_3D ( 'NONE', #38622, #54363, #61477 ) ;
#31254=AXIS2_PLACEMENT_3D ( 'NONE', #91874, #75152, #22345 ) ;
#31257=CARTESIAN_POINT ( 'NONE',  ( 3.509873074917118085, 0.3587747205144265483, 29.15869884040363758 ) ) ;
#31259=ADVANCED_FACE ( 'NONE', ( #18180 ), #56268, .T. ) ;
#31279=DIRECTION ( 'NONE',  ( 0.000000000000000000, 0.000000000000000000, -1.000000000000000000 ) ) ;
#31301=CIRCLE ( 'NONE', #21510, 28.96799999999999642 ) ;
#31316=CARTESIAN_POINT ( 'NONE',  ( 30.00738719773716312, 1.682774720514426114, -9.049252915307087974 ) ) ;
#31322=EDGE_LOOP ( 'NONE', ( #11495, #23554, #46622, #1397 ) ) ;
#31334=VERTEX_POINT ( 'NONE', #71482 ) ;
#31357=DIRECTION ( 'NONE',  ( 0.000000000000000000, 0.000000000000000000, 1.000000000000000000 ) ) ;
#31384=ORIENTED_EDGE ( 'NONE', *, *, #70272, .F. ) ;
#31395=DIRECTION ( 'NONE',  ( 0.7071067811865476838, 0.000000000000000000, -0.7071067811865474617 ) ) ;
#31400=CARTESIAN_POINT ( 'NONE',  ( -17.64648606763744354, -5.965225279485594001, -23.04404205923972526 ) ) ;
#31425=CARTESIAN_POINT ( 'NONE',  ( -27.96875734969026084, 6.376774720514426953, -0.08597719988137648983 ) ) ;
#31441=CARTESIAN_POINT ( 'NONE',  ( 17.51792015816173986, -5.965225279485572685, 29.01255224319336889 ) ) ;
#31456=EDGE_CURVE ( 'NONE', #94742, #61907, #51129, .T. ) ;
#31468=ORIENTED_EDGE ( 'NONE', *, *, #21069, .T. ) ;
#31470=DIRECTION ( 'NONE',  ( -0.6451914333552788428, 0.000000000000000000, -0.7640209514960704107 ) ) ;
#31472=EDGE_CURVE ( 'NONE', #46485, #67426, #8384, .T. ) ;
#31483=ORIENTED_EDGE ( 'NONE', *, *, #16939, .F. ) ;
#31493=VERTEX_POINT ( 'NONE', #75945 ) ;
#31495=CARTESIAN_POINT ( 'NONE',  ( -12.64432969575900323, -5.965225279485592225, -26.13179214487284696 ) ) ;
#31504=DIRECTION ( 'NONE',  ( -1.000000000000000000, -0.000000000000000000, 0.000000000000000000 ) ) ;
#31519=DIRECTION ( 'NONE',  ( 0.000000000000000000, 0.000000000000000000, -1.000000000000000000 ) ) ;
#31549=DIRECTION ( 'NONE',  ( 0.000000000000000000, -1.000000000000000000, 0.000000000000000000 ) ) ;
#31573=CARTESIAN_POINT ( 'NONE',  ( 3.252401863874210264, -5.965225279485592225, -29.35688408629928858 ) ) ;
#31584=VERTEX_POINT ( 'NONE', #52624 ) ;
#31586=CARTESIAN_POINT ( 'NONE',  ( 9.402885806365684829, -5.965225279485572685, 29.04108526060719342 ) ) ;
#31590=LINE ( 'NONE', #48334, #91860 ) ;
#31591=EDGE_LOOP ( 'NONE', ( #12972, #66330, #23225, #30033 ) ) ;
#31595=ORIENTED_EDGE ( 'NONE', *, *, #45361, .T. ) ;
#31597=DIRECTION ( 'NONE',  ( -0.000000000000000000, -1.000000000000000000, -0.000000000000000000 ) ) ;
#31611=FACE_OUTER_BOUND ( 'NONE', #43504, .T. ) ;
#31613=CIRCLE ( 'NONE', #42934, 251.4258649670780699 ) ;
#31615=ORIENTED_EDGE ( 'NONE', *, *, #51743, .F. ) ;
#31628=VERTEX_POINT ( 'NONE', #55638 ) ;
#31631=FACE_OUTER_BOUND ( 'NONE', #72711, .T. ) ;
#31632=VERTEX_POINT ( 'NONE', #77934 ) ;
#31646=ADVANCED_FACE ( 'NONE', ( #63763 ), #25671, .F. ) ;
#31656=CARTESIAN_POINT ( 'NONE',  ( 32.40199294184732537, -5.965225279485572685, -12.82361242714782712 ) ) ;
#31657=EDGE_CURVE ( 'NONE', #35613, #23703, #23656, .T. ) ;
#31675=ORIENTED_EDGE ( 'NONE', *, *, #5837, .T. ) ;
#31687=CARTESIAN_POINT ( 'NONE',  ( -19.37210865224160017, 0.3587747205143967943, -21.60955166348796297 ) ) ;
#31700=DIRECTION ( 'NONE',  ( 0.7512896232465891000, -1.109416176496795172E-16, 0.6599726524652352877 ) ) ;
#31714=CARTESIAN_POINT ( 'NONE',  ( -26.91814428177455909, 6.376774720514426953, 29.98490496616818746 ) ) ;
#31721=ORIENTED_EDGE ( 'NONE', *, *, #522, .F. ) ;
#31733=ORIENTED_EDGE ( 'NONE', *, *, #8785, .T. ) ;
#31754=EDGE_LOOP ( 'NONE', ( #40851, #6238, #81759, #19944 ) ) ;
#31761=ORIENTED_EDGE ( 'NONE', *, *, #99421, .T. ) ;
#31765=FACE_OUTER_BOUND ( 'NONE', #84039, .T. ) ;
#31772=CARTESIAN_POINT ( 'NONE',  ( -4.568292318365942073, 0.3587747205144265483, 30.06720597538392425 ) ) ;
#31785=FACE_OUTER_BOUND ( 'NONE', #45804, .T. ) ;
#31788=EDGE_LOOP ( 'NONE', ( #83992, #65229, #4703, #75460 ) ) ;
#31789=EDGE_CURVE ( 'NONE', #8495, #89963, #271, .T. ) ;
#31796=ADVANCED_FACE ( 'NONE', ( #34791 ), #75136, .T. ) ;
#31814=VECTOR ( 'NONE', #41408, 1000.000000000000000 ) ;
#31817=DIRECTION ( 'NONE',  ( 0.8264557562326034779, 0.000000000000000000, 0.5630016722799281448 ) ) ;
#31827=AXIS2_PLACEMENT_3D ( 'NONE', #40801, #2255, #31519 ) ;
#31830=VERTEX_POINT ( 'NONE', #50028 ) ;
#31832=DIRECTION ( 'NONE',  ( 0.000000000000000000, 0.000000000000000000, 1.000000000000000000 ) ) ;
#31843=ORIENTED_EDGE ( 'NONE', *, *, #44039, .F. ) ;
#31846=AXIS2_PLACEMENT_3D ( 'NONE', #66272, #73369, #79969 ) ;
#31858=LINE ( 'NONE', #17627, #55589 ) ;
#31884=CARTESIAN_POINT ( 'NONE',  ( -19.37210865224160017, -5.965225279485592225, -21.60955166348795586 ) ) ;
#31888=CARTESIAN_POINT ( 'NONE',  ( 6.437068816671457583, -5.965225279485592225, -28.37834077173919667 ) ) ;
#31898=CARTESIAN_POINT ( 'NONE',  ( -53.01255352321339842, 14.82721238576592704, 35.59556822165056644 ) ) ;
#31906=EDGE_CURVE ( 'NONE', #45969, #49424, #13222, .T. ) ;
#31911=CARTESIAN_POINT ( 'NONE',  ( 30.51738178340319152, 4.795593857178634956, 19.84760796525322135 ) ) ;
#31913=EDGE_CURVE ( 'NONE', #44056, #26199, #58628, .T. ) ;
#31929=CARTESIAN_POINT ( 'NONE',  ( 33.10022444407529463, 4.633339536272139902, -11.64480304263449106 ) ) ;
#31936=DIRECTION ( 'NONE',  ( -0.000000000000000000, -1.000000000000000000, -0.000000000000000000 ) ) ;
#31944=VECTOR ( 'NONE', #9406, 1000.000000000000000 ) ;
#31948=ORIENTED_EDGE ( 'NONE', *, *, #49612, .T. ) ;
#31950=ORIENTED_EDGE ( 'NONE', *, *, #10588, .T. ) ;
#31956=VECTOR ( 'NONE', #21755, 1000.000000000000000 ) ;
#31971=VECTOR ( 'NONE', #21746, 1000.000000000000000 ) ;
#31975=CARTESIAN_POINT ( 'NONE',  ( 12.53797248504841910, 0.3587747205144256601, -28.12591401903467059 ) ) ;
#31978=DIRECTION ( 'NONE',  ( -0.000000000000000000, 1.000000000000000000, 0.000000000000000000 ) ) ;
#31985=ORIENTED_EDGE ( 'NONE', *, *, #21599, .T. ) ;
#31994=CYLINDRICAL_SURFACE ( 'NONE', #69700, 1.149999999999998135 ) ;
#32030=CARTESIAN_POINT ( 'NONE',  ( 7.460719433876314532, 6.376774720514426953, -25.14146935902945046 ) ) ;
#32040=VECTOR ( 'NONE', #72466, 1000.000000000000000 ) ;
#32044=ADVANCED_FACE ( 'NONE', ( #36290 ), #68234, .T. ) ;
#32046=CARTESIAN_POINT ( 'NONE',  ( -24.97666371003640506, 0.3587747205143964613, -15.72894043976419454 ) ) ;
#32049=CARTESIAN_POINT ( 'NONE',  ( -65.05438548721848235, 3.316774720514426456, 29.49402280011861777 ) ) ;
#32058=CARTESIAN_POINT ( 'NONE',  ( 29.57907552799942508, 3.316774720514426456, 29.21818156447044501 ) ) ;
#32061=EDGE_LOOP ( 'NONE', ( #51287, #3589, #70679, #64457 ) ) ;
#32069=CARTESIAN_POINT ( 'NONE',  ( 15.03220655128660255, 5.152774720514423201, -26.94699118253568315 ) ) ;
#32090=VERTEX_POINT ( 'NONE', #52012 ) ;
#32093=ORIENTED_EDGE ( 'NONE', *, *, #52409, .F. ) ;
#32098=LINE ( 'NONE', #55958, #4987 ) ;
#32104=AXIS2_PLACEMENT_3D ( 'NONE', #51275, #82217, #81725 ) ;
#32128=EDGE_LOOP ( 'NONE', ( #70904, #98328 ) ) ;
#32131=EDGE_CURVE ( 'NONE', #11284, #19353, #81247, .T. ) ;
#32166=DIRECTION ( 'NONE',  ( 0.000000000000000000, 0.000000000000000000, 1.000000000000000000 ) ) ;
#32176=LINE ( 'NONE', #63149, #3093 ) ;
#32179=LINE ( 'NONE', #46915, #25791 ) ;
#32189=DIRECTION ( 'NONE',  ( 0.000000000000000000, 1.000000000000000000, 0.000000000000000000 ) ) ;
#32198=CARTESIAN_POINT ( 'NONE',  ( 0.000000000000000000, -6.943225279485572443, -1.149999999999999911 ) ) ;
#32199=CARTESIAN_POINT ( 'NONE',  ( -2.701720430790311767, -5.965225279485594001, -28.90526747363640681 ) ) ;
#32203=ORIENTED_EDGE ( 'NONE', *, *, #28611, .T. ) ;
#32205=CARTESIAN_POINT ( 'NONE',  ( -10.30858931494281450, 5.088649829473331110, 28.47370074478044444 ) ) ;
#32215=ORIENTED_EDGE ( 'NONE', *, *, #78973, .T. ) ;
#32219=EDGE_LOOP ( 'NONE', ( #30005, #62025, #96011, #7014 ) ) ;
#32239=CIRCLE ( 'NONE', #24125, 251.4258649670780699 ) ;
#32242=ORIENTED_EDGE ( 'NONE', *, *, #89842, .T. ) ;
#32248=CARTESIAN_POINT ( 'NONE',  ( 32.53135143123563466, -5.965225279485572685, 6.926385399448451885 ) ) ;
#32260=DIRECTION ( 'NONE',  ( 0.000000000000000000, -1.000000000000000000, 0.000000000000000000 ) ) ;
#32267=CARTESIAN_POINT ( 'NONE',  ( -19.69812919673063689, 0.3587747205143964613, -22.00173861453436430 ) ) ;
#32282=ORIENTED_EDGE ( 'NONE', *, *, #47135, .T. ) ;
#32294=CARTESIAN_POINT ( 'NONE',  ( 13.91401389203221406, -6.475225279485573360, 158.0376437107427137 ) ) ;
#32299=VERTEX_POINT ( 'NONE', #35171 ) ;
#32304=AXIS2_PLACEMENT_3D ( 'NONE', #80678, #58848, #3567 ) ;
#32307=AXIS2_PLACEMENT_3D ( 'NONE', #86881, #79263, #87383 ) ;
#32321=AXIS2_PLACEMENT_3D ( 'NONE', #78766, #72189, #56971 ) ;
#32323=DIRECTION ( 'NONE',  ( 0.000000000000000000, -1.000000000000000000, 0.000000000000000000 ) ) ;
#32342=ORIENTED_EDGE ( 'NONE', *, *, #12441, .T. ) ;
#32375=DIRECTION ( 'NONE',  ( -0.06283980576413537855, -0.000000000000000000, -0.9980236263794188822 ) ) ;
#32377=AXIS2_PLACEMENT_3D ( 'NONE', #40186, #41192, #8233 ) ;
#32385=CARTESIAN_POINT ( 'NONE',  ( 11.54156857142115911, 3.316774720514427344, -28.05134709678029381 ) ) ;
#32390=CARTESIAN_POINT ( 'NONE',  ( 14.76093561896379214, -5.965225279485572685, -26.55548769130089681 ) ) ;
#32403=AXIS2_PLACEMENT_3D ( 'NONE', #59334, #95894, #74556 ) ;
#32409=DIRECTION ( 'NONE',  ( -0.9978940991575084851, -0.000000000000000000, -0.06486421869277853025 ) ) ;
#32410=VERTEX_POINT ( 'NONE', #43286 ) ;
#32411=CARTESIAN_POINT ( 'NONE',  ( -23.71328795744024021, -5.965225279485594001, -17.58350715675015152 ) ) ;
#32423=CARTESIAN_POINT ( 'NONE',  ( -24.90875734969025501, 3.316774720514426456, 29.49402280011862487 ) ) ;
#32427=CARTESIAN_POINT ( 'NONE',  ( 30.56847537397349157, -4.007320673719170223, 25.16530555504002820 ) ) ;
#32443=FACE_OUTER_BOUND ( 'NONE', #93645, .T. ) ;
#32473=FACE_OUTER_BOUND ( 'NONE', #83606, .T. ) ;
#32494=ORIENTED_EDGE ( 'NONE', *, *, #89088, .F. ) ;
#32529=CARTESIAN_POINT ( 'NONE',  ( -41.32836283488544638, 4.132774720514426292, 39.26872235229541985 ) ) ;
#32546=LINE ( 'NONE', #39653, #20800 ) ;
#32553=DIRECTION ( 'NONE',  ( 0.000000000000000000, 0.000000000000000000, -1.000000000000000000 ) ) ;
#32574=VERTEX_POINT ( 'NONE', #587 ) ;
#32575=LINE ( 'NONE', #31573, #96517 ) ;
#32595=CARTESIAN_POINT ( 'NONE',  ( 29.68604458549361169, 6.066877414785177614, 27.51520267613161153 ) ) ;
#32602=ORIENTED_EDGE ( 'NONE', *, *, #35579, .T. ) ;
#32617=CARTESIAN_POINT ( 'NONE',  ( 26.51188133999063723, 5.098757596203291165, -7.190425899444944591 ) ) ;
#32642=PLANE ( 'NONE',  #52591 ) ;
#32649=ADVANCED_FACE ( 'NONE', ( #86329 ), #7191, .T. ) ;
#32699=VERTEX_POINT ( 'NONE', #38142 ) ;
#32720=ADVANCED_FACE ( 'NONE', ( #22897 ), #92, .T. ) ;
#32723=ORIENTED_EDGE ( 'NONE', *, *, #87456, .T. ) ;
#32744=AXIS2_PLACEMENT_3D ( 'NONE', #4725, #60019, #83831 ) ;
#32754=EDGE_CURVE ( 'NONE', #15615, #7760, #85316, .T. ) ;
#32758=CARTESIAN_POINT ( 'NONE',  ( -4.929522925832174884, 0.3587747205143967943, -28.63504101147569614 ) ) ;
#32760=CARTESIAN_POINT ( 'NONE',  ( 31.50024378385495893, 5.449202613762975211, -3.047402719862319032 ) ) ;
#32781=CARTESIAN_POINT ( 'NONE',  ( 3.252401863874210264, -5.965225279485592225, -29.35688408629928858 ) ) ;
#32791=VECTOR ( 'NONE', #22032, 1000.000000000000000 ) ;
#32793=CARTESIAN_POINT ( 'NONE',  ( 15.97264540888995299, 3.316774720514426456, -27.93485543958162864 ) ) ;
#32813=VECTOR ( 'NONE', #55884, 1000.000000000000000 ) ;
#32814=CARTESIAN_POINT ( 'NONE',  ( -28.47875734969026240, -5.965225279485572685, 26.43402280011862615 ) ) ;
#32821=ORIENTED_EDGE ( 'NONE', *, *, #53376, .F. ) ;
#32824=CARTESIAN_POINT ( 'NONE',  ( 32.42932432802503939, 0.3587747205144265483, -0.2107846672978405389 ) ) ;
#32829=CARTESIAN_POINT ( 'NONE',  ( 282.9764569301858046, 0.6647747205144264315, 20.79159422840526616 ) ) ;
#32844=LINE ( 'NONE', #62815, #23912 ) ;
#32856=DIRECTION ( 'NONE',  ( -0.000000000000000000, -1.000000000000000000, -0.000000000000000000 ) ) ;
#32860=EDGE_CURVE ( 'NONE', #36340, #47644, #68368, .T. ) ;
#32865=LINE ( 'NONE', #79022, #41330 ) ;
#32872=AXIS2_PLACEMENT_3D ( 'NONE', #94474, #15837, #24460 ) ;
#32877=ORIENTED_EDGE ( 'NONE', *, *, #52595, .F. ) ;
#32911=VECTOR ( 'NONE', #28376, 1000.000000000000000 ) ;
#32914=ORIENTED_EDGE ( 'NONE', *, *, #67221, .F. ) ;
#32916=DIRECTION ( 'NONE',  ( 0.000000000000000000, 0.000000000000000000, 1.000000000000000000 ) ) ;
#32926=EDGE_CURVE ( 'NONE', #19038, #82004, #99127, .T. ) ;
#32927=ORIENTED_EDGE ( 'NONE', *, *, #92795, .T. ) ;
#32929=CARTESIAN_POINT ( 'NONE',  ( 33.60454178612405229, 3.597323055450746487, -11.40641020892026170 ) ) ;
#32948=CARTESIAN_POINT ( 'NONE',  ( 13.59451591917074431, 3.316774720514426456, -28.23515841827053308 ) ) ;
#32953=ORIENTED_EDGE ( 'NONE', *, *, #21354, .T. ) ;
#32961=PLANE ( 'NONE',  #84992 ) ;
#32962=CARTESIAN_POINT ( 'NONE',  ( 22.02124265030973760, -6.143225279485574397, 16.20402280011862217 ) ) ;
#32964=EDGE_CURVE ( 'NONE', #68064, #99675, #5090, .T. ) ;
#32985=EDGE_CURVE ( 'NONE', #57426, #35959, #75092, .T. ) ;
#33024=ORIENTED_EDGE ( 'NONE', *, *, #21122, .F. ) ;
#33034=CARTESIAN_POINT ( 'NONE',  ( 5.097264368844747651, 3.299463065352477908, -27.56135813788838718 ) ) ;
#33036=CYLINDRICAL_SURFACE ( 'NONE', #83732, 0.8160000000000007248 ) ;
#33041=CIRCLE ( 'NONE', #11955, 3.060000000000000053 ) ;
#33063=DIRECTION ( 'NONE',  ( -0.000000000000000000, -1.000000000000000000, -0.000000000000000000 ) ) ;
#33070=CARTESIAN_POINT ( 'NONE',  ( 31.68607835968445485, 4.403148666511627951, 29.28367637967570758 ) ) ;
#33085=ORIENTED_EDGE ( 'NONE', *, *, #2142, .F. ) ;
#33101=CARTESIAN_POINT ( 'NONE',  ( 29.61836285113398048, 5.182350003425200136, 28.59212231372686119 ) ) ;
#33103=VERTEX_POINT ( 'NONE', #77583 ) ;
#33130=CARTESIAN_POINT ( 'NONE',  ( 29.73860345376319358, 4.772789318458390717, -4.021180035034620737 ) ) ;
#33131=LINE ( 'NONE', #62095, #58906 ) ;
#33138=ORIENTED_EDGE ( 'NONE', *, *, #25130, .F. ) ;
#33145=ORIENTED_EDGE ( 'NONE', *, *, #48402, .F. ) ;
#33174=ORIENTED_EDGE ( 'NONE', *, *, #85670, .T. ) ;
#33182=EDGE_CURVE ( 'NONE', #57678, #60428, #17703, .T. ) ;
#33185=DIRECTION ( 'NONE',  ( 0.5630016722799275897, -7.885106708985486076E-16, -0.8264557562326038109 ) ) ;
#33198=LINE ( 'NONE', #54542, #20115 ) ;
#33219=CARTESIAN_POINT ( 'NONE',  ( 22.81105451610979173, 1.682774720514426114, -18.46691820600746681 ) ) ;
#33221=ORIENTED_EDGE ( 'NONE', *, *, #59514, .F. ) ;
#33240=DIRECTION ( 'NONE',  ( -0.000000000000000000, -1.000000000000000000, -0.000000000000000000 ) ) ;
#33245=AXIS2_PLACEMENT_3D ( 'NONE', #78200, #53887, #54892 ) ;
#33261=DIRECTION ( 'NONE',  ( 1.000000000000000000, -0.000000000000000000, 0.000000000000000000 ) ) ;
#33266=CARTESIAN_POINT ( 'NONE',  ( -27.96875734969026084, 3.316774720514426456, 26.43402280011862615 ) ) ;
#33271=DIRECTION ( 'NONE',  ( 0.000000000000000000, 1.000000000000000000, 0.000000000000000000 ) ) ;
#33286=EDGE_CURVE ( 'NONE', #5376, #65689, #88718, .T. ) ;
#33287=CARTESIAN_POINT ( 'NONE',  ( 15.99992875909482137, 3.579156900695799060, -27.91088829768895963 ) ) ;
#33321=ORIENTED_EDGE ( 'NONE', *, *, #60826, .T. ) ;
#33330=CARTESIAN_POINT ( 'NONE',  ( 29.75286985256398253, 5.302859984505953861, 26.69689370802097272 ) ) ;
#33353=VECTOR ( 'NONE', #92539, 1000.000000000000000 ) ;
#33361=CARTESIAN_POINT ( 'NONE',  ( 30.77564450787170003, -1.477225279485574028, -9.689394075852828081 ) ) ;
#33366=EDGE_CURVE ( 'NONE', #17742, #91875, #42524, .T. ) ;
#33382=CARTESIAN_POINT ( 'NONE',  ( 29.64064043116815128, -6.475225279485573360, 28.71191112024341408 ) ) ;
#33393=CARTESIAN_POINT ( 'NONE',  ( 15.32643653063177958, 2.682774720514426559, -27.14485409495429380 ) ) ;
#33398=DIRECTION ( 'NONE',  ( 1.000000000000000000, 0.000000000000000000, -0.000000000000000000 ) ) ;
#33403=DIRECTION ( 'NONE',  ( 0.000000000000000000, 1.000000000000000000, -0.000000000000000000 ) ) ;
#33409=ORIENTED_EDGE ( 'NONE', *, *, #33990, .T. ) ;
#33411=PLANE ( 'NONE',  #84529 ) ;
#33445=VERTEX_POINT ( 'NONE', #17444 ) ;
#33449=AXIS2_PLACEMENT_3D ( 'NONE', #70303, #44975, #783 ) ;
#33456=EDGE_LOOP ( 'NONE', ( #43794, #15882, #59090, #54299 ) ) ;
#33459=B_SPLINE_CURVE_WITH_KNOTS ( 'NONE', 3,
 ( #79145, #63962, #40094, #48216 ),
 .UNSPECIFIED., .F., .F.,
 ( 4, 4 ),
 ( 0.000000000000000000, 0.0002633127703855885223 ),
 .UNSPECIFIED. ) ;
#33460=ORIENTED_EDGE ( 'NONE', *, *, #680, .T. ) ;
#33466=ORIENTED_EDGE ( 'NONE', *, *, #1568, .F. ) ;
#33474=AXIS2_PLACEMENT_3D ( 'NONE', #78186, #75816, #90552 ) ;
#33486=VECTOR ( 'NONE', #74095, 1000.000000000000000 ) ;
#33496=DIRECTION ( 'NONE',  ( -0.000000000000000000, -1.000000000000000000, -0.000000000000000000 ) ) ;
#33497=TOROIDAL_SURFACE ( 'NONE', #78893, 25.90800000000000125, 3.060000000000000053 ) ;
#33509=CARTESIAN_POINT ( 'NONE',  ( 282.9764569301858046, 6.376774720514426953, 20.79159422840526616 ) ) ;
#33516=DIRECTION ( 'NONE',  ( 0.000000000000000000, -1.000000000000000000, 0.000000000000000000 ) ) ;
#33518=CARTESIAN_POINT ( 'NONE',  ( 19.72776355195876263, 0.3587747205144265483, 28.39950002376595606 ) ) ;
#33532=CARTESIAN_POINT ( 'NONE',  ( 29.73860345376319358, 5.356774720496559894, 1.647607965253216511 ) ) ;
#33539=CARTESIAN_POINT ( 'NONE',  ( 11.51813299235546673, 6.376774720514426953, -25.01561358505534471 ) ) ;
#33543=CARTESIAN_POINT ( 'NONE',  ( 13.91401389203221406, 0.3587747205144265483, 158.0376437107427137 ) ) ;
#33548=CARTESIAN_POINT ( 'NONE',  ( -0.02075734969026423599, 0.3587747205144213303, -0.08597719988137648983 ) ) ;
#33554=EDGE_CURVE ( 'NONE', #10013, #25854, #11341, .T. ) ;
#33555=EDGE_CURVE ( 'NONE', #51332, #83129, #96567, .T. ) ;
#33562=CIRCLE ( 'NONE', #4383, 2.249999999999998668 ) ;
#33563=CARTESIAN_POINT ( 'NONE',  ( 14.74815398954886270, 3.719725396297121289, -28.39563063676393639 ) ) ;
#33571=CARTESIAN_POINT ( 'NONE',  ( 31.60706529141451426, 4.540774720514427543, 26.12024523944107202 ) ) ;
#33586=ORIENTED_EDGE ( 'NONE', *, *, #56612, .F. ) ;
#33601=CARTESIAN_POINT ( 'NONE',  ( 29.58519688192010832, 4.109013365083094449, 29.12059310601990703 ) ) ;
#33609=CARTESIAN_POINT ( 'NONE',  ( 15.97264540888995299, 3.316774720514426456, -27.93485543958162154 ) ) ;
#33613=CARTESIAN_POINT ( 'NONE',  ( 22.81105451610979173, 2.682774720514426559, -18.46691820600746681 ) ) ;
#33622=CARTESIAN_POINT ( 'NONE',  ( 25.31657025823196605, 5.174471705609984262, -8.330429310402083232 ) ) ;
#33628=ADVANCED_FACE ( 'NONE', ( #34184 ), #58032, .T. ) ;
#33632=EDGE_CURVE ( 'NONE', #99483, #71932, #66155, .T. ) ;
#33655=ORIENTED_EDGE ( 'NONE', *, *, #57147, .T. ) ;
#33672=DIRECTION ( 'NONE',  ( 0.000000000000000000, -1.000000000000000000, 0.000000000000000000 ) ) ;
#33676=CARTESIAN_POINT ( 'NONE',  ( 30.53060340732036337, 2.682774720514426559, -8.442346167188908623 ) ) ;
#33683=VERTEX_POINT ( 'NONE', #15820 ) ;
#33690=DIRECTION ( 'NONE',  ( 0.000000000000000000, 0.000000000000000000, -1.000000000000000000 ) ) ;
#33699=DIRECTION ( 'NONE',  ( 0.7071067811865474617, -0.000000000000000000, 0.7071067811865476838 ) ) ;
#33700=DIRECTION ( 'NONE',  ( 0.000000000000000000, -1.000000000000000000, 0.000000000000000000 ) ) ;
#33702=VECTOR ( 'NONE', #57571, 1000.000000000000000 ) ;
#33709=CARTESIAN_POINT ( 'NONE',  ( 19.75748517575715368, -5.965225279485572685, 28.87153971905864580 ) ) ;
#33724=ORIENTED_EDGE ( 'NONE', *, *, #57149, .T. ) ;
#33726=LINE ( 'NONE', #1779, #3751 ) ;
#33749=LINE ( 'NONE', #86525, #48937 ) ;
#33768=DIRECTION ( 'NONE',  ( -1.012712320732673682E-13, 0.000000000000000000, 1.000000000000000000 ) ) ;
#33777=DIRECTION ( 'NONE',  ( -0.000000000000000000, 0.000000000000000000, 1.000000000000000000 ) ) ;
#33778=CARTESIAN_POINT ( 'NONE',  ( 32.84232313084847732, 4.840274619473232676, -11.71291885348859196 ) ) ;
#33784=LINE ( 'NONE', #64769, #13838 ) ;
#33788=CARTESIAN_POINT ( 'NONE',  ( 15.15958133180904355, 5.152774720514426754, -26.63299148310930420 ) ) ;
#33791=FACE_OUTER_BOUND ( 'NONE', #8786, .T. ) ;
#33797=CARTESIAN_POINT ( 'NONE',  ( 15.98199071239991120, 3.493868136757070975, -27.92664602931597884 ) ) ;
#33824=VERTEX_POINT ( 'NONE', #70619 ) ;
#33831=VECTOR ( 'NONE', #59728, 1000.000000000000000 ) ;
#33838=ORIENTED_EDGE ( 'NONE', *, *, #87120, .T. ) ;
#33849=VECTOR ( 'NONE', #89715, 1000.000000000000000 ) ;
#33853=LINE ( 'NONE', #17120, #84751 ) ;
#33854=VERTEX_POINT ( 'NONE', #8223 ) ;
#33876=VECTOR ( 'NONE', #60251, 1000.000000000000000 ) ;
#33896=DIRECTION ( 'NONE',  ( -0.9161084732596777025, 0.000000000000000000, 0.4009304992412306978 ) ) ;
#33905=CIRCLE ( 'NONE', #3132, 80.18232118519038920 ) ;
#33916=FACE_OUTER_BOUND ( 'NONE', #70637, .T. ) ;
#33921=CIRCLE ( 'NONE', #7975, 6.000000000000000888 ) ;
#33924=CARTESIAN_POINT ( 'NONE',  ( -29.49875734969026198, -5.965225279485572685, 0.1180228001186258285 ) ) ;
#33930=CARTESIAN_POINT ( 'NONE',  ( 30.57287095715021508, -5.759977553574911369, 25.41160796525321786 ) ) ;
#33942=PLANE ( 'NONE',  #38407 ) ;
#33946=CIRCLE ( 'NONE', #69355, 27.94799999999999685 ) ;
#33952=ORIENTED_EDGE ( 'NONE', *, *, #52185, .F. ) ;
#33953=EDGE_LOOP ( 'NONE', ( #1365, #36873, #20619, #24295 ) ) ;
#33972=AXIS2_PLACEMENT_3D ( 'NONE', #21093, #52061, #13481 ) ;
#33986=DIRECTION ( 'NONE',  ( -0.000000000000000000, -1.000000000000000000, -0.000000000000000000 ) ) ;
#33990=EDGE_CURVE ( 'NONE', #51194, #22708, #45340, .T. ) ;
#33997=AXIS2_PLACEMENT_3D ( 'NONE', #80795, #11275, #12260 ) ;
#34022=CARTESIAN_POINT ( 'NONE',  ( 0.000000000000000000, 2.682774720514426559, 0.000000000000000000 ) ) ;
#34023=ORIENTED_EDGE ( 'NONE', *, *, #76444, .F. ) ;
#34025=CARTESIAN_POINT ( 'NONE',  ( 10.81255391457704640, 3.316774720514425123, -28.05044903510771803 ) ) ;
#34033=LINE ( 'NONE', #35537, #5290 ) ;
#34049=CARTESIAN_POINT ( 'NONE',  ( 26.73860345374794889, 5.333846218197647815, -4.449799762242919954 ) ) ;
#34053=VECTOR ( 'NONE', #81382, 1000.000000000000000 ) ;
#34059=VECTOR ( 'NONE', #97770, 1000.000000000000114 ) ;
#34068=CIRCLE ( 'NONE', #3306, 1.325999999999990298 ) ;
#34069=CARTESIAN_POINT ( 'NONE',  ( 15.99960863614694873, 3.577630190449803571, -27.91116951066526397 ) ) ;
#34110=CARTESIAN_POINT ( 'NONE',  ( 29.57907552799942508, 3.316774720514426456, 29.21818156447043791 ) ) ;
#34129=CARTESIAN_POINT ( 'NONE',  ( 25.10471210317054513, 4.943531924819384749, -10.06527829753310499 ) ) ;
#34131=EDGE_CURVE ( 'NONE', #42735, #86336, #96292, .T. ) ;
#34134=DIRECTION ( 'NONE',  ( 0.000000000000000000, 0.000000000000000000, -1.000000000000000000 ) ) ;
#34138=DIRECTION ( 'NONE',  ( 0.1254312216594016816, 0.000000000000000000, 0.9921023176230514551 ) ) ;
#34145=CARTESIAN_POINT ( 'NONE',  ( 14.76093561896379214, -6.475225279485573360, -26.55548769130089681 ) ) ;
#34179=CARTESIAN_POINT ( 'NONE',  ( -6.741682653110981249, -5.965225279485572685, 30.62569541381301619 ) ) ;
#34184=FACE_OUTER_BOUND ( 'NONE', #23612, .T. ) ;
#34207=DIRECTION ( 'NONE',  ( 0.000000000000000000, -1.000000000000000000, 0.000000000000000000 ) ) ;
#34210=VERTEX_POINT ( 'NONE', #27774 ) ;
#34215=ORIENTED_EDGE ( 'NONE', *, *, #83630, .F. ) ;
#34221=ADVANCED_FACE ( 'NONE', ( #49630 ), #12543, .F. ) ;
#34261=DIRECTION ( 'NONE',  ( 0.1827036106964188555, 0.000000000000000000, -0.9831680378442393398 ) ) ;
#34263=EDGE_CURVE ( 'NONE', #3153, #78991, #15003, .T. ) ;
#34265=FACE_OUTER_BOUND ( 'NONE', #89920, .T. ) ;
#34285=LINE ( 'NONE', #2337, #23096 ) ;
#34293=DIRECTION ( 'NONE',  ( -0.000000000000000000, 1.000000000000000000, -0.000000000000000000 ) ) ;
#34298=DIRECTION ( 'NONE',  ( 0.000000000000000000, 1.000000000000000000, -0.000000000000000000 ) ) ;
#34307=VECTOR ( 'NONE', #76282, 1000.000000000000000 ) ;
#34333=EDGE_CURVE ( 'NONE', #65938, #45794, #46600, .T. ) ;
#34352=EDGE_LOOP ( 'NONE', ( #53683, #21337, #6370, #91622 ) ) ;
#34373=ADVANCED_FACE ( 'NONE', ( #89048 ), #88049, .F. ) ;
#34374=DIRECTION ( 'NONE',  ( 0.000000000000000000, -1.000000000000000000, 0.000000000000000000 ) ) ;
#34390=CARTESIAN_POINT ( 'NONE',  ( 30.61643171304413613, 3.316774720514426456, 27.37433008668288181 ) ) ;
#34392=CARTESIAN_POINT ( 'NONE',  ( 25.61870917940689196, -5.965225279485572685, 29.49402280011862487 ) ) ;
#34394=CIRCLE ( 'NONE', #40907, 1.325999999999969647 ) ;
#34404=CARTESIAN_POINT ( 'NONE',  ( 32.16024265030974050, 0.3587747205144265483, 16.27760796525321751 ) ) ;
#34410=VERTEX_POINT ( 'NONE', #97155 ) ;
#34411=CARTESIAN_POINT ( 'NONE',  ( 29.73849889714944084, 4.772794184420478203, -4.021328304942501930 ) ) ;
#34459=CARTESIAN_POINT ( 'NONE',  ( 33.12653832968937451, 6.376774720514426953, -7.315055336576590683 ) ) ;
#34463=DIRECTION ( 'NONE',  ( 1.000000000000000000, -0.000000000000000000, -0.000000000000000000 ) ) ;
#34467=ORIENTED_EDGE ( 'NONE', *, *, #6823, .F. ) ;
#34490=ORIENTED_EDGE ( 'NONE', *, *, #57147, .F. ) ;
#34504=DIRECTION ( 'NONE',  ( 0.000000000000000000, -1.000000000000000000, 0.000000000000000000 ) ) ;
#34533=DIRECTION ( 'NONE',  ( 0.000000000000000000, 0.000000000000000000, -1.000000000000000000 ) ) ;
#34551=CARTESIAN_POINT ( 'NONE',  ( 33.08751910920749140, 4.671536413567966228, -11.65282283138775377 ) ) ;
#34562=ORIENTED_EDGE ( 'NONE', *, *, #75193, .T. ) ;
#34570=CARTESIAN_POINT ( 'NONE',  ( 14.70028154896511552, 3.418387289166273657, -28.41026772490838681 ) ) ;
#34571=VECTOR ( 'NONE', #50901, 1000.000000000000000 ) ;
#34575=CIRCLE ( 'NONE', #11894, 2.040000000000000036 ) ;
#34579=CARTESIAN_POINT ( 'NONE',  ( 31.65328924465906368, 5.892800044774432422, 28.08003312682333785 ) ) ;
#34589=ORIENTED_EDGE ( 'NONE', *, *, #69180, .T. ) ;
#34592=ORIENTED_EDGE ( 'NONE', *, *, #32754, .F. ) ;
#34596=LINE ( 'NONE', #26974, #47013 ) ;
#34610=CARTESIAN_POINT ( 'NONE',  ( 10.86264265031000775, -1.324225279485583551, -28.05717073599341660 ) ) ;
#34617=ORIENTED_EDGE ( 'NONE', *, *, #86984, .F. ) ;
#34621=DIRECTION ( 'NONE',  ( 0.000000000000000000, 0.000000000000000000, -1.000000000000000000 ) ) ;
#34633=CARTESIAN_POINT ( 'NONE',  ( -24.90875734969025501, -5.965225279485572685, 26.43402280011862615 ) ) ;
#34645=ORIENTED_EDGE ( 'NONE', *, *, #62086, .F. ) ;
#34648=CIRCLE ( 'NONE', #47619, 251.4258649670780699 ) ;
#34651=DIRECTION ( 'NONE',  ( -0.000000000000000000, -1.000000000000000000, -0.000000000000000000 ) ) ;
#34676=CARTESIAN_POINT ( 'NONE',  ( -25.92875734969026169, 5.356774720514426491, 23.50402280011861933 ) ) ;
#34693=EDGE_CURVE ( 'NONE', #44666, #3225, #1663, .T. ) ;
#34697=CARTESIAN_POINT ( 'NONE',  ( -10.26098930579144763, 5.972795536074636757, 28.98685178976001353 ) ) ;
#34740=CARTESIAN_POINT ( 'NONE',  ( 29.73860345376319358, 5.356774720514425603, -4.021109907510727943 ) ) ;
#34749=ORIENTED_EDGE ( 'NONE', *, *, #22393, .T. ) ;
#34765=CARTESIAN_POINT ( 'NONE',  ( 8.720390671794367776, 5.356774720513354460, -27.07197491334870065 ) ) ;
#34791=FACE_OUTER_BOUND ( 'NONE', #62137, .T. ) ;
#34792=FACE_OUTER_BOUND ( 'NONE', #14825, .T. ) ;
#34798=DIRECTION ( 'NONE',  ( 0.000000000000000000, 0.000000000000000000, -1.000000000000000000 ) ) ;
#34811=ADVANCED_FACE ( 'NONE', ( #24585 ), #87497, .F. ) ;
#34812=VECTOR ( 'NONE', #67429, 1000.000000000000000 ) ;
#34821=PLANE ( 'NONE',  #28551 ) ;
#34838=VERTEX_POINT ( 'NONE', #10368 ) ;
#34840=DIRECTION ( 'NONE',  ( -0.000000000000000000, -1.000000000000000000, -0.000000000000000000 ) ) ;
#34861=VERTEX_POINT ( 'NONE', #47942 ) ;
#34864=CARTESIAN_POINT ( 'NONE',  ( 8.667033081675079131, 3.316774720514425567, -27.07192531862967400 ) ) ;
#34880=EDGE_CURVE ( 'NONE', #63208, #76713, #25085, .T. ) ;
#34900=CARTESIAN_POINT ( 'NONE',  ( 0.000000000000000000, -1.473225279485573802, 3.500000000000000000 ) ) ;
#34922=CARTESIAN_POINT ( 'NONE',  ( -27.61845239340658154, 0.3587747205144057872, -10.37513603161905706 ) ) ;
#34944=DIRECTION ( 'NONE',  ( -0.000000000000000000, 1.000000000000000000, -0.000000000000000000 ) ) ;
#34951=ORIENTED_EDGE ( 'NONE', *, *, #53735, .T. ) ;
#34956=AXIS2_PLACEMENT_3D ( 'NONE', #63105, #78793, #2209 ) ;
#34960=AXIS2_PLACEMENT_3D ( 'NONE', #84711, #31936, #68994 ) ;
#34967=ORIENTED_EDGE ( 'NONE', *, *, #50409, .T. ) ;
#34974=CARTESIAN_POINT ( 'NONE',  ( -13.89275734969026388, -5.965225279485572685, 31.02402280011862246 ) ) ;
#34993=FACE_OUTER_BOUND ( 'NONE', #56854, .T. ) ;
#35019=B_SPLINE_CURVE_WITH_KNOTS ( 'NONE', 3,
 ( #23131, #16524, #30762, #94153 ),
 .UNSPECIFIED., .F., .F.,
 ( 4, 4 ),
 ( 1.734723475976806902E-18, 0.002763707449907618768 ),
 .UNSPECIFIED. ) ;
#35023=AXIS2_PLACEMENT_3D ( 'NONE', #65792, #89108, #35325 ) ;
#35040=CIRCLE ( 'NONE', #91729, 91.74549126261079834 ) ;
#35047=CARTESIAN_POINT ( 'NONE',  ( -10.11875734969026297, 6.376774720514426953, 30.51402280011862089 ) ) ;
#35052=CARTESIAN_POINT ( 'NONE',  ( 22.81105451610979173, 2.682774720514426559, -16.21691820600746681 ) ) ;
#35090=DIRECTION ( 'NONE',  ( -0.4009304992412300317, -6.845827386180410961E-16, -0.9161084732596779245 ) ) ;
#35092=AXIS2_PLACEMENT_3D ( 'NONE', #47691, #39570, #40581 ) ;
#35110=DIRECTION ( 'NONE',  ( -1.000000000000000000, 0.000000000000000000, 0.000000000000000000 ) ) ;
#35169=TOROIDAL_SURFACE ( 'NONE', #7561, 80.18232118519038920, 8.160000000000000142 ) ;
#35171=CARTESIAN_POINT ( 'NONE',  ( 27.86270917940689174, 0.3587747205144265483, 29.02104833056109001 ) ) ;
#35220=EDGE_CURVE ( 'NONE', #65068, #48069, #17881, .T. ) ;
#35226=CARTESIAN_POINT ( 'NONE',  ( 5.097264368844747651, 3.299463065352477908, -27.56135813788838718 ) ) ;
#35228=DIRECTION ( 'NONE',  ( -1.000000000000000000, -0.000000000000000000, -0.000000000000000000 ) ) ;
#35274=CARTESIAN_POINT ( 'NONE',  ( 11.25623914429021788, 3.316774720514424235, -27.04805245727492391 ) ) ;
#35284=CARTESIAN_POINT ( 'NONE',  ( 9.843544857143434967, -5.965225279485572685, -27.49819965379373343 ) ) ;
#35290=DIRECTION ( 'NONE',  ( 0.1489078231574191002, -6.845827386180410961E-16, -0.9888510809027407644 ) ) ;
#35305=CARTESIAN_POINT ( 'NONE',  ( -27.15721599100127648, 6.376774720514425177, -10.22292133548837256 ) ) ;
#35313=ORIENTED_EDGE ( 'NONE', *, *, #47248, .T. ) ;
#35320=ORIENTED_EDGE ( 'NONE', *, *, #58597, .T. ) ;
#35325=DIRECTION ( 'NONE',  ( 0.000000000000000000, 0.000000000000000000, -1.000000000000000000 ) ) ;
#35332=DIRECTION ( 'NONE',  ( 0.000000000000000000, 1.000000000000000000, 0.000000000000000000 ) ) ;
#35361=EDGE_LOOP ( 'NONE', ( #56507, #69892, #18870, #62775 ) ) ;
#35385=EDGE_CURVE ( 'NONE', #2131, #55067, #13233, .T. ) ;
#35402=EDGE_CURVE ( 'NONE', #82156, #89020, #11742, .T. ) ;
#35425=VERTEX_POINT ( 'NONE', #36576 ) ;
#35433=DIRECTION ( 'NONE',  ( -0.1875268396392987258, 0.000000000000000000, -0.9822594791677485837 ) ) ;
#35447=LINE ( 'NONE', #74008, #10600 ) ;
#35449=CYLINDRICAL_SURFACE ( 'NONE', #94641, 3.060000000000000053 ) ;
#35453=CIRCLE ( 'NONE', #79247, 1.325999999999990298 ) ;
#35465=DIRECTION ( 'NONE',  ( 0.000000000000000000, -1.000000000000000000, 0.000000000000000000 ) ) ;
#35492=LINE ( 'NONE', #43601, #50826 ) ;
#35501=DIRECTION ( 'NONE',  ( -0.000000000000000000, 1.000000000000000000, -0.000000000000000000 ) ) ;
#35509=CARTESIAN_POINT ( 'NONE',  ( 5.851028665930490646, 3.316774720514426011, -27.43979700150094558 ) ) ;
#35510=DIRECTION ( 'NONE',  ( 0.000000000000000000, 1.000000000000000000, -0.000000000000000000 ) ) ;
#35519=VECTOR ( 'NONE', #19683, 1000.000000000000000 ) ;
#35520=DIRECTION ( 'NONE',  ( 0.000000000000000000, 1.000000000000000000, 0.000000000000000000 ) ) ;
#35525=DIRECTION ( 'NONE',  ( -0.000000000000000000, -1.000000000000000000, -0.000000000000000000 ) ) ;
#35526=DIRECTION ( 'NONE',  ( 0.000000000000000000, -0.7071067811865513475, 0.7071067811865437980 ) ) ;
#35537=CARTESIAN_POINT ( 'NONE',  ( -24.90875734969025501, -5.965225279485572685, 30.51402280011862089 ) ) ;
#35548=CARTESIAN_POINT ( 'NONE',  ( 3.252401863874215593, 0.3587747205143964613, -29.35688408629929214 ) ) ;
#35564=DIRECTION ( 'NONE',  ( -0.000000000000000000, -1.000000000000000000, -0.000000000000000000 ) ) ;
#35571=ORIENTED_EDGE ( 'NONE', *, *, #90946, .T. ) ;
#35577=AXIS2_PLACEMENT_3D ( 'NONE', #83879, #20976, #14360 ) ;
#35579=EDGE_CURVE ( 'NONE', #654, #48919, #47087, .T. ) ;
#35584=CIRCLE ( 'NONE', #4804, 83.21379343477475743 ) ;
#35597=VERTEX_POINT ( 'NONE', #71426 ) ;
#35613=VERTEX_POINT ( 'NONE', #88151 ) ;
#35625=DIRECTION ( 'NONE',  ( 0.000000000000000000, 1.000000000000000000, 0.000000000000000000 ) ) ;
#35638=EDGE_CURVE ( 'NONE', #30854, #16991, #50093, .T. ) ;
#35648=CARTESIAN_POINT ( 'NONE',  ( 14.76093561896379214, -5.965225279485572685, -27.88148769130088667 ) ) ;
#35656=AXIS2_PLACEMENT_3D ( 'NONE', #22800, #1500, #53786 ) ;
#35670=LINE ( 'NONE', #56649, #11045 ) ;
#35692=EDGE_LOOP ( 'NONE', ( #10085, #6612, #89511, #5032 ) ) ;
#35702=VECTOR ( 'NONE', #80769, 1000.000000000000000 ) ;
#35706=ORIENTED_EDGE ( 'NONE', *, *, #76878, .F. ) ;
#35726=LINE ( 'NONE', #5762, #92279 ) ;
#35729=AXIS2_PLACEMENT_3D ( 'NONE', #1870, #10979, #19079 ) ;
#35733=VERTEX_POINT ( 'NONE', #5893 ) ;
#35739=VERTEX_POINT ( 'NONE', #51584 ) ;
#35746=DIRECTION ( 'NONE',  ( 0.000000000000000000, -1.000000000000000000, 0.000000000000000000 ) ) ;
#35753=ORIENTED_EDGE ( 'NONE', *, *, #78084, .F. ) ;
#35763=CARTESIAN_POINT ( 'NONE',  ( 32.42932432802503939, -5.965225279485572685, -0.2107846672978405389 ) ) ;
#35768=ORIENTED_EDGE ( 'NONE', *, *, #10061, .F. ) ;
#35770=CARTESIAN_POINT ( 'NONE',  ( 9.214646252612421762, 3.316774720514544583, -27.04520690475792222 ) ) ;
#35785=CARTESIAN_POINT ( 'NONE',  ( 30.00738719773716312, -1.477225279485574028, -9.049252915307087974 ) ) ;
#35800=CARTESIAN_POINT ( 'NONE',  ( 30.56408408303725466, -2.971977064529662371, 24.90465250750439097 ) ) ;
#35801=DIRECTION ( 'NONE',  ( 0.000000000000000000, 0.000000000000000000, 1.000000000000000000 ) ) ;
#35805=CARTESIAN_POINT ( 'NONE',  ( 32.73857899460460175, -6.475225279485576024, -13.20677013500359820 ) ) ;
#35806=CARTESIAN_POINT ( 'NONE',  ( 30.59299694858157892, 5.371884064401012182, 26.41087035901067637 ) ) ;
#35826=VERTEX_POINT ( 'NONE', #12012 ) ;
#35848=VECTOR ( 'NONE', #32409, 1000.000000000000114 ) ;
#35854=VERTEX_POINT ( 'NONE', #60202 ) ;
#35869=AXIS2_PLACEMENT_3D ( 'NONE', #24404, #41149, #2092 ) ;
#35874=ADVANCED_FACE ( 'NONE', ( #31224 ), #61696, .F. ) ;
#35888=CARTESIAN_POINT ( 'NONE',  ( -65.05438548721848235, 5.356774720514425603, 27.45402280011862572 ) ) ;
#35894=CARTESIAN_POINT ( 'NONE',  ( -24.90875734969025501, -6.475225279485573360, 30.00402280011862288 ) ) ;
#35900=ORIENTED_EDGE ( 'NONE', *, *, #74274, .F. ) ;
#35914=CARTESIAN_POINT ( 'NONE',  ( 8.255033872309153864, -6.475225279485571583, -27.10684724722607442 ) ) ;
#35918=CARTESIAN_POINT ( 'NONE',  ( 3.509873074917118085, -5.965225279485572685, 29.15869884040363758 ) ) ;
#35937=PLANE ( 'NONE',  #57553 ) ;
#35959=VERTEX_POINT ( 'NONE', #26117 ) ;
#35992=CARTESIAN_POINT ( 'NONE',  ( 6.620851319379956301, -6.475225279485576024, -27.30756699305372592 ) ) ;
#36000=AXIS2_PLACEMENT_3D ( 'NONE', #93186, #69864, #37912 ) ;
#36007=CYLINDRICAL_SURFACE ( 'NONE', #28193, 3.349999999999998757 ) ;
#36009=EDGE_CURVE ( 'NONE', #85275, #20569, #40636, .T. ) ;
#36015=CYLINDRICAL_SURFACE ( 'NONE', #17200, 1.325999999999969647 ) ;
#36035=CIRCLE ( 'NONE', #74915, 25.90800000000000125 ) ;
#36038=CARTESIAN_POINT ( 'NONE',  ( 31.62416306531753918, 4.295372699094516022, 26.87458401151571508 ) ) ;
#36044=EDGE_CURVE ( 'NONE', #55518, #9188, #56080, .T. ) ;
#36045=LINE ( 'NONE', #3120, #85562 ) ;
#36052=CARTESIAN_POINT ( 'NONE',  ( 30.55456828421201720, -1.252966014080255430, 24.28055799599966846 ) ) ;
#36067=VECTOR ( 'NONE', #52606, 1000.000000000000114 ) ;
#36125=VECTOR ( 'NONE', #92426, 1000.000000000000227 ) ;
#36130=DIRECTION ( 'NONE',  ( 0.000000000000000000, -1.000000000000000000, 0.000000000000000000 ) ) ;
#36138=EDGE_CURVE ( 'NONE', #44563, #17901, #9834, .T. ) ;
#36154=VECTOR ( 'NONE', #53510, 999.9999999999998863 ) ;
#36160=DIRECTION ( 'NONE',  ( 0.06283980576413539243, 0.000000000000000000, 0.9980236263794188822 ) ) ;
#36167=CARTESIAN_POINT ( 'NONE',  ( 30.93860345374796594, 0.6647747205144264315, 19.84760796525321780 ) ) ;
#36170=LINE ( 'NONE', #67626, #34571 ) ;
#36172=EDGE_CURVE ( 'NONE', #70078, #41837, #77755, .T. ) ;
#36175=CARTESIAN_POINT ( 'NONE',  ( 30.93860345374796594, -5.965225279485573573, 28.83647319851474933 ) ) ;
#36191=CARTESIAN_POINT ( 'NONE',  ( -24.90875734969025501, 3.316774720514426456, 30.51402280011862089 ) ) ;
#36222=LINE ( 'NONE', #59070, #25801 ) ;
#36223=CARTESIAN_POINT ( 'NONE',  ( -25.92875734969026169, 5.356774720514426491, 24.50402280011861933 ) ) ;
#36235=LINE ( 'NONE', #50461, #40121 ) ;
#36265=EDGE_CURVE ( 'NONE', #38164, #33103, #32098, .T. ) ;
#36266=CARTESIAN_POINT ( 'NONE',  ( -11.64875734969026233, -5.965225279485572685, 30.51402280011862089 ) ) ;
#36271=CIRCLE ( 'NONE', #44388, 129.7684398600581233 ) ;
#36280=CARTESIAN_POINT ( 'NONE',  ( 32.16024265030974050, 0.3587747205144265483, 16.27760796525321751 ) ) ;
#36285=DIRECTION ( 'NONE',  ( 0.9685340172660599212, 0.000000000000000000, -0.2488812114211667037 ) ) ;
#36290=FACE_OUTER_BOUND ( 'NONE', #75644, .T. ) ;
#36298=DIRECTION ( 'NONE',  ( -0.000000000000000000, -0.000000000000000000, -1.000000000000000000 ) ) ;
#36302=CARTESIAN_POINT ( 'NONE',  ( 31.21773176006472283, 5.300046855345732943, 2.139914057118826651 ) ) ;
#36307=CARTESIAN_POINT ( 'NONE',  ( 29.70909950603835625, 4.224653874731083114, 27.99670097642948008 ) ) ;
#36319=B_SPLINE_CURVE_WITH_KNOTS ( 'NONE', 3,
 ( #59032, #66164, #51414, #91448, #44306, #98061 ),
 .UNSPECIFIED., .F., .F.,
 ( 4, 2, 4 ),
 ( 0.000000000000000000, 0.0005107898210030669545, 0.001021579642006133909 ),
 .UNSPECIFIED. ) ;
#36330=ORIENTED_EDGE ( 'NONE', *, *, #8611, .F. ) ;
#36340=VERTEX_POINT ( 'NONE', #2672 ) ;
#36345=VERTEX_POINT ( 'NONE', #33609 ) ;
#36346=DIRECTION ( 'NONE',  ( 0.000000000000000000, 0.000000000000000000, -1.000000000000000000 ) ) ;
#36352=ORIENTED_EDGE ( 'NONE', *, *, #72695, .F. ) ;
#36356=ORIENTED_EDGE ( 'NONE', *, *, #98582, .F. ) ;
#36369=ORIENTED_EDGE ( 'NONE', *, *, #9242, .T. ) ;
#36373=ORIENTED_EDGE ( 'NONE', *, *, #43321, .T. ) ;
#36393=LINE ( 'NONE', #35894, #36950 ) ;
#36402=CARTESIAN_POINT ( 'NONE',  ( 33.74607884027702909, 0.3587747205144265483, -4.999864028243830916 ) ) ;
#36408=ORIENTED_EDGE ( 'NONE', *, *, #62637, .F. ) ;
#36421=CARTESIAN_POINT ( 'NONE',  ( 32.45853543194704116, -5.965225279485572685, 9.169203677920338080 ) ) ;
#36429=CARTESIAN_POINT ( 'NONE',  ( -22.05275734969026047, 0.3587747205144262708, 31.02402280011862246 ) ) ;
#36443=ORIENTED_EDGE ( 'NONE', *, *, #10615, .F. ) ;
#36444=VERTEX_POINT ( 'NONE', #99715 ) ;
#36454=ORIENTED_EDGE ( 'NONE', *, *, #47832, .T. ) ;
#36471=EDGE_CURVE ( 'NONE', #92240, #76194, #7380, .T. ) ;
#36482=DIRECTION ( 'NONE',  ( -1.000000000000000000, 0.000000000000000000, -0.000000000000000000 ) ) ;
#36496=FACE_OUTER_BOUND ( 'NONE', #76084, .T. ) ;
#36502=EDGE_CURVE ( 'NONE', #23842, #73137, #87643, .T. ) ;
#36506=ORIENTED_EDGE ( 'NONE', *, *, #38073, .F. ) ;
#36510=PLANE ( 'NONE',  #43981 ) ;
#36516=LINE ( 'NONE', #98405, #48244 ) ;
#36532=LINE ( 'NONE', #14691, #23392 ) ;
#36541=VECTOR ( 'NONE', #3245, 1000.000000000000000 ) ;
#36557=CARTESIAN_POINT ( 'NONE',  ( 13.91401389203221406, 6.376774720514426953, 27.24920385068457662 ) ) ;
#36562=VECTOR ( 'NONE', #66659, 1000.000000000000000 ) ;
#36568=ORIENTED_EDGE ( 'NONE', *, *, #59411, .T. ) ;
#36576=CARTESIAN_POINT ( 'NONE',  ( -29.49875734969025842, -5.965225279485572685, 25.61802280011862720 ) ) ;
#36577=DIRECTION ( 'NONE',  ( 0.000000000000000000, 0.000000000000000000, -1.000000000000000000 ) ) ;
#36601=VECTOR ( 'NONE', #39607, 1000.000000000000000 ) ;
#36606=AXIS2_PLACEMENT_3D ( 'NONE', #82319, #89440, #96054 ) ;
#36630=CARTESIAN_POINT ( 'NONE',  ( -28.98875734969026396, 3.316774720514426456, -0.08597719988137648983 ) ) ;
#36642=CARTESIAN_POINT ( 'NONE',  ( 10.59058046163345423, 3.703784075859317682, -26.99573265033922453 ) ) ;
#36649=DIRECTION ( 'NONE',  ( -0.000000000000000000, 0.000000000000000000, 1.000000000000000000 ) ) ;
#36663=DIRECTION ( 'NONE',  ( 0.6599726524652352877, 0.000000000000000000, -0.7512896232465891000 ) ) ;
#36694=CARTESIAN_POINT ( 'NONE',  ( 31.74473449900405697, 4.976825198871215328, -4.259190951192157293 ) ) ;
#36696=ORIENTED_EDGE ( 'NONE', *, *, #31131, .F. ) ;
#36706=EDGE_CURVE ( 'NONE', #38639, #71522, #90012, .T. ) ;
#36725=ORIENTED_EDGE ( 'NONE', *, *, #62439, .T. ) ;
#36728=ORIENTED_EDGE ( 'NONE', *, *, #10615, .T. ) ;
#36750=EDGE_CURVE ( 'NONE', #47172, #50535, #19994, .T. ) ;
#36769=VERTEX_POINT ( 'NONE', #68172 ) ;
#36790=CIRCLE ( 'NONE', #48169, 1.020000000000000018 ) ;
#36804=CARTESIAN_POINT ( 'NONE',  ( 29.70397367894831930, 3.853389802531868469, 28.15179473738050220 ) ) ;
#36807=DIRECTION ( 'NONE',  ( 0.000000000000000000, 0.000000000000000000, -1.000000000000000000 ) ) ;
#36808=ORIENTED_EDGE ( 'NONE', *, *, #86089, .T. ) ;
#36809=AXIS2_PLACEMENT_3D ( 'NONE', #40625, #2566, #48238 ) ;
#36810=ORIENTED_EDGE ( 'NONE', *, *, #84278, .T. ) ;
#36828=ORIENTED_EDGE ( 'NONE', *, *, #95508, .F. ) ;
#36853=ORIENTED_EDGE ( 'NONE', *, *, #23039, .T. ) ;
#36855=ORIENTED_EDGE ( 'NONE', *, *, #23308, .T. ) ;
#36867=ORIENTED_EDGE ( 'NONE', *, *, #55309, .T. ) ;
#36868=ORIENTED_EDGE ( 'NONE', *, *, #56423, .F. ) ;
#36873=ORIENTED_EDGE ( 'NONE', *, *, #73705, .T. ) ;
#36874=DIRECTION ( 'NONE',  ( 0.000000000000000000, 0.000000000000000000, -1.000000000000000000 ) ) ;
#36889=VECTOR ( 'NONE', #24835, 1000.000000000000000 ) ;
#36906=VERTEX_POINT ( 'NONE', #1160 ) ;
#36908=FACE_OUTER_BOUND ( 'NONE', #74484, .T. ) ;
#36915=LINE ( 'NONE', #5961, #79962 ) ;
#36919=ORIENTED_EDGE ( 'NONE', *, *, #68012, .F. ) ;
#36934=DIRECTION ( 'NONE',  ( -1.000000000000000000, 0.000000000000000000, 0.000000000000000000 ) ) ;
#36938=ADVANCED_FACE ( 'NONE', ( #2173, #31093 ), #62562, .T. ) ;
#36941=VERTEX_POINT ( 'NONE', #93487 ) ;
#36947=EDGE_CURVE ( 'NONE', #23691, #4955, #16872, .T. ) ;
#36950=VECTOR ( 'NONE', #66862, 1000.000000000000000 ) ;
#36953=CARTESIAN_POINT ( 'NONE',  ( -25.92875734969026524, 6.376774720514426953, -0.08597719988137648983 ) ) ;
#36964=ORIENTED_EDGE ( 'NONE', *, *, #94859, .T. ) ;
#36971=EDGE_CURVE ( 'NONE', #89124, #21600, #85889, .T. ) ;
#36978=DIRECTION ( 'NONE',  ( 1.000000000000000000, 4.015979463811607402E-15, 0.000000000000000000 ) ) ;
#36989=DIRECTION ( 'NONE',  ( 0.000000000000000000, -1.000000000000000000, 0.000000000000000000 ) ) ;
#36992=CARTESIAN_POINT ( 'NONE',  ( 11.41483471809167405, -6.475225279485574248, -27.05170832580397189 ) ) ;
#36997=ORIENTED_EDGE ( 'NONE', *, *, #11451, .T. ) ;
#37036=ORIENTED_EDGE ( 'NONE', *, *, #39279, .T. ) ;
#37043=CARTESIAN_POINT ( 'NONE',  ( 282.9764569301858046, 1.682774720514426114, 20.79159422840526616 ) ) ;
#37049=CARTESIAN_POINT ( 'NONE',  ( -24.55517127435777169, -5.965225279485592225, -15.44180958690142802 ) ) ;
#37069=EDGE_LOOP ( 'NONE', ( #60220, #86389, #64328, #36443, #7169 ) ) ;
#37075=FACE_OUTER_BOUND ( 'NONE', #61574, .T. ) ;
#37087=DIRECTION ( 'NONE',  ( 0.000000000000000000, 0.000000000000000000, 1.000000000000000000 ) ) ;
#37104=VECTOR ( 'NONE', #82842, 1000.000000000000000 ) ;
#37132=ORIENTED_EDGE ( 'NONE', *, *, #40918, .T. ) ;
#37142=CYLINDRICAL_SURFACE ( 'NONE', #77152, 84.48086791635432746 ) ;
#37143=ADVANCED_FACE ( 'NONE', ( #70434 ), #62842, .T. ) ;
#37160=TOROIDAL_SURFACE ( 'NONE', #93874, 80.18232118519038920, 9.179999999999999716 ) ;
#37164=CIRCLE ( 'NONE', #50149, 0.8160000000000007248 ) ;
#37175=VERTEX_POINT ( 'NONE', #55225 ) ;
#37179=CARTESIAN_POINT ( 'NONE',  ( 20.65867867180746487, 4.278699498676136415, -17.77077369076281599 ) ) ;
#37200=ORIENTED_EDGE ( 'NONE', *, *, #48468, .F. ) ;
#37209=DIRECTION ( 'NONE',  ( 0.000000000000000000, 1.000000000000000000, 0.000000000000000000 ) ) ;
#37210=DIRECTION ( 'NONE',  ( -0.000000000000000000, -1.000000000000000000, -0.000000000000000000 ) ) ;
#37212=ADVANCED_FACE ( 'NONE', ( #42002 ), #3439, .T. ) ;
#37214=DIRECTION ( 'NONE',  ( -0.000000000000000000, -1.000000000000000000, -0.000000000000000000 ) ) ;
#37217=CARTESIAN_POINT ( 'NONE',  ( -27.83739072329610664, -5.965225279485592225, -8.084349702057698650 ) ) ;
#37222=ORIENTED_EDGE ( 'NONE', *, *, #76201, .F. ) ;
#37223=ORIENTED_EDGE ( 'NONE', *, *, #55005, .T. ) ;
#37233=CARTESIAN_POINT ( 'NONE',  ( 32.73857899460458754, -5.965225279485572685, -13.20677013500358399 ) ) ;
#37247=AXIS2_PLACEMENT_3D ( 'NONE', #5098, #45667, #75102 ) ;
#37248=DIRECTION ( 'NONE',  ( -1.000000000000000000, -0.000000000000000000, -0.000000000000000000 ) ) ;
#37254=FACE_OUTER_BOUND ( 'NONE', #49626, .T. ) ;
#37271=CARTESIAN_POINT ( 'NONE',  ( 13.91401389203221406, -5.965225279485572685, 27.75920385068456042 ) ) ;
#37275=ADVANCED_FACE ( 'NONE', ( #96271 ), #79538, .T. ) ;
#37281=CARTESIAN_POINT ( 'NONE',  ( -24.90875734969025501, 5.356774720514425603, 27.45402280011862572 ) ) ;
#37289=EDGE_CURVE ( 'NONE', #63916, #59325, #80540, .T. ) ;
#37295=LINE ( 'NONE', #59140, #100227 ) ;
#37305=CARTESIAN_POINT ( 'NONE',  ( 29.72852606603716552, 4.950008708102185295, 27.41398129243886217 ) ) ;
#37343=EDGE_LOOP ( 'NONE', ( #5233, #3912, #27521, #79026 ) ) ;
#37386=CARTESIAN_POINT ( 'NONE',  ( 22.02124265030973760, 5.356774720514425603, 16.20402280011862217 ) ) ;
#37391=AXIS2_PLACEMENT_3D ( 'NONE', #1533, #63447, #24854 ) ;
#37434=FACE_OUTER_BOUND ( 'NONE', #22006, .T. ) ;
#37440=CARTESIAN_POINT ( 'NONE',  ( -41.32836283488544638, 4.132774720514426292, 39.26872235229541985 ) ) ;
#37448=VERTEX_POINT ( 'NONE', #19632 ) ;
#37449=ORIENTED_EDGE ( 'NONE', *, *, #100404, .F. ) ;
#37481=VERTEX_POINT ( 'NONE', #93132 ) ;
#37496=B_SPLINE_CURVE_WITH_KNOTS ( 'NONE', 3,
 ( #58566, #89506, #81897, #67186, #98101, #49968 ),
 .UNSPECIFIED., .F., .F.,
 ( 4, 2, 4 ),
 ( 0.002936590050694640099, 0.005175337996430707382, 0.007414085942166775967 ),
 .UNSPECIFIED. ) ;
#37499=LINE ( 'NONE', #13646, #83807 ) ;
#37500=CARTESIAN_POINT ( 'NONE',  ( 12.28518416766336507, 5.152774720514428530, -26.38359849988869144 ) ) ;
#37507=AXIS2_PLACEMENT_3D ( 'NONE', #40020, #87191, #33398 ) ;
#37522=CARTESIAN_POINT ( 'NONE',  ( 13.37813176289109407, 2.682774720514426559, -27.17274205579463242 ) ) ;
#37541=CARTESIAN_POINT ( 'NONE',  ( 30.56047832681638354, -2.297196155479634516, 24.67598410064775649 ) ) ;
#37545=EDGE_CURVE ( 'NONE', #23928, #7917, #49074, .T. ) ;
#37553=DIRECTION ( 'NONE',  ( 0.000000000000000000, 3.056206645085457922E-15, -1.000000000000000000 ) ) ;
#37555=VECTOR ( 'NONE', #36482, 1000.000000000000000 ) ;
#37593=VERTEX_POINT ( 'NONE', #78909 ) ;
#37596=FACE_OUTER_BOUND ( 'NONE', #77982, .T. ) ;
#37599=ORIENTED_EDGE ( 'NONE', *, *, #74274, .T. ) ;
#37637=ORIENTED_EDGE ( 'NONE', *, *, #65166, .T. ) ;
#37662=CARTESIAN_POINT ( 'NONE',  ( 30.93860345374796594, -6.475225279485573360, 29.23160796525321814 ) ) ;
#37664=DIRECTION ( 'NONE',  ( -0.06283980576413537855, -0.000000000000000000, -0.9980236263794188822 ) ) ;
#37666=DIRECTION ( 'NONE',  ( -9.779078418496698369E-14, 0.000000000000000000, -1.000000000000000000 ) ) ;
#37670=AXIS2_PLACEMENT_3D ( 'NONE', #83524, #29748, #795 ) ;
#37672=CARTESIAN_POINT ( 'NONE',  ( 20.59899778430702710, 4.215349365190572684, -17.99869025002255896 ) ) ;
#37686=CARTESIAN_POINT ( 'NONE',  ( 16.15056352287344410, 5.152774720514413431, -27.77856273171768109 ) ) ;
#37687=ORIENTED_EDGE ( 'NONE', *, *, #78652, .T. ) ;
#37702=CARTESIAN_POINT ( 'NONE',  ( -20.27875734969026311, 3.456774720514426136, 24.00402280011862288 ) ) ;
#37720=PLANE ( 'NONE',  #54763 ) ;
#37733=ADVANCED_FACE ( 'NONE', ( #71319 ), #71822, .F. ) ;
#37747=ORIENTED_EDGE ( 'NONE', *, *, #47248, .F. ) ;
#37757=DIRECTION ( 'NONE',  ( -0.000000000000000000, 1.000000000000000000, -0.000000000000000000 ) ) ;
#37775=LINE ( 'NONE', #76318, #43657 ) ;
#37786=CIRCLE ( 'NONE', #96100, 0.8160000000000008358 ) ;
#37842=VERTEX_POINT ( 'NONE', #4306 ) ;
#37861=ADVANCED_FACE ( 'NONE', ( #68913 ), #84631, .F. ) ;
#37863=VERTEX_POINT ( 'NONE', #77508 ) ;
#37889=EDGE_CURVE ( 'NONE', #95525, #31584, #31301, .T. ) ;
#37906=EDGE_CURVE ( 'NONE', #12577, #64113, #6517, .T. ) ;
#37910=DIRECTION ( 'NONE',  ( 1.000000000000000000, 4.218088402344531063E-15, 0.000000000000000000 ) ) ;
#37912=DIRECTION ( 'NONE',  ( -1.000000000000000000, 0.000000000000000000, -0.000000000000000000 ) ) ;
#37920=FACE_OUTER_BOUND ( 'NONE', #32128, .T. ) ;
#37946=ORIENTED_EDGE ( 'NONE', *, *, #82767, .F. ) ;
#37959=ORIENTED_EDGE ( 'NONE', *, *, #98468, .F. ) ;
#37962=EDGE_CURVE ( 'NONE', #22769, #22324, #83631, .T. ) ;
#37970=EDGE_CURVE ( 'NONE', #37842, #22614, #23222, .T. ) ;
#37979=ORIENTED_EDGE ( 'NONE', *, *, #83260, .F. ) ;
#37989=DIRECTION ( 'NONE',  ( -0.000000000000000000, 1.000000000000000000, -0.000000000000000000 ) ) ;
#37996=EDGE_CURVE ( 'NONE', #50697, #22271, #33853, .T. ) ;
#38009=DIRECTION ( 'NONE',  ( -0.000000000000000000, -1.000000000000000000, -0.000000000000000000 ) ) ;
#38036=LINE ( 'NONE', #31425, #49969 ) ;
#38041=ORIENTED_EDGE ( 'NONE', *, *, #78084, .T. ) ;
#38050=CARTESIAN_POINT ( 'NONE',  ( -4.568292318365942073, 0.3587747205144265483, 30.06720597538392425 ) ) ;
#38058=VERTEX_POINT ( 'NONE', #63833 ) ;
#38072=ORIENTED_EDGE ( 'NONE', *, *, #83630, .T. ) ;
#38073=EDGE_CURVE ( 'NONE', #68279, #37863, #31858, .T. ) ;
#38074=DIRECTION ( 'NONE',  ( 0.000000000000000000, 0.000000000000000000, -1.000000000000000000 ) ) ;
#38084=ADVANCED_FACE ( 'NONE', ( #12010 ), #66824, .F. ) ;
#38107=LINE ( 'NONE', #99987, #60890 ) ;
#38123=ORIENTED_EDGE ( 'NONE', *, *, #88571, .F. ) ;
#38131=CARTESIAN_POINT ( 'NONE',  ( 10.86431179149619908, 3.316774720514763075, -28.05678185015766246 ) ) ;
#38132=DIRECTION ( 'NONE',  ( 0.000000000000000000, 0.000000000000000000, -1.000000000000000000 ) ) ;
#38133=EDGE_CURVE ( 'NONE', #43478, #25854, #75045, .T. ) ;
#38139=FACE_OUTER_BOUND ( 'NONE', #7525, .T. ) ;
#38142=CARTESIAN_POINT ( 'NONE',  ( 33.12653832968932477, -5.965225279485572685, -7.315055336576597789 ) ) ;
#38151=CARTESIAN_POINT ( 'NONE',  ( 29.73860345376316872, 5.356774720514427379, 17.30421508979850387 ) ) ;
#38157=CYLINDRICAL_SURFACE ( 'NONE', #30724, 2.499999999999998668 ) ;
#38164=VERTEX_POINT ( 'NONE', #42978 ) ;
#38203=CARTESIAN_POINT ( 'NONE',  ( 32.66876533700882845, -5.965225279485572685, -12.58926540598385557 ) ) ;
#38206=VERTEX_POINT ( 'NONE', #25888 ) ;
#38210=CARTESIAN_POINT ( 'NONE',  ( 13.91401389203221406, 6.376774720514426953, 158.0376437107427137 ) ) ;
#38230=CARTESIAN_POINT ( 'NONE',  ( 29.70220533433691301, -6.475225279485573360, 28.20564067601639735 ) ) ;
#38253=DIRECTION ( 'NONE',  ( 0.6599726524652352877, -0.000000000000000000, -0.7512896232465891000 ) ) ;
#38255=CARTESIAN_POINT ( 'NONE',  ( 30.53060340732036337, 1.682774720514426114, -1.352392034746782823 ) ) ;
#38261=FACE_OUTER_BOUND ( 'NONE', #46347, .T. ) ;
#38291=VECTOR ( 'NONE', #9295, 1000.000000000000000 ) ;
#38292=ORIENTED_EDGE ( 'NONE', *, *, #5017, .F. ) ;
#38293=ORIENTED_EDGE ( 'NONE', *, *, #10326, .F. ) ;
#38296=CARTESIAN_POINT ( 'NONE',  ( 19.75748517575715368, -5.965225279485572685, 28.87153971905864580 ) ) ;
#38306=ORIENTED_EDGE ( 'NONE', *, *, #24587, .T. ) ;
#38345=VECTOR ( 'NONE', #59063, 1000.000000000000000 ) ;
#38353=ORIENTED_EDGE ( 'NONE', *, *, #49327, .T. ) ;
#38370=CARTESIAN_POINT ( 'NONE',  ( 32.98733314340959311, -5.965225279485572685, 2.074222136288530027 ) ) ;
#38378=CARTESIAN_POINT ( 'NONE',  ( -10.58858228176428717, -5.965225279485594001, -27.03148018517017093 ) ) ;
#38381=CARTESIAN_POINT ( 'NONE',  ( -20.27875734969026311, -4.543225279485573864, 26.25402280011862288 ) ) ;
#38386=DIRECTION ( 'NONE',  ( -0.6599726524652352877, 0.000000000000000000, 0.7512896232465891000 ) ) ;
#38407=AXIS2_PLACEMENT_3D ( 'NONE', #3502, #87733, #81615 ) ;
#38412=CARTESIAN_POINT ( 'NONE',  ( 32.98733314340959311, 0.3587747205144265483, 2.074222136288530027 ) ) ;
#38415=ADVANCED_FACE ( 'NONE', ( #91765 ), #64419, .F. ) ;
#38418=CARTESIAN_POINT ( 'NONE',  ( 31.16918082143019220, 5.911085521256299380, -1.357342440710215481 ) ) ;
#38420=EDGE_CURVE ( 'NONE', #38639, #63436, #75042, .T. ) ;
#38425=CYLINDRICAL_SURFACE ( 'NONE', #7959, 28.45799999999999486 ) ;
#38433=DIRECTION ( 'NONE',  ( -0.000000000000000000, -1.000000000000000000, 0.000000000000000000 ) ) ;
#38449=CARTESIAN_POINT ( 'NONE',  ( -29.49875734969026198, 0.3587747205144262708, 7.870022800118625206 ) ) ;
#38450=DIRECTION ( 'NONE',  ( 1.000000000000000000, 0.000000000000000000, 0.000000000000000000 ) ) ;
#38457=VERTEX_POINT ( 'NONE', #97397 ) ;
#38463=EDGE_LOOP ( 'NONE', ( #33221, #15591 ) ) ;
#38468=ORIENTED_EDGE ( 'NONE', *, *, #27378, .T. ) ;
#38484=ORIENTED_EDGE ( 'NONE', *, *, #88162, .T. ) ;
#38500=FACE_OUTER_BOUND ( 'NONE', #43658, .T. ) ;
#38516=DIRECTION ( 'NONE',  ( 1.000000000000000000, 0.000000000000000000, -0.000000000000000000 ) ) ;
#38521=DIRECTION ( 'NONE',  ( 0.000000000000000000, 0.000000000000000000, 1.000000000000000000 ) ) ;
#38541=CARTESIAN_POINT ( 'NONE',  ( 0.000000000000000000, -16.94322527948557422, 0.000000000000000000 ) ) ;
#38557=AXIS2_PLACEMENT_3D ( 'NONE', #72705, #51859, #90410 ) ;
#38608=ORIENTED_EDGE ( 'NONE', *, *, #31657, .F. ) ;
#38609=DIRECTION ( 'NONE',  ( 0.000000000000000000, 0.000000000000000000, 1.000000000000000000 ) ) ;
#38618=DIRECTION ( 'NONE',  ( 0.000000000000000000, 0.000000000000000000, 1.000000000000000000 ) ) ;
#38620=DIRECTION ( 'NONE',  ( -0.000000000000000000, 1.000000000000000000, -0.000000000000000000 ) ) ;
#38622=CARTESIAN_POINT ( 'NONE',  ( 30.93860345374796594, -5.515143950957555496, 14.99689261510125249 ) ) ;
#38624=CARTESIAN_POINT ( 'NONE',  ( 11.69063526134919684, 3.622774720514426949, -29.65990201929480108 ) ) ;
#38637=CARTESIAN_POINT ( 'NONE',  ( 7.822518687389895753, 3.316774720514091168, -28.18023264461383448 ) ) ;
#38639=VERTEX_POINT ( 'NONE', #94271 ) ;
#38644=CARTESIAN_POINT ( 'NONE',  ( -28.98875734969026396, -5.965225279485572685, -0.08597719988137648983 ) ) ;
#38647=ADVANCED_FACE ( 'NONE', ( #78031 ), #8543, .T. ) ;
#38648=FACE_OUTER_BOUND ( 'NONE', #28635, .T. ) ;
#38668=DIRECTION ( 'NONE',  ( 8.719066383522879804E-15, 0.000000000000000000, -1.000000000000000000 ) ) ;
#38688=CARTESIAN_POINT ( 'NONE',  ( 22.81105451610979173, -6.475225279485573360, -18.46691820600746681 ) ) ;
#38713=EDGE_LOOP ( 'NONE', ( #71249, #44997, #69809, #97420 ) ) ;
#38730=CARTESIAN_POINT ( 'NONE',  ( -28.98875734969026041, 0.3587747205144265483, 17.86602280011862476 ) ) ;
#38733=CARTESIAN_POINT ( 'NONE',  ( 33.07248226229787491, 4.977706540348799891, -12.91345179487514905 ) ) ;
#38736=EDGE_LOOP ( 'NONE', ( #59314, #54212, #63706, #92408, #5119, #86038, #93301, #63703, #88878, #58788, #73158, #66421 ) ) ;
#38742=ORIENTED_EDGE ( 'NONE', *, *, #18898, .T. ) ;
#38744=CARTESIAN_POINT ( 'NONE',  ( 13.91401389203221406, 3.316774720514426456, 158.0376437107427137 ) ) ;
#38755=DIRECTION ( 'NONE',  ( 0.000000000000000000, 0.000000000000000000, 1.000000000000000000 ) ) ;
#38763=VECTOR ( 'NONE', #75232, 1000.000000000000000 ) ;
#38787=ORIENTED_EDGE ( 'NONE', *, *, #5017, .T. ) ;
#38804=CARTESIAN_POINT ( 'NONE',  ( 282.9764569301858046, 2.682774720514426559, 20.79159422840526616 ) ) ;
#38808=ORIENTED_EDGE ( 'NONE', *, *, #10588, .F. ) ;
#38810=ORIENTED_EDGE ( 'NONE', *, *, #83022, .T. ) ;
#38813=LINE ( 'NONE', #91603, #25856 ) ;
#38817=ADVANCED_FACE ( 'NONE', ( #37254 ), #66003, .T. ) ;
#38829=AXIS2_PLACEMENT_3D ( 'NONE', #81756, #66565, #58436 ) ;
#38835=ORIENTED_EDGE ( 'NONE', *, *, #15749, .F. ) ;
#38836=CIRCLE ( 'NONE', #64808, 3.500000000000000000 ) ;
#38840=ORIENTED_EDGE ( 'NONE', *, *, #54136, .F. ) ;
#38850=EDGE_CURVE ( 'NONE', #50604, #68064, #22498, .T. ) ;
#38875=LINE ( 'NONE', #31772, #5826 ) ;
#38876=FACE_OUTER_BOUND ( 'NONE', #56464, .T. ) ;
#38908=CARTESIAN_POINT ( 'NONE',  ( 30.61004588589006659, 4.070814610512477394, 27.12580813198458785 ) ) ;
#38916=CARTESIAN_POINT ( 'NONE',  ( -19.77875734969026311, 5.356774720514426491, 27.45402280011862217 ) ) ;
#38931=CARTESIAN_POINT ( 'NONE',  ( 32.53346577320678534, 0.6027747205144262654, -11.93731717363831102 ) ) ;
#38940=ORIENTED_EDGE ( 'NONE', *, *, #75302, .F. ) ;
#38947=EDGE_CURVE ( 'NONE', #39863, #11676, #99384, .T. ) ;
#38958=DIRECTION ( 'NONE',  ( 3.639962309748244178E-15, -1.000000000000000000, -2.135627652102599075E-15 ) ) ;
#38984=CARTESIAN_POINT ( 'NONE',  ( 282.9764569301858046, -5.965225279485572685, 20.79159422840526616 ) ) ;
#38997=CARTESIAN_POINT ( 'NONE',  ( 4.784292611718076849, 5.356774720514425603, -25.54547254883186014 ) ) ;
#39000=EDGE_CURVE ( 'NONE', #42693, #66086, #34575, .T. ) ;
#39007=LINE ( 'NONE', #15671, #53190 ) ;
#39008=CARTESIAN_POINT ( 'NONE',  ( 31.63608488009065667, 6.376774720514426953, 27.34773273846995068 ) ) ;
#39012=EDGE_CURVE ( 'NONE', #45125, #51264, #33131, .T. ) ;
#39015=DIRECTION ( 'NONE',  ( -0.000000000000000000, 1.000000000000000000, -0.000000000000000000 ) ) ;
#39024=ORIENTED_EDGE ( 'NONE', *, *, #37289, .F. ) ;
#39077=VERTEX_POINT ( 'NONE', #66613 ) ;
#39083=CARTESIAN_POINT ( 'NONE',  ( -28.98875734969026041, -5.965225279485572685, 25.61802280011862720 ) ) ;
#39091=VERTEX_POINT ( 'NONE', #42277 ) ;
#39102=ORIENTED_EDGE ( 'NONE', *, *, #64574, .F. ) ;
#39105=CARTESIAN_POINT ( 'NONE',  ( -32.30247028140506416, -6.475225279485573360, 27.60502002861223048 ) ) ;
#39133=CARTESIAN_POINT ( 'NONE',  ( -10.11875734969026297, 3.316774720514426456, 30.51402280011862089 ) ) ;
#39147=CARTESIAN_POINT ( 'NONE',  ( 22.81105451610979173, -1.477225279485574028, -18.46691820600746681 ) ) ;
#39187=EDGE_LOOP ( 'NONE', ( #50206, #73656, #22074, #96256 ) ) ;
#39215=EDGE_CURVE ( 'NONE', #67600, #91984, #92927, .T. ) ;
#39227=EDGE_CURVE ( 'NONE', #94973, #68532, #93906, .T. ) ;
#39229=VECTOR ( 'NONE', #92792, 1000.000000000000000 ) ;
#39261=CARTESIAN_POINT ( 'NONE',  ( 0.000000000000000000, 5.356774720514425603, 6.000000000000000888 ) ) ;
#39275=DIRECTION ( 'NONE',  ( -0.2488812114211666759, 0.000000000000000000, -0.9685340172660599212 ) ) ;
#39279=EDGE_CURVE ( 'NONE', #88430, #40707, #78663, .T. ) ;
#39282=CIRCLE ( 'NONE', #62033, 91.74549126261076992 ) ;
#39309=LINE ( 'NONE', #86981, #98021 ) ;
#39311=FACE_OUTER_BOUND ( 'NONE', #24098, .T. ) ;
#39312=ORIENTED_EDGE ( 'NONE', *, *, #37545, .T. ) ;
#39313=EDGE_LOOP ( 'NONE', ( #38608, #43982, #45565, #51130, #9341, #86769, #74993, #56497 ) ) ;
#39323=AXIS2_PLACEMENT_3D ( 'NONE', #52255, #6570, #45638 ) ;
#39350=ORIENTED_EDGE ( 'NONE', *, *, #56085, .T. ) ;
#39352=DIRECTION ( 'NONE',  ( 0.000000000000000000, -1.000000000000000000, 0.000000000000000000 ) ) ;
#39361=ADVANCED_FACE ( 'NONE', ( #26406 ), #88309, .F. ) ;
#39363=AXIS2_PLACEMENT_3D ( 'NONE', #80444, #57622, #27162 ) ;
#39371=ORIENTED_EDGE ( 'NONE', *, *, #89994, .F. ) ;
#39379=VECTOR ( 'NONE', #55402, 1000.000000000000000 ) ;
#39394=DIRECTION ( 'NONE',  ( 1.000000000000000000, -0.000000000000000000, -0.000000000000000000 ) ) ;
#39403=AXIS2_PLACEMENT_3D ( 'NONE', #75697, #69092, #22403 ) ;
#39411=EDGE_CURVE ( 'NONE', #23469, #92122, #64500, .T. ) ;
#39413=VECTOR ( 'NONE', #23532, 1000.000000000000000 ) ;
#39420=DIRECTION ( 'NONE',  ( -0.8264557562326038109, -6.454799914155187856E-16, -0.5630016722799275897 ) ) ;
#39448=ORIENTED_EDGE ( 'NONE', *, *, #31913, .F. ) ;
#39453=CIRCLE ( 'NONE', #91305, 2.499999999999998668 ) ;
#39454=ORIENTED_EDGE ( 'NONE', *, *, #92415, .T. ) ;
#39470=DIRECTION ( 'NONE',  ( 0.000000000000000000, -1.000000000000000000, 0.000000000000000000 ) ) ;
#39472=VERTEX_POINT ( 'NONE', #87807 ) ;
#39475=DIRECTION ( 'NONE',  ( 0.000000000000000000, 1.000000000000000000, -0.000000000000000000 ) ) ;
#39481=VECTOR ( 'NONE', #67380, 1000.000000000000000 ) ;
#39485=ADVANCED_FACE ( 'NONE', ( #18293 ), #48758, .T. ) ;
#39496=CARTESIAN_POINT ( 'NONE',  ( -29.49875734969025842, 0.3587747205144265483, 17.86602280011862476 ) ) ;
#39502=ORIENTED_EDGE ( 'NONE', *, *, #92652, .F. ) ;
#39516=CARTESIAN_POINT ( 'NONE',  ( 15.22325621495362391, 2.682774720514426559, -27.23549315679322547 ) ) ;
#39522=DIRECTION ( 'NONE',  ( -2.313651251573816365E-16, 1.000000000000000000, -8.068660792749104624E-16 ) ) ;
#39555=EDGE_CURVE ( 'NONE', #22708, #54184, #55502, .T. ) ;
#39567=ADVANCED_FACE ( 'NONE', ( #51238 ), #36007, .T. ) ;
#39570=DIRECTION ( 'NONE',  ( 0.000000000000000000, 1.000000000000000000, -0.000000000000000000 ) ) ;
#39592=DIRECTION ( 'NONE',  ( -0.9921023176230514551, 0.000000000000000000, 0.1254312216594016816 ) ) ;
#39596=EDGE_CURVE ( 'NONE', #88353, #36769, #83171, .T. ) ;
#39607=DIRECTION ( 'NONE',  ( 0.000000000000000000, 1.000000000000000000, -8.393823270855521221E-16 ) ) ;
#39635=DIRECTION ( 'NONE',  ( 0.000000000000000000, -1.000000000000000000, 0.000000000000000000 ) ) ;
#39639=CARTESIAN_POINT ( 'NONE',  ( 10.16466294932649106, 6.376774720514429617, -24.98589889747637116 ) ) ;
#39646=CARTESIAN_POINT ( 'NONE',  ( -10.16634758543296613, -5.965225279485572685, 30.00402280011862288 ) ) ;
#39653=CARTESIAN_POINT ( 'NONE',  ( 5.471383689419962337, -5.965225279485594001, -29.02273493113403902 ) ) ;
#39655=VERTEX_POINT ( 'NONE', #6056 ) ;
#39664=ADVANCED_FACE ( 'NONE', ( #29393 ), #67975, .F. ) ;
#39680=CARTESIAN_POINT ( 'NONE',  ( 15.99960863614630391, 3.577630190450220571, -27.91116951066582175 ) ) ;
#39681=ORIENTED_EDGE ( 'NONE', *, *, #21343, .T. ) ;
#39708=ORIENTED_EDGE ( 'NONE', *, *, #20090, .T. ) ;
#39717=CARTESIAN_POINT ( 'NONE',  ( 5.271800844963591359, 6.376774720514426953, -28.56638892015329034 ) ) ;
#39720=ORIENTED_EDGE ( 'NONE', *, *, #53212, .T. ) ;
#39725=VECTOR ( 'NONE', #92002, 1000.000000000000000 ) ;
#39728=ORIENTED_EDGE ( 'NONE', *, *, #5552, .T. ) ;
#39730=ORIENTED_EDGE ( 'NONE', *, *, #71933, .F. ) ;
#39731=DIRECTION ( 'NONE',  ( 0.9913618264504691080, -7.885106708985488048E-16, -0.1311553622875927805 ) ) ;
#39746=DIRECTION ( 'NONE',  ( 0.000000000000000000, 0.000000000000000000, 1.000000000000000000 ) ) ;
#39777=CIRCLE ( 'NONE', #54362, 0.8160000000000007248 ) ;
#39787=AXIS2_PLACEMENT_3D ( 'NONE', #66853, #66359, #28269 ) ;
#39806=DIRECTION ( 'NONE',  ( -1.000000000000000000, 0.000000000000000000, 0.000000000000000000 ) ) ;
#39819=EDGE_CURVE ( 'NONE', #20097, #86154, #57260, .T. ) ;
#39821=LINE ( 'NONE', #31714, #93172 ) ;
#39823=CARTESIAN_POINT ( 'NONE',  ( 14.15579980161844986, 3.316774720514426456, -28.31186755866361437 ) ) ;
#39825=DIRECTION ( 'NONE',  ( -0.000000000000000000, -1.000000000000000000, -0.000000000000000000 ) ) ;
#39835=ADVANCED_FACE ( 'NONE', ( #11549 ), #50622, .T. ) ;
#39838=DIRECTION ( 'NONE',  ( 1.000000000000000000, 4.218136541796977197E-15, 0.000000000000000000 ) ) ;
#39840=VERTEX_POINT ( 'NONE', #34900 ) ;
#39857=CARTESIAN_POINT ( 'NONE',  ( 13.91401389203221406, 0.3587747205144265483, 158.0376437107427137 ) ) ;
#39863=VERTEX_POINT ( 'NONE', #25279 ) ;
#39864=VECTOR ( 'NONE', #31978, 1000.000000000000000 ) ;
#39893=DIRECTION ( 'NONE',  ( 0.000000000000000000, -1.000000000000000000, 0.000000000000000000 ) ) ;
#39906=CARTESIAN_POINT ( 'NONE',  ( -24.90875734969025501, 6.376774720514426953, 30.51402280011862089 ) ) ;
#39909=ORIENTED_EDGE ( 'NONE', *, *, #16723, .F. ) ;
#39929=VERTEX_POINT ( 'NONE', #75935 ) ;
#39940=AXIS2_PLACEMENT_3D ( 'NONE', #41082, #86243, #93850 ) ;
#39982=AXIS2_PLACEMENT_3D ( 'NONE', #93010, #54468, #70188 ) ;
#39995=DIRECTION ( 'NONE',  ( 1.000000000000000000, 1.232047923278981953E-16, 0.000000000000000000 ) ) ;
#40000=AXIS2_PLACEMENT_3D ( 'NONE', #24645, #7928, #55627 ) ;
#40020=CARTESIAN_POINT ( 'NONE',  ( 33.69795529655567634, -6.475225279485573360, 20.86760796525322093 ) ) ;
#40033=DIRECTION ( 'NONE',  ( 0.000000000000000000, -1.000000000000000000, 1.478457507934778393E-16 ) ) ;
#40036=CARTESIAN_POINT ( 'NONE',  ( -24.57525087998974200, 0.3587747205143967943, -15.45548830044932664 ) ) ;
#40057=AXIS2_PLACEMENT_3D ( 'NONE', #31257, #61234, #23635 ) ;
#40067=EDGE_LOOP ( 'NONE', ( #51898, #4298 ) ) ;
#40073=VECTOR ( 'NONE', #63986, 1000.000000000000000 ) ;
#40087=VERTEX_POINT ( 'NONE', #24153 ) ;
#40094=CARTESIAN_POINT ( 'NONE',  ( 15.30859874843628354, 3.492299066144916697, -27.16052374892713317 ) ) ;
#40098=CARTESIAN_POINT ( 'NONE',  ( -4.568292318365942073, -5.965225279485572685, 30.06720597538392425 ) ) ;
#40099=CARTESIAN_POINT ( 'NONE',  ( 22.33191539159815164, 2.682774720514426559, -16.26852658953823649 ) ) ;
#40109=LINE ( 'NONE', #22486, #34307 ) ;
#40121=VECTOR ( 'NONE', #19001, 1000.000000000000000 ) ;
#40130=CARTESIAN_POINT ( 'NONE',  ( 22.74089357256066535, 4.772774720514425972, -19.20396252371061863 ) ) ;
#40137=CYLINDRICAL_SURFACE ( 'NONE', #4517, 1.530000000000001359 ) ;
#40186=CARTESIAN_POINT ( 'NONE',  ( 13.91401389203221406, -5.965225279485572685, 158.0376437107427137 ) ) ;
#40215=CARTESIAN_POINT ( 'NONE',  ( 29.58888977143521970, 4.303425171653743497, 29.06172452911802750 ) ) ;
#40218=ORIENTED_EDGE ( 'NONE', *, *, #56028, .F. ) ;
#40221=AXIS2_PLACEMENT_3D ( 'NONE', #70879, #24679, #15075 ) ;
#40235=ORIENTED_EDGE ( 'NONE', *, *, #50357, .T. ) ;
#40247=DIRECTION ( 'NONE',  ( 0.000000000000000000, 0.000000000000000000, -1.000000000000000000 ) ) ;
#40258=ORIENTED_EDGE ( 'NONE', *, *, #90940, .T. ) ;
#40262=EDGE_CURVE ( 'NONE', #35959, #64113, #95176, .T. ) ;
#40284=CARTESIAN_POINT ( 'NONE',  ( 22.81105451610979173, -1.477225279485574028, -18.46691820600746681 ) ) ;
#40293=ORIENTED_EDGE ( 'NONE', *, *, #34333, .F. ) ;
#40307=CARTESIAN_POINT ( 'NONE',  ( -10.22992732494356005, 5.749436596009021017, 29.32115093811272288 ) ) ;
#40315=ORIENTED_EDGE ( 'NONE', *, *, #46226, .F. ) ;
#40328=ORIENTED_EDGE ( 'NONE', *, *, #61767, .T. ) ;
#40329=LINE ( 'NONE', #2281, #96375 ) ;
#40333=CARTESIAN_POINT ( 'NONE',  ( -27.25988310792305214, -5.965225279485572685, 30.32664379231667695 ) ) ;
#40335=EDGE_CURVE ( 'NONE', #35854, #24351, #34285, .T. ) ;
#40338=DIRECTION ( 'NONE',  ( -0.000000000000000000, 1.000000000000000000, -0.000000000000000000 ) ) ;
#40366=ORIENTED_EDGE ( 'NONE', *, *, #22221, .T. ) ;
#40372=VERTEX_POINT ( 'NONE', #33266 ) ;
#40391=CARTESIAN_POINT ( 'NONE',  ( 33.96422015159436114, -5.965225279485572685, -7.233236000911337449 ) ) ;
#40395=VECTOR ( 'NONE', #46508, 1000.000000000000000 ) ;
#40405=EDGE_CURVE ( 'NONE', #76194, #99483, #34648, .T. ) ;
#40428=PLANE ( 'NONE',  #80361 ) ;
#40429=VECTOR ( 'NONE', #25986, 1000.000000000000000 ) ;
#40431=ORIENTED_EDGE ( 'NONE', *, *, #52164, .T. ) ;
#40443=CARTESIAN_POINT ( 'NONE',  ( 32.29806486058159010, 4.575840390334028562, -4.131869215359018632 ) ) ;
#40445=DIRECTION ( 'NONE',  ( 0.000000000000000000, 1.000000000000000000, 0.000000000000000000 ) ) ;
#40448=CARTESIAN_POINT ( 'NONE',  ( 22.02124265030973760, -4.543225279485573864, 16.20402280011862217 ) ) ;
#40460=ORIENTED_EDGE ( 'NONE', *, *, #64392, .F. ) ;
#40461=CARTESIAN_POINT ( 'NONE',  ( 29.73612274945269718, 5.099749465620300626, 27.18845636319765191 ) ) ;
#40462=DIRECTION ( 'NONE',  ( 0.000000000000000000, 0.000000000000000000, -1.000000000000000000 ) ) ;
#40508=DIRECTION ( 'NONE',  ( 1.000000000000000000, 0.000000000000000000, -0.000000000000000000 ) ) ;
#40520=LINE ( 'NONE', #26280, #32040 ) ;
#40533=ORIENTED_EDGE ( 'NONE', *, *, #99252, .T. ) ;
#40548=CARTESIAN_POINT ( 'NONE',  ( 33.47959399259596580, 3.475369878553063341, -12.33463419434873032 ) ) ;
#40567=CARTESIAN_POINT ( 'NONE',  ( -53.01255352321339842, 4.132774720514426292, 35.59556822165056644 ) ) ;
#40579=CIRCLE ( 'NONE', #63260, 251.4258649670780699 ) ;
#40581=DIRECTION ( 'NONE',  ( 0.000000000000000000, 0.000000000000000000, 1.000000000000000000 ) ) ;
#40591=DIRECTION ( 'NONE',  ( 0.000000000000000000, 0.000000000000000000, -1.000000000000000000 ) ) ;
#40605=DIRECTION ( 'NONE',  ( 1.000000000000000000, -0.000000000000000000, -0.000000000000000000 ) ) ;
#40622=EDGE_LOOP ( 'NONE', ( #40749, #6014, #2419, #24701 ) ) ;
#40625=CARTESIAN_POINT ( 'NONE',  ( 0.000000000000000000, -16.94322527948557422, 0.000000000000000000 ) ) ;
#40627=EDGE_CURVE ( 'NONE', #57808, #23980, #31145, .T. ) ;
#40630=LINE ( 'NONE', #93900, #97561 ) ;
#40636=CIRCLE ( 'NONE', #16281, 84.48086791635431325 ) ;
#40656=AXIS2_PLACEMENT_3D ( 'NONE', #3092, #71596, #56884 ) ;
#40657=ORIENTED_EDGE ( 'NONE', *, *, #93416, .T. ) ;
#40667=DIRECTION ( 'NONE',  ( 0.000000000000000000, -0.000000000000000000, -1.000000000000000000 ) ) ;
#40686=CARTESIAN_POINT ( 'NONE',  ( 0.000000000000000000, 4.132774720514426292, 0.000000000000000000 ) ) ;
#40707=VERTEX_POINT ( 'NONE', #89817 ) ;
#40727=CARTESIAN_POINT ( 'NONE',  ( 3.180076745125948179, -5.965225279485592225, -28.87659520466657526 ) ) ;
#40732=CARTESIAN_POINT ( 'NONE',  ( 25.20856462023905564, 4.845009571353474875, -10.39575909395317943 ) ) ;
#40734=ORIENTED_EDGE ( 'NONE', *, *, #21257, .F. ) ;
#40749=ORIENTED_EDGE ( 'NONE', *, *, #90444, .F. ) ;
#40752=PLANE ( 'NONE',  #91725 ) ;
#40772=DIRECTION ( 'NONE',  ( 0.9921023176230513441, 0.000000000000000000, -0.1254312216594016538 ) ) ;
#40779=DIRECTION ( 'NONE',  ( -0.000000000000000000, -1.000000000000000000, -0.000000000000000000 ) ) ;
#40781=AXIS2_PLACEMENT_3D ( 'NONE', #48668, #55775, #86700 ) ;
#40786=FACE_OUTER_BOUND ( 'NONE', #67409, .T. ) ;
#40796=CARTESIAN_POINT ( 'NONE',  ( -53.01255352321339842, 4.772774720514425972, 35.59556822165056644 ) ) ;
#40801=CARTESIAN_POINT ( 'NONE',  ( -29.49975734969026320, -6.475225279485573360, 13.17908622612278613 ) ) ;
#40809=VECTOR ( 'NONE', #60095, 1000.000000000000000 ) ;
#40834=ORIENTED_EDGE ( 'NONE', *, *, #76930, .T. ) ;
#40848=DIRECTION ( 'NONE',  ( -0.000000000000000000, 1.000000000000000000, -0.000000000000000000 ) ) ;
#40851=ORIENTED_EDGE ( 'NONE', *, *, #6924, .F. ) ;
#40852=DIRECTION ( 'NONE',  ( 0.000000000000000000, -1.478457507934778393E-16, -1.000000000000000000 ) ) ;
#40858=ORIENTED_EDGE ( 'NONE', *, *, #53564, .F. ) ;
#40868=ORIENTED_EDGE ( 'NONE', *, *, #51844, .F. ) ;
#40877=DIRECTION ( 'NONE',  ( 0.000000000000000000, 0.000000000000000000, 1.000000000000000000 ) ) ;
#40907=AXIS2_PLACEMENT_3D ( 'NONE', #94677, #25670, #3360 ) ;
#40914=EDGE_CURVE ( 'NONE', #67734, #88430, #67990, .T. ) ;
#40918=EDGE_CURVE ( 'NONE', #43471, #50604, #44147, .T. ) ;
#40933=ORIENTED_EDGE ( 'NONE', *, *, #1046, .F. ) ;
#40986=CIRCLE ( 'NONE', #2099, 2.499999999999998668 ) ;
#40993=EDGE_CURVE ( 'NONE', #93421, #5378, #85704, .T. ) ;
#41003=DIRECTION ( 'NONE',  ( 0.000000000000000000, -0.7071067811865513475, 0.7071067811865437980 ) ) ;
#41006=CARTESIAN_POINT ( 'NONE',  ( -29.49875734969025842, -5.965225279485572685, 23.37402280011862743 ) ) ;
#41012=VECTOR ( 'NONE', #64025, 1000.000000000000000 ) ;
#41039=VERTEX_POINT ( 'NONE', #48664 ) ;
#41045=CARTESIAN_POINT ( 'NONE',  ( 32.98371819488264833, 4.742969794006914874, -11.67826368001470172 ) ) ;
#41057=CARTESIAN_POINT ( 'NONE',  ( 33.61456970919605425, 3.316774720514426900, -11.35828564741663449 ) ) ;
#41075=DIRECTION ( 'NONE',  ( 0.000000000000000000, 0.000000000000000000, 1.000000000000000000 ) ) ;
#41079=B_SPLINE_CURVE_WITH_KNOTS ( 'NONE', 3,
 ( #959, #31911, #71985, #17177, #62884, #93803 ),
 .UNSPECIFIED., .F., .F.,
 ( 4, 2, 4 ),
 ( 0.005040430490715508416, 0.005640264188159228517, 0.006240097885602948619 ),
 .UNSPECIFIED. ) ;
#41082=CARTESIAN_POINT ( 'NONE',  ( -27.96875734969026084, 6.376774720514426953, 0.7300228001186309656 ) ) ;
#41085=ADVANCED_FACE ( 'NONE', ( #11077 ), #12063, .F. ) ;
#41089=VECTOR ( 'NONE', #44288, 1000.000000000000000 ) ;
#41096=AXIS2_PLACEMENT_3D ( 'NONE', #54976, #48871, #9284 ) ;
#41109=EDGE_CURVE ( 'NONE', #18484, #67714, #87946, .T. ) ;
#41126=ORIENTED_EDGE ( 'NONE', *, *, #44790, .F. ) ;
#41129=FACE_OUTER_BOUND ( 'NONE', #42581, .T. ) ;
#41149=DIRECTION ( 'NONE',  ( 0.000000000000000000, 0.000000000000000000, 1.000000000000000000 ) ) ;
#41153=DIRECTION ( 'NONE',  ( -0.000000000000000000, 1.000000000000000000, -0.000000000000000000 ) ) ;
#41163=DIRECTION ( 'NONE',  ( -0.02119372647572909107, 0.000000000000000000, -0.9997753877537054468 ) ) ;
#41180=ADVANCED_FACE ( 'NONE', ( #33916 ), #57279, .T. ) ;
#41182=ORIENTED_EDGE ( 'NONE', *, *, #83324, .T. ) ;
#41186=CARTESIAN_POINT ( 'NONE',  ( 31.63910543787539709, 6.180494461685818841, 27.51903215948834358 ) ) ;
#41188=EDGE_CURVE ( 'NONE', #22271, #69136, #96056, .T. ) ;
#41192=DIRECTION ( 'NONE',  ( -0.000000000000000000, 1.000000000000000000, -0.000000000000000000 ) ) ;
#41194=DIRECTION ( 'NONE',  ( 0.000000000000000000, 0.000000000000000000, -1.000000000000000000 ) ) ;
#41202=ORIENTED_EDGE ( 'NONE', *, *, #90589, .F. ) ;
#41217=CARTESIAN_POINT ( 'NONE',  ( 9.315600972258346602, -5.965225279485572685, 28.35070303307545458 ) ) ;
#41220=FACE_OUTER_BOUND ( 'NONE', #48579, .T. ) ;
#41222=CARTESIAN_POINT ( 'NONE',  ( 29.64418490232317893, 5.621712738193696879, 28.18100406333994457 ) ) ;
#41273=DIRECTION ( 'NONE',  ( 0.000000000000000000, 1.000000000000000000, 0.000000000000000000 ) ) ;
#41279=LINE ( 'NONE', #41795, #55927 ) ;
#41285=CARTESIAN_POINT ( 'NONE',  ( -25.92875734969025814, 3.316774720514426456, 26.43402280011862615 ) ) ;
#41304=EDGE_CURVE ( 'NONE', #84489, #39077, #30282, .T. ) ;
#41305=VERTEX_POINT ( 'NONE', #90194 ) ;
#41307=CARTESIAN_POINT ( 'NONE',  ( -10.32858501761201353, 6.295917116278983983, 28.25808420984930791 ) ) ;
#41316=CARTESIAN_POINT ( 'NONE',  ( 7.117251336872616463, 5.324156306579707731, -25.56604299071238984 ) ) ;
#41321=ORIENTED_EDGE ( 'NONE', *, *, #90444, .T. ) ;
#41330=VECTOR ( 'NONE', #80033, 1000.000000000000000 ) ;
#41333=CARTESIAN_POINT ( 'NONE',  ( -10.21384395349167562, 3.451719627175087179, 29.49402280011861777 ) ) ;
#41351=CARTESIAN_POINT ( 'NONE',  ( 26.73860345374794534, 1.682774720514426114, -7.113848178280766099 ) ) ;
#41376=( BOUNDED_SURFACE ( )  B_SPLINE_SURFACE ( 3, 2, ( 
 ( #78190, #7689, #93417 ),
 ( #92915, #93924, #23911 ),
 ( #92419, #22886, #7181 ),
 ( #32030, #78684, #38637 ),
 ( #47770, #84808, #68596 ),
 ( #53875, #61989, #15292 ),
 ( #23391, #86321, #54378 ),
 ( #77683, #85308, #85819 ),
 ( #60990, #16301, #15796 ),
 ( #47265, #8703, #63005 ),
 ( #39639, #24417, #55382 ),
 ( #53380, #84306, #14789 ),
 ( #45757, #76678, #38131 ),
 ( #69086, #49785, #26930 ),
 ( #33539, #17816, #9191 ),
 ( #94935, #1596, #96438 ),
 ( #56899, #87831, #94429 ),
 ( #56398, #17307, #26437 ) ),
 .UNSPECIFIED., .F., .F., .T. ) 
 B_SPLINE_SURFACE_WITH_KNOTS ( ( 4, 2, 2, 2, 2, 2, 2, 2, 4 ),
 ( 3, 3 ),
 ( -3.428680950268159222E-15, 0.002319258964652063781, 0.003478888446979810228, 0.004058703188143683235, 0.004638517929307556242, 0.005798147411635302256, 0.006377962152799175263, 0.006957776893963049138, 0.009277035858618542033 ),
 ( 0.000000000000000000, 1.000000000000000000 ),
 .UNSPECIFIED. ) 
 GEOMETRIC_REPRESENTATION_ITEM ( )  RATIONAL_B_SPLINE_SURFACE ( (
 ( 1.000000000000000000, 0.7071067811865475727, 1.000000000000000000),
 ( 1.000000000000000000, 0.7071067811865475727, 1.000000000000000000),
 ( 1.000000000000000000, 0.7071067811865471286, 1.000000000000000000),
 ( 1.000000000000000000, 0.7071067811865471286, 1.000000000000000000),
 ( 1.000000000000000000, 0.7071067811865473507, 1.000000000000000000),
 ( 1.000000000000000000, 0.7071067811865473507, 1.000000000000000000),
 ( 1.000000000000000000, 0.7071067811865475727, 1.000000000000000000),
 ( 1.000000000000000000, 0.7071067811865475727, 1.000000000000000000),
 ( 1.000000000000000000, 0.7071067811865476838, 1.000000000000000000),
 ( 1.000000000000000000, 0.7071067811865476838, 1.000000000000000000),
 ( 1.000000000000000000, 0.7071067811865473507, 1.000000000000000000),
 ( 1.000000000000000000, 0.7071067811865473507, 1.000000000000000000),
 ( 1.000000000000000000, 0.7071067811865471286, 1.000000000000000000),
 ( 1.000000000000000000, 0.7071067811865471286, 1.000000000000000000),
 ( 1.000000000000000000, 0.7071067811865471286, 1.000000000000000000),
 ( 1.000000000000000000, 0.7071067811865471286, 1.000000000000000000),
 ( 1.000000000000000000, 0.7071067811865475727, 1.000000000000000000),
 ( 1.000000000000000000, 0.7071067811865475727, 1.000000000000000000) ) ) 
 REPRESENTATION_ITEM ( '' )  SURFACE ( )  );
#41384=DIRECTION ( 'NONE',  ( -0.000000000000000000, -1.000000000000000000, 0.000000000000000000 ) ) ;
#41408=DIRECTION ( 'NONE',  ( 0.7071067811865476838, 0.000000000000000000, -0.7071067811865474617 ) ) ;
#41443=ORIENTED_EDGE ( 'NONE', *, *, #91163, .F. ) ;
#41446=ORIENTED_EDGE ( 'NONE', *, *, #74935, .T. ) ;
#41450=ORIENTED_EDGE ( 'NONE', *, *, #71491, .T. ) ;
#41468=ORIENTED_EDGE ( 'NONE', *, *, #69180, .F. ) ;
#41471=AXIS2_PLACEMENT_3D ( 'NONE', #17470, #32189, #15463 ) ;
#41477=DIRECTION ( 'NONE',  ( 0.000000000000000000, 1.000000000000000000, 0.000000000000000000 ) ) ;
#41488=VECTOR ( 'NONE', #18734, 1000.000000000000000 ) ;
#41503=VERTEX_POINT ( 'NONE', #78449 ) ;
#41528=CARTESIAN_POINT ( 'NONE',  ( 29.73860345376319358, 4.772803916115708311, -4.021109907510727943 ) ) ;
#41535=CIRCLE ( 'NONE', #46367, 3.060000000000000053 ) ;
#41542=PLANE ( 'NONE',  #40781 ) ;
#41544=CARTESIAN_POINT ( 'NONE',  ( 25.05730599792488178, 500000.0000000000582, -18.59674224247031304 ) ) ;
#41547=CARTESIAN_POINT ( 'NONE',  ( 33.54680291763921929, 3.871631182425088191, -11.45966867074879580 ) ) ;
#41569=EDGE_CURVE ( 'NONE', #14228, #89486, #9952, .T. ) ;
#41582=FACE_OUTER_BOUND ( 'NONE', #251, .T. ) ;
#41583=CARTESIAN_POINT ( 'NONE',  ( 0.000000000000000000, -1.473225279485573802, 0.000000000000000000 ) ) ;
#41585=EDGE_CURVE ( 'NONE', #93008, #28007, #8630, .T. ) ;
#41599=EDGE_LOOP ( 'NONE', ( #75128, #19609, #33952, #84472 ) ) ;
#41601=( NAMED_UNIT ( * ) SI_UNIT ( $, .STERADIAN. ) SOLID_ANGLE_UNIT ( ) );
#41618=VECTOR ( 'NONE', #76702, 1000.000000000000000 ) ;
#41633=CARTESIAN_POINT ( 'NONE',  ( -65.05438548721848235, -6.475225279485573360, 0.7300228001186309656 ) ) ;
#41643=DIRECTION ( 'NONE',  ( 0.000000000000000000, 0.7071067811865437980, 0.7071067811865513475 ) ) ;
#41658=AXIS2_PLACEMENT_3D ( 'NONE', #27006, #11773, #3185 ) ;
#41672=ORIENTED_EDGE ( 'NONE', *, *, #61611, .F. ) ;
#41690=ADVANCED_FACE ( 'NONE', ( #60641 ), #13438, .F. ) ;
#41699=CARTESIAN_POINT ( 'NONE',  ( 31.61404304915243202, 4.508643932895013862, 26.44173824648443727 ) ) ;
#41703=EDGE_CURVE ( 'NONE', #14845, #42618, #53024, .T. ) ;
#41716=ORIENTED_EDGE ( 'NONE', *, *, #47680, .T. ) ;
#41754=ORIENTED_EDGE ( 'NONE', *, *, #28523, .F. ) ;
#41767=ORIENTED_EDGE ( 'NONE', *, *, #31789, .F. ) ;
#41772=EDGE_CURVE ( 'NONE', #24307, #96497, #16938, .T. ) ;
#41773=PLANE ( 'NONE',  #90151 ) ;
#41790=LINE ( 'NONE', #64135, #73364 ) ;
#41795=CARTESIAN_POINT ( 'NONE',  ( 32.25183987940364005, 6.376774720514426953, 2.026414261721653176 ) ) ;
#41803=DIRECTION ( 'NONE',  ( -0.2488812114211667037, -0.000000000000000000, -0.9685340172660599212 ) ) ;
#41809=ORIENTED_EDGE ( 'NONE', *, *, #88179, .T. ) ;
#41816=CARTESIAN_POINT ( 'NONE',  ( -4.929522925832178437, -5.965225279485572685, -28.63504101147568903 ) ) ;
#41825=PLANE ( 'NONE',  #30795 ) ;
#41837=VERTEX_POINT ( 'NONE', #34676 ) ;
#41845=DIRECTION ( 'NONE',  ( -0.000000000000000000, 0.000000000000000000, 1.000000000000000000 ) ) ;
#41857=ORIENTED_EDGE ( 'NONE', *, *, #90530, .F. ) ;
#41861=DIRECTION ( 'NONE',  ( 0.000000000000000000, 1.000000000000000000, 0.000000000000000000 ) ) ;
#41875=CARTESIAN_POINT ( 'NONE',  ( 13.91401389203221406, 6.376774720514426953, 158.0376437107427137 ) ) ;
#41880=ORIENTED_EDGE ( 'NONE', *, *, #27573, .T. ) ;
#41889=B_SPLINE_CURVE_WITH_KNOTS ( 'NONE', 3,
 ( #79450, #73353, #49525, #94675, #11941, #9942, #57142 ),
 .UNSPECIFIED., .F., .F.,
 ( 4, 3, 4 ),
 ( 0.000000000000000000, 1.195459452644217715E-05, 2.107775188753445374E-05 ),
 .UNSPECIFIED. ) ;
#41897=ADVANCED_FACE ( 'NONE', ( #18936 ), #17946, .F. ) ;
#41901=DIRECTION ( 'NONE',  ( -0.000000000000000000, 1.000000000000000000, -0.000000000000000000 ) ) ;
#41902=ORIENTED_EDGE ( 'NONE', *, *, #85531, .F. ) ;
#41916=VECTOR ( 'NONE', #2878, 1000.000000000000000 ) ;
#41940=ADVANCED_FACE ( 'NONE', ( #50402 ), #26052, .T. ) ;
#41944=CARTESIAN_POINT ( 'NONE',  ( 32.66876533700882845, -5.965225279485572685, -12.58926540598385557 ) ) ;
#41945=FACE_OUTER_BOUND ( 'NONE', #80293, .T. ) ;
#41948=EDGE_LOOP ( 'NONE', ( #90777, #25978, #71770, #68194 ) ) ;
#41952=CARTESIAN_POINT ( 'NONE',  ( -0.02075734969026423599, 5.866774720514426278, -0.08597719988137648983 ) ) ;
#41963=VECTOR ( 'NONE', #27277, 1000.000000000000000 ) ;
#41974=DIRECTION ( 'NONE',  ( 0.000000000000000000, -0.000000000000000000, -1.000000000000000000 ) ) ;
#41975=DIRECTION ( 'NONE',  ( 0.000000000000000000, 0.000000000000000000, 1.000000000000000000 ) ) ;
#41990=ORIENTED_EDGE ( 'NONE', *, *, #73705, .F. ) ;
#41995=CARTESIAN_POINT ( 'NONE',  ( 6.881670032588234953, 3.316774720514422903, -27.26384557944684062 ) ) ;
#42002=FACE_OUTER_BOUND ( 'NONE', #82808, .T. ) ;
#42025=EDGE_CURVE ( 'NONE', #72159, #16956, #36170, .T. ) ;
#42066=CARTESIAN_POINT ( 'NONE',  ( 33.61713288457014670, 3.416362262365323144, -11.96006463429725564 ) ) ;
#42086=CARTESIAN_POINT ( 'NONE',  ( -24.90875734969025501, 3.316774720514426456, 27.45402280011862572 ) ) ;
#42093=EDGE_LOOP ( 'NONE', ( #11917, #46189, #51839, #86553, #36506, #19471, #81272, #97726 ) ) ;
#42099=ORIENTED_EDGE ( 'NONE', *, *, #67550, .T. ) ;
#42118=ORIENTED_EDGE ( 'NONE', *, *, #2219, .F. ) ;
#42119=CIRCLE ( 'NONE', #25939, 1.835999999999993859 ) ;
#42120=EDGE_CURVE ( 'NONE', #67426, #12600, #82335, .T. ) ;
#42121=ORIENTED_EDGE ( 'NONE', *, *, #71711, .F. ) ;
#42151=DIRECTION ( 'NONE',  ( 1.000000000000000000, 0.000000000000000000, -0.000000000000000000 ) ) ;
#42179=CARTESIAN_POINT ( 'NONE',  ( -19.77875734969026311, -6.143225279485574397, 27.35402280011862430 ) ) ;
#42187=FACE_OUTER_BOUND ( 'NONE', #11797, .T. ) ;
#42195=DIRECTION ( 'NONE',  ( -0.000000000000000000, -1.000000000000000000, -0.000000000000000000 ) ) ;
#42200=CARTESIAN_POINT ( 'NONE',  ( 14.52861783435592713, 3.922795597835279313, -28.30212872328009510 ) ) ;
#42207=CARTESIAN_POINT ( 'NONE',  ( 31.67769140193662381, 4.988134948533209823, 28.98636546410035564 ) ) ;
#42211=CARTESIAN_POINT ( 'NONE',  ( 14.71033543815184252, 3.370934240161822526, -27.37556158125726213 ) ) ;
#42218=ORIENTED_EDGE ( 'NONE', *, *, #37906, .F. ) ;
#42240=DIRECTION ( 'NONE',  ( -0.1311553622875919756, 0.000000000000000000, -0.9913618264504692190 ) ) ;
#42277=CARTESIAN_POINT ( 'NONE',  ( 33.10875634548599322, -5.965225279485572685, -11.42349945801155719 ) ) ;
#42281=VERTEX_POINT ( 'NONE', #32758 ) ;
#42315=AXIS2_PLACEMENT_3D ( 'NONE', #91657, #90173, #76920 ) ;
#42325=CARTESIAN_POINT ( 'NONE',  ( 26.74698519091204574, -1.477225279485574028, -10.98683230472873973 ) ) ;
#42329=AXIS2_PLACEMENT_3D ( 'NONE', #36280, #67239, #99641 ) ;
#42335=CARTESIAN_POINT ( 'NONE',  ( 7.346158715828313923, 5.304593391634067068, -25.62898491049482885 ) ) ;
#42338=DIRECTION ( 'NONE',  ( 0.000000000000000000, 0.000000000000000000, 1.000000000000000000 ) ) ;
#42343=EDGE_CURVE ( 'NONE', #68827, #39091, #96135, .T. ) ;
#42345=LINE ( 'NONE', #19472, #77761 ) ;
#42352=CARTESIAN_POINT ( 'NONE',  ( -10.23311166579590825, 4.222446552888387217, 29.28685113854110966 ) ) ;
#42370=EDGE_LOOP ( 'NONE', ( #74319, #65067, #83762, #42493 ) ) ;
#42432=LINE ( 'NONE', #97192, #10264 ) ;
#42448=CARTESIAN_POINT ( 'NONE',  ( 30.53060340732036337, 1.682774720514426114, -8.442346167188908623 ) ) ;
#42453=VECTOR ( 'NONE', #14188, 1000.000000000000000 ) ;
#42463=EDGE_CURVE ( 'NONE', #61220, #36345, #21512, .T. ) ;
#42474=CARTESIAN_POINT ( 'NONE',  ( -12.84880425037202656, 0.3587747205143964613, -26.59900746623529244 ) ) ;
#42493=ORIENTED_EDGE ( 'NONE', *, *, #14470, .F. ) ;
#42524=CIRCLE ( 'NONE', #99199, 4.080000000000000071 ) ;
#42549=CARTESIAN_POINT ( 'NONE',  ( 16.09831413233135677, 3.622774720514429614, -27.82446136760824018 ) ) ;
#42555=LINE ( 'NONE', #12578, #55646 ) ;
#42581=EDGE_LOOP ( 'NONE', ( #43857, #100193, #83830, #78512, #73667, #74725, #68160, #53818, #91202, #99204 ) ) ;
#42618=VERTEX_POINT ( 'NONE', #18300 ) ;
#42632=ORIENTED_EDGE ( 'NONE', *, *, #59636, .F. ) ;
#42648=CARTESIAN_POINT ( 'NONE',  ( 14.76093561896379214, -5.965225279485572685, -26.55548769130089681 ) ) ;
#42666=DIRECTION ( 'NONE',  ( -0.1875268396392987258, -0.000000000000000000, -0.9822594791677485837 ) ) ;
#42669=ORIENTED_EDGE ( 'NONE', *, *, #63895, .F. ) ;
#42676=CYLINDRICAL_SURFACE ( 'NONE', #91418, 3.349999999999998757 ) ;
#42679=FACE_OUTER_BOUND ( 'NONE', #52689, .T. ) ;
#42681=CARTESIAN_POINT ( 'NONE',  ( -16.22218391600152643, 6.376774720514426953, -54.85883559227303863 ) ) ;
#42684=VECTOR ( 'NONE', #39731, 1000.000000000000114 ) ;
#42691=AXIS2_PLACEMENT_3D ( 'NONE', #59139, #82947, #75337 ) ;
#42693=VERTEX_POINT ( 'NONE', #74574 ) ;
#42702=CARTESIAN_POINT ( 'NONE',  ( 15.30286968208600307, 3.576092370626933636, -27.16555646467131524 ) ) ;
#42703=LINE ( 'NONE', #4129, #5896 ) ;
#42709=EDGE_LOOP ( 'NONE', ( #39024, #71404, #68329, #64072, #9859, #13548, #44840, #1668, #95886, #44561, #20098, #69134, #79153 ) ) ;
#42726=DIRECTION ( 'NONE',  ( 0.000000000000000000, 1.000000000000000000, 0.000000000000000000 ) ) ;
#42732=CARTESIAN_POINT ( 'NONE',  ( -25.92875734969025814, 3.316774720514426456, -0.08597719988137648983 ) ) ;
#42735=VERTEX_POINT ( 'NONE', #50753 ) ;
#42748=PLANE ( 'NONE',  #70644 ) ;
#42753=LINE ( 'NONE', #49872, #4172 ) ;
#42763=ADVANCED_FACE ( 'NONE', ( #88818 ), #2263, .F. ) ;
#42779=DIRECTION ( 'NONE',  ( -0.000000000000000000, 1.000000000000000000, -0.000000000000000000 ) ) ;
#42786=CARTESIAN_POINT ( 'NONE',  ( 19.75748517575715368, -5.965225279485572685, 28.87153971905864580 ) ) ;
#42795=ORIENTED_EDGE ( 'NONE', *, *, #78039, .T. ) ;
#42806=ORIENTED_EDGE ( 'NONE', *, *, #55786, .T. ) ;
#42812=DIRECTION ( 'NONE',  ( 0.000000000000000000, -1.000000000000000000, 0.000000000000000000 ) ) ;
#42817=CARTESIAN_POINT ( 'NONE',  ( 30.43908124610669930, 1.684774720514424784, -13.86910542224428866 ) ) ;
#42825=CARTESIAN_POINT ( 'NONE',  ( -28.98875734969026396, -5.965225279485572685, 10.11402280011862587 ) ) ;
#42827=LINE ( 'NONE', #11857, #67138 ) ;
#42840=ORIENTED_EDGE ( 'NONE', *, *, #97084, .T. ) ;
#42843=LINE ( 'NONE', #99088, #38345 ) ;
#42845=EDGE_CURVE ( 'NONE', #42876, #38457, #77059, .T. ) ;
#42848=ORIENTED_EDGE ( 'NONE', *, *, #14761, .T. ) ;
#42854=VECTOR ( 'NONE', #65902, 1000.000000000000114 ) ;
#42856=ORIENTED_EDGE ( 'NONE', *, *, #47259, .T. ) ;
#42876=VERTEX_POINT ( 'NONE', #46639 ) ;
#42880=DIRECTION ( 'NONE',  ( 0.000000000000000000, 0.000000000000000000, -1.000000000000000000 ) ) ;
#42885=ORIENTED_EDGE ( 'NONE', *, *, #2706, .F. ) ;
#42888=CARTESIAN_POINT ( 'NONE',  ( 7.732492002959944877, 5.356774720515138810, -27.16032169580908473 ) ) ;
#42897=CARTESIAN_POINT ( 'NONE',  ( 13.74975846015576586, -5.965225279485572685, -27.72022515045486557 ) ) ;
#42917=CARTESIAN_POINT ( 'NONE',  ( 0.000000000000000000, -6.943225279485572443, 0.000000000000000000 ) ) ;
#42928=VERTEX_POINT ( 'NONE', #446 ) ;
#42934=AXIS2_PLACEMENT_3D ( 'NONE', #63177, #94103, #86497 ) ;
#42941=DIRECTION ( 'NONE',  ( -0.000000000000000000, 1.000000000000000000, -0.000000000000000000 ) ) ;
#42943=CARTESIAN_POINT ( 'NONE',  ( -19.69812919673063689, 0.3587747205143964613, -22.00173861453436430 ) ) ;
#42944=CARTESIAN_POINT ( 'NONE',  ( -0.02075734969026423599, -5.965225279485572685, -29.05397719988136984 ) ) ;
#42949=EDGE_CURVE ( 'NONE', #3684, #52365, #8149, .T. ) ;
#42959=ORIENTED_EDGE ( 'NONE', *, *, #1325, .F. ) ;
#42962=PLANE ( 'NONE',  #30935 ) ;
#42964=ORIENTED_EDGE ( 'NONE', *, *, #87417, .T. ) ;
#42969=LINE ( 'NONE', #64832, #96650 ) ;
#42978=CARTESIAN_POINT ( 'NONE',  ( -11.64875734969026233, 0.3587747205144265483, 31.02402280011862246 ) ) ;
#42984=PLANE ( 'NONE',  #73703 ) ;
#42997=AXIS2_PLACEMENT_3D ( 'NONE', #4502, #75979, #12596 ) ;
#42999=VERTEX_POINT ( 'NONE', #70972 ) ;
#43006=ORIENTED_EDGE ( 'NONE', *, *, #46226, .T. ) ;
#43041=CARTESIAN_POINT ( 'NONE',  ( 11.44401587981593060, -6.475225279485572472, -27.05278809890034353 ) ) ;
#43080=VECTOR ( 'NONE', #90832, 999.9999999999998863 ) ;
#43106=VERTEX_POINT ( 'NONE', #8568 ) ;
#43112=PLANE ( 'NONE',  #86157 ) ;
#43140=CARTESIAN_POINT ( 'NONE',  ( 8.026968004785691946, 3.316774720514427344, -28.15626605682496830 ) ) ;
#43141=CARTESIAN_POINT ( 'NONE',  ( 5.271800844963591359, 3.316774720514426456, -28.56638892015329034 ) ) ;
#43165=EDGE_CURVE ( 'NONE', #95461, #99483, #27292, .T. ) ;
#43191=CARTESIAN_POINT ( 'NONE',  ( 14.76093561896379214, -6.475225279485574248, -26.55548769130089681 ) ) ;
#43194=CIRCLE ( 'NONE', #27034, 84.48086791635432746 ) ;
#43205=EDGE_CURVE ( 'NONE', #40372, #56438, #33041, .T. ) ;
#43224=CARTESIAN_POINT ( 'NONE',  ( 27.86270917940689174, 0.3587747205144265483, 29.49402280011862487 ) ) ;
#43247=AXIS2_PLACEMENT_3D ( 'NONE', #12989, #28226, #41975 ) ;
#43264=ORIENTED_EDGE ( 'NONE', *, *, #92979, .F. ) ;
#43269=CARTESIAN_POINT ( 'NONE',  ( 13.91401389203221406, -5.965225279485572685, 158.0376437107427137 ) ) ;
#43271=ORIENTED_EDGE ( 'NONE', *, *, #21343, .F. ) ;
#43273=CARTESIAN_POINT ( 'NONE',  ( 10.73203334292264088, 3.902996417034998000, -26.95265065337511601 ) ) ;
#43286=CARTESIAN_POINT ( 'NONE',  ( 30.93860345374796594, -6.475225279485573360, 20.86760796525322093 ) ) ;
#43289=EDGE_CURVE ( 'NONE', #64548, #64559, #20068, .T. ) ;
#43293=CARTESIAN_POINT ( 'NONE',  ( 7.347880794884120722E-16, 1.826774720514426464, -6.000000000000000888 ) ) ;
#43315=AXIS2_PLACEMENT_3D ( 'NONE', #89058, #56624, #40877 ) ;
#43321=EDGE_CURVE ( 'NONE', #37593, #5624, #26789, .T. ) ;
#43329=DIRECTION ( 'NONE',  ( -0.000000000000000000, 1.000000000000000000, -0.000000000000000000 ) ) ;
#43359=CIRCLE ( 'NONE', #27127, 251.4258649670780699 ) ;
#43367=CARTESIAN_POINT ( 'NONE',  ( 15.30881860688521989, 3.493868136757170451, -27.16033061360459300 ) ) ;
#43369=ORIENTED_EDGE ( 'NONE', *, *, #93085, .T. ) ;
#43379=CARTESIAN_POINT ( 'NONE',  ( 31.52236416363829363, 4.132774720514426292, -3.023391441407382807 ) ) ;
#43392=DIRECTION ( 'NONE',  ( -0.000000000000000000, -1.000000000000000000, 0.000000000000000000 ) ) ;
#43413=EDGE_CURVE ( 'NONE', #54573, #44858, #14545, .T. ) ;
#43421=DIRECTION ( 'NONE',  ( -0.000000000000000000, 1.000000000000000000, -0.000000000000000000 ) ) ;
#43425=DIRECTION ( 'NONE',  ( -0.000000000000000000, -1.000000000000000000, -0.000000000000000000 ) ) ;
#43429=CARTESIAN_POINT ( 'NONE',  ( 30.60111574538730039, 4.387371784078713866, 26.76015704162893627 ) ) ;
#43434=ORIENTED_EDGE ( 'NONE', *, *, #16675, .F. ) ;
#43448=PLANE ( 'NONE',  #73838 ) ;
#43451=CARTESIAN_POINT ( 'NONE',  ( 5.109298100548420152, 3.316774720514426456, -27.55941679637948383 ) ) ;
#43471=VERTEX_POINT ( 'NONE', #52126 ) ;
#43478=VERTEX_POINT ( 'NONE', #59745 ) ;
#43485=VERTEX_POINT ( 'NONE', #6444 ) ;
#43490=VECTOR ( 'NONE', #54513, 1000.000000000000227 ) ;
#43504=EDGE_LOOP ( 'NONE', ( #391, #30851, #48845, #52083 ) ) ;
#43508=CARTESIAN_POINT ( 'NONE',  ( -29.49875734969026198, -5.965225279485572685, 0.1180228001186258285 ) ) ;
#43511=CIRCLE ( 'NONE', #6188, 84.48086791635432746 ) ;
#43532=DIRECTION ( 'NONE',  ( 0.000000000000000000, 0.000000000000000000, -1.000000000000000000 ) ) ;
#43536=CARTESIAN_POINT ( 'NONE',  ( 13.74975846015576586, -5.965225279485572685, -27.72022515045486557 ) ) ;
#43538=CARTESIAN_POINT ( 'NONE',  ( 15.99960863614631101, 3.577630190450212577, -27.91116951066581819 ) ) ;
#43546=ORIENTED_EDGE ( 'NONE', *, *, #84278, .F. ) ;
#43567=ORIENTED_EDGE ( 'NONE', *, *, #67550, .F. ) ;
#43568=ORIENTED_EDGE ( 'NONE', *, *, #97272, .T. ) ;
#43586=ORIENTED_EDGE ( 'NONE', *, *, #88387, .T. ) ;
#43590=ADVANCED_FACE ( 'NONE', ( #4832 ), #89071, .T. ) ;
#43601=CARTESIAN_POINT ( 'NONE',  ( 15.63605935613269438, -5.965225279485572685, -27.55169773172585934 ) ) ;
#43602=VERTEX_POINT ( 'NONE', #19547 ) ;
#43616=CARTESIAN_POINT ( 'NONE',  ( 10.62437663934349530, -6.475225279485576024, -27.03002426119959978 ) ) ;
#43624=FACE_OUTER_BOUND ( 'NONE', #31322, .T. ) ;
#43630=LINE ( 'NONE', #57380, #69767 ) ;
#43647=DIRECTION ( 'NONE',  ( -0.9994733861282923959, -0.000000000000000000, -0.03244919754393515293 ) ) ;
#43651=VERTEX_POINT ( 'NONE', #51511 ) ;
#43657=VECTOR ( 'NONE', #92055, 1000.000000000000000 ) ;
#43658=EDGE_LOOP ( 'NONE', ( #91318, #61794, #78780, #66197, #99186, #19858, #91520, #24642, #57108, #87331, #70295 ) ) ;
#43661=CARTESIAN_POINT ( 'NONE',  ( 31.61049571213237641, 4.540774720514426654, 26.28206907949443050 ) ) ;
#43666=PLANE ( 'NONE',  #9440 ) ;
#43674=ORIENTED_EDGE ( 'NONE', *, *, #84833, .T. ) ;
#43681=AXIS2_PLACEMENT_3D ( 'NONE', #84258, #84762, #60944 ) ;
#43682=CARTESIAN_POINT ( 'NONE',  ( -27.25988310792305214, 0.3587747205144265483, 30.32664379231667695 ) ) ;
#43732=CARTESIAN_POINT ( 'NONE',  ( 10.86264265030973952, -5.965225279485574461, -28.05717073599341305 ) ) ;
#43736=EDGE_CURVE ( 'NONE', #44198, #55557, #43895, .T. ) ;
#43741=CARTESIAN_POINT ( 'NONE',  ( -28.98875734969026396, 0.3587747205144262708, 7.870022800118625206 ) ) ;
#43767=CARTESIAN_POINT ( 'NONE',  ( 10.84340024150424497, 4.021317321268781164, -26.91457715659927175 ) ) ;
#43771=ADVANCED_FACE ( 'NONE', ( #38261 ), #69219, .T. ) ;
#43772=EDGE_LOOP ( 'NONE', ( #17983, #12810, #27599, #37200 ) ) ;
#43794=ORIENTED_EDGE ( 'NONE', *, *, #7856, .F. ) ;
#43810=AXIS2_PLACEMENT_3D ( 'NONE', #100189, #78367, #99697 ) ;
#43815=LINE ( 'NONE', #6736, #62415 ) ;
#43827=DIRECTION ( 'NONE',  ( 1.000000000000000000, 4.015954566446630556E-15, 0.000000000000000000 ) ) ;
#43840=ORIENTED_EDGE ( 'NONE', *, *, #80136, .T. ) ;
#43843=VERTEX_POINT ( 'NONE', #94050 ) ;
#43857=ORIENTED_EDGE ( 'NONE', *, *, #90940, .F. ) ;
#43877=CARTESIAN_POINT ( 'NONE',  ( 8.720390671778812219, 3.316774720514306996, -27.07197491306147086 ) ) ;
#43884=VERTEX_POINT ( 'NONE', #16416 ) ;
#43895=LINE ( 'NONE', #45398, #15033 ) ;
#43903=DIRECTION ( 'NONE',  ( -1.000000000000000000, 0.000000000000000000, 0.000000000000000000 ) ) ;
#43913=CARTESIAN_POINT ( 'NONE',  ( 31.73616390345410920, 3.909076239803030539, -3.851095480477756627 ) ) ;
#43918=CARTESIAN_POINT ( 'NONE',  ( 30.64109437917162637, 3.603390417177663174, 28.31981403122773955 ) ) ;
#43962=CARTESIAN_POINT ( 'NONE',  ( -65.05438548721848235, 5.356774720514425603, 0.7300228001186309656 ) ) ;
#43980=ORIENTED_EDGE ( 'NONE', *, *, #72599, .T. ) ;
#43981=AXIS2_PLACEMENT_3D ( 'NONE', #90304, #13166, #20774 ) ;
#43982=ORIENTED_EDGE ( 'NONE', *, *, #62068, .F. ) ;
#43986=CARTESIAN_POINT ( 'NONE',  ( -24.90875734969025501, 6.376774720514426953, 26.43402280011862615 ) ) ;
#44003=AXIS2_PLACEMENT_3D ( 'NONE', #8401, #47474, #53601 ) ;
#44030=LINE ( 'NONE', #22172, #39481 ) ;
#44034=SHAPE_REPRESENTATION ( 'Plastic Part 1', ( #37391 ), #11455 ) ;
#44039=EDGE_CURVE ( 'NONE', #16877, #44339, #41790, .T. ) ;
#44048=DIRECTION ( 'NONE',  ( 0.000000000000000000, 0.000000000000000000, 1.000000000000000000 ) ) ;
#44051=DIRECTION ( 'NONE',  ( -1.000000000000000000, -0.000000000000000000, 0.000000000000000000 ) ) ;
#44056=VERTEX_POINT ( 'NONE', #66135 ) ;
#44095=DIRECTION ( 'NONE',  ( 0.000000000000000000, 0.000000000000000000, -1.000000000000000000 ) ) ;
#44101=VERTEX_POINT ( 'NONE', #74702 ) ;
#44110=CARTESIAN_POINT ( 'NONE',  ( 13.91401389203221406, -6.475225279485573360, 27.24920385068457662 ) ) ;
#44112=DIRECTION ( 'NONE',  ( -0.000000000000000000, -1.000000000000000000, 0.000000000000000000 ) ) ;
#44114=CARTESIAN_POINT ( 'NONE',  ( 9.016989526679575206, -6.475225279485574248, -27.05137190084761301 ) ) ;
#44120=CARTESIAN_POINT ( 'NONE',  ( 11.94353453780502683, 5.048182838635504766, -26.89061828217040784 ) ) ;
#44121=DIRECTION ( 'NONE',  ( 0.000000000000000000, 0.000000000000000000, -1.000000000000000000 ) ) ;
#44146=CARTESIAN_POINT ( 'NONE',  ( 32.53135143123563466, -5.965225279485572685, 6.926385399448451885 ) ) ;
#44147=LINE ( 'NONE', #52757, #73396 ) ;
#44157=CARTESIAN_POINT ( 'NONE',  ( 31.63608488009066733, 3.316774720514426456, 27.34773273846990094 ) ) ;
#44158=FACE_OUTER_BOUND ( 'NONE', #72321, .T. ) ;
#44166=EDGE_CURVE ( 'NONE', #15254, #51264, #22402, .T. ) ;
#44198=VERTEX_POINT ( 'NONE', #70101 ) ;
#44199=AXIS2_PLACEMENT_3D ( 'NONE', #2475, #65398, #25803 ) ;
#44201=CARTESIAN_POINT ( 'NONE',  ( 29.68479148105952348, -1.477225279485574028, -9.431263391055122014 ) ) ;
#44219=DIRECTION ( 'NONE',  ( 0.000000000000000000, 0.000000000000000000, -1.000000000000000000 ) ) ;
#44222=ORIENTED_EDGE ( 'NONE', *, *, #75182, .F. ) ;
#44223=ORIENTED_EDGE ( 'NONE', *, *, #34333, .T. ) ;
#44239=CARTESIAN_POINT ( 'NONE',  ( -0.02075734969026145696, 5.866774720514426278, -22.78097719988138081 ) ) ;
#44245=DIRECTION ( 'NONE',  ( -1.000000000000000000, 0.000000000000000000, -0.000000000000000000 ) ) ;
#44263=TOROIDAL_SURFACE ( 'NONE', #39403, 253.2618649670780826, 1.835999999999999854 ) ;
#44270=AXIS2_PLACEMENT_3D ( 'NONE', #42917, #49536, #34798 ) ;
#44281=EDGE_CURVE ( 'NONE', #18260, #68279, #46768, .T. ) ;
#44288=DIRECTION ( 'NONE',  ( 0.000000000000000000, 1.000000000000000000, 0.000000000000000000 ) ) ;
#44306=CARTESIAN_POINT ( 'NONE',  ( 14.87948092214613460, 4.970807589639875346, -27.40745209048265352 ) ) ;
#44309=VERTEX_POINT ( 'NONE', #94431 ) ;
#44320=CARTESIAN_POINT ( 'NONE',  ( 30.93860345374796594, -6.475225279485573360, 19.84760796525321780 ) ) ;
#44327=CARTESIAN_POINT ( 'NONE',  ( 22.81105451610979173, 1.682774720514426114, -18.46691820600746681 ) ) ;
#44332=ORIENTED_EDGE ( 'NONE', *, *, #94097, .T. ) ;
#44339=VERTEX_POINT ( 'NONE', #88 ) ;
#44340=FACE_OUTER_BOUND ( 'NONE', #10114, .T. ) ;
#44348=ORIENTED_EDGE ( 'NONE', *, *, #12661, .T. ) ;
#44364=DIRECTION ( 'NONE',  ( -1.000000000000000000, 0.000000000000000000, 0.000000000000000000 ) ) ;
#44365=CARTESIAN_POINT ( 'NONE',  ( 14.62591090210861999, 3.611920024593927803, -27.34381298535168270 ) ) ;
#44368=ORIENTED_EDGE ( 'NONE', *, *, #85601, .T. ) ;
#44388=AXIS2_PLACEMENT_3D ( 'NONE', #10990, #12484, #74871 ) ;
#44390=ORIENTED_EDGE ( 'NONE', *, *, #30315, .T. ) ;
#44428=CYLINDRICAL_SURFACE ( 'NONE', #78748, 3.500000000000000000 ) ;
#44448=EDGE_LOOP ( 'NONE', ( #24120, #45329, #44348, #37747 ) ) ;
#44459=EDGE_CURVE ( 'NONE', #87661, #95272, #573, .T. ) ;
#44498=DIRECTION ( 'NONE',  ( -0.000000000000000000, -1.000000000000000000, -0.000000000000000000 ) ) ;
#44509=VECTOR ( 'NONE', #30545, 1000.000000000000000 ) ;
#44511=FACE_OUTER_BOUND ( 'NONE', #5992, .T. ) ;
#44530=DIRECTION ( 'NONE',  ( 0.000000000000000000, 1.000000000000000000, 0.000000000000000000 ) ) ;
#44538=CARTESIAN_POINT ( 'NONE',  ( 32.16024265030974050, 0.3587747205144265483, 16.27760796525321751 ) ) ;
#44541=ORIENTED_EDGE ( 'NONE', *, *, #74793, .F. ) ;
#44554=CARTESIAN_POINT ( 'NONE',  ( 11.04644962722740864, 4.132774720514426292, -26.87113206189456704 ) ) ;
#44561=ORIENTED_EDGE ( 'NONE', *, *, #79437, .T. ) ;
#44563=VERTEX_POINT ( 'NONE', #48786 ) ;
#44564=EDGE_CURVE ( 'NONE', #5126, #79593, #37786, .T. ) ;
#44568=ORIENTED_EDGE ( 'NONE', *, *, #9583, .T. ) ;
#44569=CARTESIAN_POINT ( 'NONE',  ( 29.70220533433690946, 3.451715827188561736, 28.20564067601642222 ) ) ;
#44571=EDGE_CURVE ( 'NONE', #10266, #44198, #52350, .T. ) ;
#44596=DIRECTION ( 'NONE',  ( 4.015954566446630556E-15, -1.000000000000000000, 1.297050502119899750E-15 ) ) ;
#44598=ORIENTED_EDGE ( 'NONE', *, *, #62086, .T. ) ;
#44602=EDGE_CURVE ( 'NONE', #42281, #57513, #65355, .T. ) ;
#44605=ORIENTED_EDGE ( 'NONE', *, *, #522, .T. ) ;
#44609=EDGE_CURVE ( 'NONE', #74213, #39929, #21663, .T. ) ;
#44611=CARTESIAN_POINT ( 'NONE',  ( -29.49875734969025842, 0.3587747205144262708, 23.37402280011862743 ) ) ;
#44634=LINE ( 'NONE', #98400, #22865 ) ;
#44638=ORIENTED_EDGE ( 'NONE', *, *, #67775, .F. ) ;
#44663=EDGE_CURVE ( 'NONE', #24863, #61929, #78255, .T. ) ;
#44666=VERTEX_POINT ( 'NONE', #49039 ) ;
#44675=LINE ( 'NONE', #68504, #1465 ) ;
#44686=ORIENTED_EDGE ( 'NONE', *, *, #73265, .F. ) ;
#44693=ORIENTED_EDGE ( 'NONE', *, *, #29316, .T. ) ;
#44712=ORIENTED_EDGE ( 'NONE', *, *, #92415, .F. ) ;
#44714=CARTESIAN_POINT ( 'NONE',  ( 32.15269211224249091, 4.540774720514427543, 3.401810532325273417 ) ) ;
#44724=TOROIDAL_SURFACE ( 'NONE', #15517, 132.8284398600581540, 2.040000000000000036 ) ;
#44727=LINE ( 'NONE', #99979, #67977 ) ;
#44767=CARTESIAN_POINT ( 'NONE',  ( -41.32836283488544638, 2.682774720514426559, 39.26872235229541985 ) ) ;
#44768=EDGE_CURVE ( 'NONE', #91326, #12744, #59141, .T. ) ;
#44774=PLANE ( 'NONE',  #676 ) ;
#44782=ORIENTED_EDGE ( 'NONE', *, *, #64574, .T. ) ;
#44787=LINE ( 'NONE', #84325, #15118 ) ;
#44790=EDGE_CURVE ( 'NONE', #78621, #31830, #42432, .T. ) ;
#44793=AXIS2_PLACEMENT_3D ( 'NONE', #86810, #41153, #49276 ) ;
#44805=DIRECTION ( 'NONE',  ( 0.000000000000000000, 1.000000000000000000, -0.000000000000000000 ) ) ;
#44821=ORIENTED_EDGE ( 'NONE', *, *, #12466, .T. ) ;
#44836=CARTESIAN_POINT ( 'NONE',  ( 282.9764569301858046, -5.965225279485572685, 20.79159422840526616 ) ) ;
#44838=CIRCLE ( 'NONE', #27018, 91.74549126261076992 ) ;
#44840=ORIENTED_EDGE ( 'NONE', *, *, #52750, .F. ) ;
#44858=VERTEX_POINT ( 'NONE', #26185 ) ;
#44865=AXIS2_PLACEMENT_3D ( 'NONE', #48512, #79440, #93154 ) ;
#44874=CARTESIAN_POINT ( 'NONE',  ( 33.34043384136949584, 4.658726884274782876, -12.67806891602221064 ) ) ;
#44882=AXIS2_PLACEMENT_3D ( 'NONE', #71939, #96756, #72436 ) ;
#44887=VECTOR ( 'NONE', #45133, 1000.000000000000000 ) ;
#44919=EDGE_CURVE ( 'NONE', #9882, #57723, #79938, .T. ) ;
#44926=CARTESIAN_POINT ( 'NONE',  ( 30.59918777245023236, 5.333550415411136392, 26.68477081578061316 ) ) ;
#44969=DIRECTION ( 'NONE',  ( 0.000000000000000000, -0.000000000000000000, 1.000000000000000000 ) ) ;
#44974=CARTESIAN_POINT ( 'NONE',  ( 22.81105451610979173, -1.475225279485572916, -19.61691820600746539 ) ) ;
#44975=DIRECTION ( 'NONE',  ( -0.000000000000000000, 1.000000000000000000, -0.000000000000000000 ) ) ;
#44987=ADVANCED_FACE ( 'NONE', ( #60643 ), #75838, .F. ) ;
#44996=DIRECTION ( 'NONE',  ( 0.000000000000000000, 0.000000000000000000, 1.000000000000000000 ) ) ;
#44997=ORIENTED_EDGE ( 'NONE', *, *, #98696, .T. ) ;
#45002=ORIENTED_EDGE ( 'NONE', *, *, #29941, .F. ) ;
#45025=DIRECTION ( 'NONE',  ( 0.000000000000000000, 1.000000000000000000, 0.000000000000000000 ) ) ;
#45026=ORIENTED_EDGE ( 'NONE', *, *, #99188, .F. ) ;
#45045=DIRECTION ( 'NONE',  ( 0.000000000000000000, 0.000000000000000000, -1.000000000000000000 ) ) ;
#45049=CARTESIAN_POINT ( 'NONE',  ( 32.48849721025742099, 4.168223360657076881, -0.9137309853436130780 ) ) ;
#45062=LINE ( 'NONE', #38931, #18703 ) ;
#45065=CARTESIAN_POINT ( 'NONE',  ( -20.77875734969026311, 3.316774720514426456, 29.49402280011862487 ) ) ;
#45078=VECTOR ( 'NONE', #35290, 1000.000000000000114 ) ;
#45084=DIRECTION ( 'NONE',  ( 0.000000000000000000, -0.000000000000000000, -1.000000000000000000 ) ) ;
#45092=EDGE_LOOP ( 'NONE', ( #65333, #35313, #90660 ) ) ;
#45106=ORIENTED_EDGE ( 'NONE', *, *, #34880, .T. ) ;
#45109=ORIENTED_EDGE ( 'NONE', *, *, #18183, .F. ) ;
#45125=VERTEX_POINT ( 'NONE', #9831 ) ;
#45126=CARTESIAN_POINT ( 'NONE',  ( 11.56983764158150407, 6.376774720514426953, 28.29037853177889517 ) ) ;
#45133=DIRECTION ( 'NONE',  ( -0.000000000000000000, -1.000000000000000000, -0.000000000000000000 ) ) ;
#45161=ORIENTED_EDGE ( 'NONE', *, *, #41585, .T. ) ;
#45172=VECTOR ( 'NONE', #63524, 1000.000000000000000 ) ;
#45176=DIRECTION ( 'NONE',  ( 0.7071067811865476838, 0.000000000000000000, -0.7071067811865474617 ) ) ;
#45177=CARTESIAN_POINT ( 'NONE',  ( -24.55517127435777525, 0.3587747205143967943, -15.44180958690143157 ) ) ;
#45178=ADVANCED_FACE ( 'NONE', ( #62634 ), #16942, .F. ) ;
#45181=EDGE_LOOP ( 'NONE', ( #31985, #52449, #55184, #22891 ) ) ;
#45189=CARTESIAN_POINT ( 'NONE',  ( -2.872281323269014752, -16.94322527948557422, 1.999999999999999556 ) ) ;
#45199=CARTESIAN_POINT ( 'NONE',  ( 33.61456970919605425, 3.316774720514426900, -11.35828564741663449 ) ) ;
#45234=ORIENTED_EDGE ( 'NONE', *, *, #48921, .T. ) ;
#45254=ORIENTED_EDGE ( 'NONE', *, *, #25149, .F. ) ;
#45281=AXIS2_PLACEMENT_3D ( 'NONE', #69041, #39592, #15249 ) ;
#45288=CIRCLE ( 'NONE', #14493, 132.8284398600581824 ) ;
#45295=ORIENTED_EDGE ( 'NONE', *, *, #30058, .F. ) ;
#45308=EDGE_CURVE ( 'NONE', #18260, #18475, #44787, .T. ) ;
#45309=CARTESIAN_POINT ( 'NONE',  ( 2.872281323269014752, 4.293056017849825601, 1.999999999999999556 ) ) ;
#45322=CARTESIAN_POINT ( 'NONE',  ( -19.80875734969026425, -5.965225279485572685, 30.51402280011862089 ) ) ;
#45329=ORIENTED_EDGE ( 'NONE', *, *, #27367, .T. ) ;
#45334=CARTESIAN_POINT ( 'NONE',  ( -17.97250661212648026, -5.965225279485594001, -23.43622901028613015 ) ) ;
#45340=CIRCLE ( 'NONE', #56731, 1.325999999999990298 ) ;
#45358=CARTESIAN_POINT ( 'NONE',  ( 26.73860345374794178, 5.356774720496559894, 19.84760796525321780 ) ) ;
#45361=EDGE_CURVE ( 'NONE', #66086, #56438, #15312, .T. ) ;
#45365=ORIENTED_EDGE ( 'NONE', *, *, #71662, .T. ) ;
#45375=CARTESIAN_POINT ( 'NONE',  ( 32.90449424769446551, 3.618459821963367240, -13.06102137676440300 ) ) ;
#45389=LINE ( 'NONE', #12915, #20196 ) ;
#45398=CARTESIAN_POINT ( 'NONE',  ( 17.47419131657910540, 6.376774720514426953, 28.31804950686278843 ) ) ;
#45401=CARTESIAN_POINT ( 'NONE',  ( 30.93860345374796594, -6.475225279485573360, 25.41160796525322141 ) ) ;
#45420=EDGE_CURVE ( 'NONE', #45969, #19596, #69405, .T. ) ;
#45421=CIRCLE ( 'NONE', #98857, 7.652410033082763796 ) ;
#45441=VECTOR ( 'NONE', #94709, 1000.000000000000227 ) ;
#45453=ORIENTED_EDGE ( 'NONE', *, *, #46736, .F. ) ;
#45472=EDGE_LOOP ( 'NONE', ( #75016, #47323, #47254, #31615, #41202, #79396 ) ) ;
#45493=EDGE_CURVE ( 'NONE', #68827, #17038, #13149, .T. ) ;
#45496=CARTESIAN_POINT ( 'NONE',  ( -25.92875734969026524, 5.356774720514425603, 0.7300228001186309656 ) ) ;
#45507=AXIS2_PLACEMENT_3D ( 'NONE', #92406, #46244, #69589 ) ;
#45510=VECTOR ( 'NONE', #96600, 1000.000000000000000 ) ;
#45523=ORIENTED_EDGE ( 'NONE', *, *, #13967, .F. ) ;
#45538=ORIENTED_EDGE ( 'NONE', *, *, #61772, .F. ) ;
#45560=DIRECTION ( 'NONE',  ( 0.000000000000000000, 0.000000000000000000, -1.000000000000000000 ) ) ;
#45565=ORIENTED_EDGE ( 'NONE', *, *, #34880, .F. ) ;
#45578=VECTOR ( 'NONE', #26161, 1000.000000000000000 ) ;
#45584=CARTESIAN_POINT ( 'NONE',  ( 14.43441819135929194, 3.316774720514426456, -28.36222020317710957 ) ) ;
#45586=ORIENTED_EDGE ( 'NONE', *, *, #7856, .T. ) ;
#45601=ORIENTED_EDGE ( 'NONE', *, *, #5664, .F. ) ;
#45602=EDGE_LOOP ( 'NONE', ( #16229, #52214, #77997, #46834, #7374, #7107, #17342, #6790, #14130, #86613, #36964, #38840, #80675, #51045, #22212, #27994 ) ) ;
#45610=CARTESIAN_POINT ( 'NONE',  ( 5.184553252003285984, -5.965225279485572685, -28.06387035751381731 ) ) ;
#45619=CARTESIAN_POINT ( 'NONE',  ( 13.59451591917074431, 3.316774720514426456, -28.23515841827053308 ) ) ;
#45620=CARTESIAN_POINT ( 'NONE',  ( 25.61870917940689196, -5.965225279485572685, 29.49402280011862487 ) ) ;
#45626=CARTESIAN_POINT ( 'NONE',  ( 3.509873074917118085, 0.3587747205144265483, 29.15869884040363758 ) ) ;
#45637=EDGE_LOOP ( 'NONE', ( #18847, #36828, #6418, #5895 ) ) ;
#45638=DIRECTION ( 'NONE',  ( 0.000000000000000000, 0.000000000000000000, 1.000000000000000000 ) ) ;
#45639=CARTESIAN_POINT ( 'NONE',  ( 12.66784028006542151, 2.682774720514427003, -27.12025593822526304 ) ) ;
#45655=DIRECTION ( 'NONE',  ( 0.000000000000000000, 0.000000000000000000, 1.000000000000000000 ) ) ;
#45660=DIRECTION ( 'NONE',  ( -0.000000000000000000, 1.000000000000000000, -0.000000000000000000 ) ) ;
#45662=EDGE_LOOP ( 'NONE', ( #27218, #89373, #89261, #27101, #10490, #34562, #23815, #45002 ) ) ;
#45667=DIRECTION ( 'NONE',  ( -0.000000000000000000, -1.000000000000000000, -0.000000000000000000 ) ) ;
#45672=DIRECTION ( 'NONE',  ( 0.000000000000000000, 0.000000000000000000, -1.000000000000000000 ) ) ;
#45675=DIRECTION ( 'NONE',  ( -0.000000000000000000, 1.000000000000000000, -0.000000000000000000 ) ) ;
#45676=VERTEX_POINT ( 'NONE', #80558 ) ;
#45687=ORIENTED_EDGE ( 'NONE', *, *, #68898, .T. ) ;
#45694=ORIENTED_EDGE ( 'NONE', *, *, #77944, .F. ) ;
#45709=VERTEX_POINT ( 'NONE', #89176 ) ;
#45730=CARTESIAN_POINT ( 'NONE',  ( 27.53860345374808105, 3.356774720514427379, 1.647607965253216067 ) ) ;
#45747=CARTESIAN_POINT ( 'NONE',  ( 13.91401389203221406, 0.3587747205144265483, 158.0376437107427137 ) ) ;
#45757=CARTESIAN_POINT ( 'NONE',  ( 10.93823315965619791, 6.376774720514427841, -24.99764212866241309 ) ) ;
#45758=DIRECTION ( 'NONE',  ( 0.000000000000000000, -1.000000000000000000, 0.000000000000000000 ) ) ;
#45772=ORIENTED_EDGE ( 'NONE', *, *, #22832, .T. ) ;
#45773=VECTOR ( 'NONE', #88319, 1000.000000000000000 ) ;
#45781=ADVANCED_FACE ( 'NONE', ( #20149 ), #3948, .T. ) ;
#45792=CARTESIAN_POINT ( 'NONE',  ( -29.49875734969025842, 0.3587747205144262708, 15.62202280011862321 ) ) ;
#45794=VERTEX_POINT ( 'NONE', #82057 ) ;
#45802=AXIS2_PLACEMENT_3D ( 'NONE', #83549, #98769, #96917 ) ;
#45804=EDGE_LOOP ( 'NONE', ( #60928, #79152, #28197, #12857 ) ) ;
#45821=CARTESIAN_POINT ( 'NONE',  ( 5.717391271363888805, 6.376774720514426953, -25.39218285751184467 ) ) ;
#45825=VERTEX_POINT ( 'NONE', #34390 ) ;
#45848=ORIENTED_EDGE ( 'NONE', *, *, #39227, .F. ) ;
#45854=CIRCLE ( 'NONE', #55569, 1.836000000000000743 ) ;
#45857=CARTESIAN_POINT ( 'NONE',  ( 30.93860345374796594, 0.6647747205144264315, 19.84760796525321780 ) ) ;
#45901=VECTOR ( 'NONE', #79390, 1000.000000000000000 ) ;
#45907=CARTESIAN_POINT ( 'NONE',  ( 33.00535138976610483, -5.965225279485572685, -12.97242311383961066 ) ) ;
#45916=EDGE_CURVE ( 'NONE', #82569, #91875, #69888, .T. ) ;
#45939=VECTOR ( 'NONE', #91067, 1000.000000000000000 ) ;
#45940=VERTEX_POINT ( 'NONE', #16093 ) ;
#45943=VERTEX_POINT ( 'NONE', #7477 ) ;
#45952=ORIENTED_EDGE ( 'NONE', *, *, #39411, .T. ) ;
#45954=DIRECTION ( 'NONE',  ( -0.02119372647573786531, -9.594337693711052596E-15, -0.9997753877537052247 ) ) ;
#45969=VERTEX_POINT ( 'NONE', #54182 ) ;
#45978=CARTESIAN_POINT ( 'NONE',  ( -28.98875734969026396, -5.965225279485572685, 10.11402280011862587 ) ) ;
#45984=CIRCLE ( 'NONE', #21621, 1.150000000000003464 ) ;
#45994=ORIENTED_EDGE ( 'NONE', *, *, #6609, .T. ) ;
#45998=EDGE_CURVE ( 'NONE', #63531, #149, #25708, .T. ) ;
#46007=FACE_OUTER_BOUND ( 'NONE', #29011, .T. ) ;
#46029=EDGE_CURVE ( 'NONE', #60699, #17009, #45984, .T. ) ;
#46037=FACE_OUTER_BOUND ( 'NONE', #42370, .T. ) ;
#46046=CARTESIAN_POINT ( 'NONE',  ( 30.32108885906865936, 6.376774720514427841, 3.274824222184972822 ) ) ;
#46047=EDGE_CURVE ( 'NONE', #74508, #89020, #29750, .T. ) ;
#46053=CARTESIAN_POINT ( 'NONE',  ( -0.02075734969026423599, -5.965225279485572685, -0.08597719988137648983 ) ) ;
#46082=DIRECTION ( 'NONE',  ( 0.000000000000000000, 0.000000000000000000, -1.000000000000000000 ) ) ;
#46088=DIRECTION ( 'NONE',  ( 0.000000000000000000, 0.000000000000000000, -1.000000000000000000 ) ) ;
#46105=CARTESIAN_POINT ( 'NONE',  ( 1.305682803664691249, 0.3587747205144265483, 29.57950906855421991 ) ) ;
#46122=DIRECTION ( 'NONE',  ( 0.000000000000000000, 0.000000000000000000, -1.000000000000000000 ) ) ;
#46128=CARTESIAN_POINT ( 'NONE',  ( -17.66201745896767505, 6.376774720514425177, -23.06272557202527906 ) ) ;
#46143=DIRECTION ( 'NONE',  ( -0.000000000000000000, 1.000000000000000000, -0.000000000000000000 ) ) ;
#46153=ORIENTED_EDGE ( 'NONE', *, *, #69511, .F. ) ;
#46180=VERTEX_POINT ( 'NONE', #43451 ) ;
#46189=ORIENTED_EDGE ( 'NONE', *, *, #95468, .T. ) ;
#46204=EDGE_CURVE ( 'NONE', #98622, #82569, #36271, .T. ) ;
#46209=TOROIDAL_SURFACE ( 'NONE', #2478, 80.18232118519038920, 8.160000000000000142 ) ;
#46223=CARTESIAN_POINT ( 'NONE',  ( -25.92875734969025814, 3.316774720514426456, 23.50402280011861933 ) ) ;
#46225=DIRECTION ( 'NONE',  ( 0.9921023176230513441, 0.000000000000000000, -0.1254312216594016538 ) ) ;
#46226=EDGE_CURVE ( 'NONE', #88353, #79519, #98204, .T. ) ;
#46229=DIRECTION ( 'NONE',  ( -0.1254312216594016538, -0.000000000000000000, -0.9921023176230513441 ) ) ;
#46244=DIRECTION ( 'NONE',  ( -0.000000000000000000, 1.000000000000000000, -0.000000000000000000 ) ) ;
#46262=DIRECTION ( 'NONE',  ( 0.000000000000000000, 0.000000000000000000, 1.000000000000000000 ) ) ;
#46276=CARTESIAN_POINT ( 'NONE',  ( 22.02124265030973760, -4.543225279485573864, 15.05402280011862004 ) ) ;
#46301=ORIENTED_EDGE ( 'NONE', *, *, #83075, .F. ) ;
#46329=ORIENTED_EDGE ( 'NONE', *, *, #81386, .F. ) ;
#46347=EDGE_LOOP ( 'NONE', ( #26932, #63302, #12975, #39708 ) ) ;
#46355=DIRECTION ( 'NONE',  ( 0.000000000000000000, 0.000000000000000000, 1.000000000000000000 ) ) ;
#46364=ORIENTED_EDGE ( 'NONE', *, *, #31456, .F. ) ;
#46367=AXIS2_PLACEMENT_3D ( 'NONE', #26684, #34298, #71360 ) ;
#46372=EDGE_LOOP ( 'NONE', ( #78867, #79940, #43434, #80382 ) ) ;
#46374=DIRECTION ( 'NONE',  ( 0.000000000000000000, -1.000000000000000000, 0.000000000000000000 ) ) ;
#46378=AXIS2_PLACEMENT_3D ( 'NONE', #73011, #88232, #18696 ) ;
#46390=CIRCLE ( 'NONE', #73929, 129.7684398600581517 ) ;
#46403=ORIENTED_EDGE ( 'NONE', *, *, #43736, .T. ) ;
#46420=ORIENTED_EDGE ( 'NONE', *, *, #85156, .F. ) ;
#46423=EDGE_CURVE ( 'NONE', #97857, #47577, #53559, .T. ) ;
#46441=CARTESIAN_POINT ( 'NONE',  ( -10.35374248095108030, 5.304213687372781649, 27.98611676734227771 ) ) ;
#46484=EDGE_CURVE ( 'NONE', #20042, #9985, #33198, .T. ) ;
#46485=VERTEX_POINT ( 'NONE', #56054 ) ;
#46491=FACE_OUTER_BOUND ( 'NONE', #93206, .T. ) ;
#46499=CARTESIAN_POINT ( 'NONE',  ( 29.73860345376319358, 4.772803916115708311, -4.021109907510727943 ) ) ;
#46508=DIRECTION ( 'NONE',  ( 0.000000000000000000, 1.000000000000000000, 0.000000000000000000 ) ) ;
#46509=CARTESIAN_POINT ( 'NONE',  ( -15.54901181048698255, 6.376774720514426953, -55.62515100798455592 ) ) ;
#46512=CYLINDRICAL_SURFACE ( 'NONE', #29976, 1.699999999999996625 ) ;
#46526=CIRCLE ( 'NONE', #12479, 2.500000000000000444 ) ;
#46532=CIRCLE ( 'NONE', #2799, 1.149999999999998135 ) ;
#46534=FACE_BOUND ( 'NONE', #27339, .T. ) ;
#46537=LINE ( 'NONE', #56162, #62993 ) ;
#46555=DIRECTION ( 'NONE',  ( 0.000000000000000000, 1.000000000000000000, 0.000000000000000000 ) ) ;
#46569=ADVANCED_FACE ( 'NONE', ( #59045 ), #26087, .T. ) ;
#46577=CARTESIAN_POINT ( 'NONE',  ( 14.97946386127326157, 3.496757005395687123, -28.37921330198105352 ) ) ;
#46578=ADVANCED_FACE ( 'NONE', ( #73272 ), #16842, .F. ) ;
#46600=B_SPLINE_CURVE_WITH_KNOTS ( 'NONE', 3,
 ( #73812, #81434, #11915, #26139, #43379, #82418, #97644, #3819, #20512, #58111 ),
 .UNSPECIFIED., .F., .F.,
 ( 4, 2, 2, 2, 4 ),
 ( 1.734723475976807094E-18, 0.001417051740733931559, 0.002125577611100896037, 0.002479840546284378926, 0.002834103481467860949 ),
 .UNSPECIFIED. ) ;
#46622=ORIENTED_EDGE ( 'NONE', *, *, #96644, .F. ) ;
#46639=CARTESIAN_POINT ( 'NONE',  ( 31.63608488009066733, 3.316774720514426456, 27.34773273846990094 ) ) ;
#46657=CARTESIAN_POINT ( 'NONE',  ( -10.79305683637731406, -5.965225279485594001, -27.49869550653260930 ) ) ;
#46666=VERTEX_POINT ( 'NONE', #57558 ) ;
#46676=AXIS2_PLACEMENT_3D ( 'NONE', #72788, #25602, #4271 ) ;
#46684=EDGE_CURVE ( 'NONE', #23928, #69379, #42827, .T. ) ;
#46701=DIRECTION ( 'NONE',  ( -1.000000000000000000, 0.000000000000000000, -7.994117400814786717E-16 ) ) ;
#46723=ORIENTED_EDGE ( 'NONE', *, *, #28011, .T. ) ;
#46736=EDGE_CURVE ( 'NONE', #91432, #95809, #14838, .T. ) ;
#46747=LINE ( 'NONE', #7168, #84699 ) ;
#46752=VECTOR ( 'NONE', #81837, 1000.000000000000000 ) ;
#46755=CARTESIAN_POINT ( 'NONE',  ( 5.184553252003285984, -6.475225279485573360, -28.06387035751381731 ) ) ;
#46758=CARTESIAN_POINT ( 'NONE',  ( 22.02124265030973760, -6.143225279485574397, 12.85402280011862430 ) ) ;
#46763=FACE_OUTER_BOUND ( 'NONE', #20682, .T. ) ;
#46768=LINE ( 'NONE', #7187, #36125 ) ;
#46775=DIRECTION ( 'NONE',  ( 6.267148949376394486E-16, 1.000000000000000000, -5.583826031377232793E-16 ) ) ;
#46789=EDGE_CURVE ( 'NONE', #48376, #71418, #30572, .T. ) ;
#46806=CARTESIAN_POINT ( 'NONE',  ( 15.94332860179727618, 4.994534053091038039, -27.96060887785597515 ) ) ;
#46834=ORIENTED_EDGE ( 'NONE', *, *, #97067, .F. ) ;
#46836=ORIENTED_EDGE ( 'NONE', *, *, #95504, .F. ) ;
#46863=ORIENTED_EDGE ( 'NONE', *, *, #61611, .T. ) ;
#46878=CARTESIAN_POINT ( 'NONE',  ( -4.686006777320704586, 0.3587747205144265483, 29.60911411231907309 ) ) ;
#46915=CARTESIAN_POINT ( 'NONE',  ( 14.52511747680497933, -5.965225279485572685, -27.86035006098926559 ) ) ;
#46933=CARTESIAN_POINT ( 'NONE',  ( -25.92875734969026524, 5.356774720514425603, -0.08597719988137648983 ) ) ;
#46940=EDGE_CURVE ( 'NONE', #80243, #43471, #23435, .T. ) ;
#46975=ORIENTED_EDGE ( 'NONE', *, *, #51743, .T. ) ;
#46980=ORIENTED_EDGE ( 'NONE', *, *, #74006, .F. ) ;
#46981=CARTESIAN_POINT ( 'NONE',  ( 31.27206728860909024, 4.132774720514318822, -3.930752063305056332 ) ) ;
#46984=CARTESIAN_POINT ( 'NONE',  ( 24.71017632900191074, 5.356774720514427379, -0.3523920347467613956 ) ) ;
#46993=FACE_BOUND ( 'NONE', #13629, .T. ) ;
#47002=CARTESIAN_POINT ( 'NONE',  ( -28.98875734969026041, -5.965225279485572685, 15.62202280011862321 ) ) ;
#47013=VECTOR ( 'NONE', #57945, 1000.000000000000000 ) ;
#47025=CIRCLE ( 'NONE', #74603, 1.149999999999998135 ) ;
#47041=DIRECTION ( 'NONE',  ( -0.5630016722799275897, 0.000000000000000000, 0.8264557562326038109 ) ) ;
#47044=CARTESIAN_POINT ( 'NONE',  ( 32.65112488154859705, 3.727967435732443047, -2.714891177973568492 ) ) ;
#47060=FACE_OUTER_BOUND ( 'NONE', #13415, .T. ) ;
#47065=VERTEX_POINT ( 'NONE', #94972 ) ;
#47076=CARTESIAN_POINT ( 'NONE',  ( 29.76209104404536987, 5.356774720514427379, 26.42884784083909366 ) ) ;
#47078=EDGE_CURVE ( 'NONE', #36444, #26340, #70638, .T. ) ;
#47084=CARTESIAN_POINT ( 'NONE',  ( 15.89146238746078765, 3.595713655330297520, -28.00617091144485826 ) ) ;
#47087=CIRCLE ( 'NONE', #97335, 1.020000000000000018 ) ;
#47088=ORIENTED_EDGE ( 'NONE', *, *, #98511, .T. ) ;
#47094=ORIENTED_EDGE ( 'NONE', *, *, #73265, .T. ) ;
#47099=DIRECTION ( 'NONE',  ( -1.000000000000000000, 0.000000000000000000, 0.000000000000000000 ) ) ;
#47107=EDGE_LOOP ( 'NONE', ( #86623, #7590, #93971, #53303 ) ) ;
#47108=AXIS2_PLACEMENT_3D ( 'NONE', #90120, #28219, #51068 ) ;
#47112=DIRECTION ( 'NONE',  ( 0.000000000000000000, 0.000000000000000000, 1.000000000000000000 ) ) ;
#47123=CARTESIAN_POINT ( 'NONE',  ( 11.54156857142115911, -5.965225279485592225, -28.05134709678029381 ) ) ;
#47135=EDGE_CURVE ( 'NONE', #5380, #80239, #84708, .T. ) ;
#47172=VERTEX_POINT ( 'NONE', #80761 ) ;
#47181=ORIENTED_EDGE ( 'NONE', *, *, #75734, .F. ) ;
#47190=EDGE_CURVE ( 'NONE', #22003, #67705, #40986, .T. ) ;
#47213=DIRECTION ( 'NONE',  ( -0.1311553622875928082, -6.454799914155188842E-16, -0.9913618264504692190 ) ) ;
#47225=CARTESIAN_POINT ( 'NONE',  ( -6.914873625533459744, 0.3587747205144265483, 29.95171384920748281 ) ) ;
#47248=EDGE_CURVE ( 'NONE', #51956, #35854, #96985, .T. ) ;
#47249=FACE_OUTER_BOUND ( 'NONE', #53249, .T. ) ;
#47254=ORIENTED_EDGE ( 'NONE', *, *, #42845, .F. ) ;
#47256=CARTESIAN_POINT ( 'NONE',  ( 29.57907552799941087, -5.965225279485572685, 29.21818156447043791 ) ) ;
#47259=EDGE_CURVE ( 'NONE', #75060, #23364, #55202, .T. ) ;
#47261=PLANE ( 'NONE',  #33474 ) ;
#47265=CARTESIAN_POINT ( 'NONE',  ( 9.777643287007670381, 6.376774720514424288, -24.98776412748719977 ) ) ;
#47271=DIRECTION ( 'NONE',  ( -0.000000000000000000, 1.000000000000000000, -0.000000000000000000 ) ) ;
#47278=EDGE_CURVE ( 'NONE', #62379, #72159, #21682, .T. ) ;
#47286=LINE ( 'NONE', #78213, #6260 ) ;
#47293=ORIENTED_EDGE ( 'NONE', *, *, #91347, .F. ) ;
#47295=PLANE ( 'NONE',  #80923 ) ;
#47323=ORIENTED_EDGE ( 'NONE', *, *, #77456, .T. ) ;
#47325=FACE_OUTER_BOUND ( 'NONE', #4910, .T. ) ;
#47329=ORIENTED_EDGE ( 'NONE', *, *, #96413, .T. ) ;
#47336=VECTOR ( 'NONE', #55232, 1000.000000000000000 ) ;
#47343=DIRECTION ( 'NONE',  ( 0.000000000000000000, 0.000000000000000000, -1.000000000000000000 ) ) ;
#47344=CARTESIAN_POINT ( 'NONE',  ( 30.32108885906865936, 4.540774720514427543, 3.274824222184972822 ) ) ;
#47401=DIRECTION ( 'NONE',  ( -0.000000000000000000, 1.000000000000000000, -0.000000000000000000 ) ) ;
#47425=ORIENTED_EDGE ( 'NONE', *, *, #46940, .F. ) ;
#47431=EDGE_LOOP ( 'NONE', ( #79113, #92635, #5130, #61040 ) ) ;
#47435=ORIENTED_EDGE ( 'NONE', *, *, #58645, .F. ) ;
#47453=DIRECTION ( 'NONE',  ( -0.1311553622875919756, -6.845827386180409975E-16, -0.9913618264504692190 ) ) ;
#47472=ORIENTED_EDGE ( 'NONE', *, *, #15243, .T. ) ;
#47474=DIRECTION ( 'NONE',  ( 7.994117400814786717E-16, 0.000000000000000000, -1.000000000000000000 ) ) ;
#47486=DIRECTION ( 'NONE',  ( 0.000000000000000000, 0.000000000000000000, -1.000000000000000000 ) ) ;
#47491=CIRCLE ( 'NONE', #83111, 11.85241003308275864 ) ;
#47495=FACE_BOUND ( 'NONE', #65442, .T. ) ;
#47502=EDGE_LOOP ( 'NONE', ( #92524, #69906, #33460, #54316, #81905 ) ) ;
#47517=DIRECTION ( 'NONE',  ( 0.000000000000000000, 0.000000000000000000, -1.000000000000000000 ) ) ;
#47566=CARTESIAN_POINT ( 'NONE',  ( 282.9764569301858046, 3.316774720514426900, 20.79159422840526616 ) ) ;
#47577=VERTEX_POINT ( 'NONE', #30215 ) ;
#47604=CARTESIAN_POINT ( 'NONE',  ( 25.05730599792489599, 2.682774720514426559, -18.59674224247002172 ) ) ;
#47619=AXIS2_PLACEMENT_3D ( 'NONE', #29651, #73835, #90553 ) ;
#47638=CARTESIAN_POINT ( 'NONE',  ( -28.98875734969026396, -5.965225279485572685, -0.08597719988137648983 ) ) ;
#47644=VERTEX_POINT ( 'NONE', #95624 ) ;
#47661=CARTESIAN_POINT ( 'NONE',  ( 33.50941771711500650, 4.400593307868417625, -12.46354170163595221 ) ) ;
#47675=CARTESIAN_POINT ( 'NONE',  ( 33.65278273286722310, 3.366611878523314783, -11.65467467704458393 ) ) ;
#47680=EDGE_CURVE ( 'NONE', #19685, #43485, #47491, .T. ) ;
#47683=EDGE_LOOP ( 'NONE', ( #40533, #95775, #13822, #1677 ) ) ;
#47689=DIRECTION ( 'NONE',  ( 0.000000000000000000, 0.000000000000000000, 1.000000000000000000 ) ) ;
#47691=CARTESIAN_POINT ( 'NONE',  ( -24.90875734969025501, 3.316774720514426456, 26.43402280011862615 ) ) ;
#47698=ADVANCED_FACE ( 'NONE', ( #64199 ), #56073, .F. ) ;
#47726=ORIENTED_EDGE ( 'NONE', *, *, #52594, .F. ) ;
#47736=EDGE_CURVE ( 'NONE', #69136, #50260, #33726, .T. ) ;
#47760=EDGE_CURVE ( 'NONE', #11284, #37448, #87005, .T. ) ;
#47765=CARTESIAN_POINT ( 'NONE',  ( 14.76093561896379214, 3.316774720514426456, -26.55548769130089681 ) ) ;
#47768=VERTEX_POINT ( 'NONE', #36223 ) ;
#47770=CARTESIAN_POINT ( 'NONE',  ( 7.844850387708879325, 6.376774720514429617, -25.09814097568368751 ) ) ;
#47773=EDGE_LOOP ( 'NONE', ( #90307, #45365, #69303, #169 ) ) ;
#47781=VECTOR ( 'NONE', #41477, 1000.000000000000000 ) ;
#47790=DIRECTION ( 'NONE',  ( 0.000000000000000000, 0.000000000000000000, -1.000000000000000000 ) ) ;
#47812=ORIENTED_EDGE ( 'NONE', *, *, #19177, .T. ) ;
#47814=ORIENTED_EDGE ( 'NONE', *, *, #56085, .F. ) ;
#47832=EDGE_CURVE ( 'NONE', #65938, #83405, #37496, .T. ) ;
#47844=CARTESIAN_POINT ( 'NONE',  ( 32.88562546571903056, -5.965225279485572685, -5.083907541707159972 ) ) ;
#47845=DIRECTION ( 'NONE',  ( 0.9976052577199501226, -2.125886612716675376E-15, 0.06916465693916179491 ) ) ;
#47851=EDGE_CURVE ( 'NONE', #18484, #871, #87980, .T. ) ;
#47854=AXIS2_PLACEMENT_3D ( 'NONE', #27124, #50460, #81411 ) ;
#47873=DIRECTION ( 'NONE',  ( 0.000000000000000000, 0.000000000000000000, -1.000000000000000000 ) ) ;
#47892=FACE_OUTER_BOUND ( 'NONE', #25103, .T. ) ;
#47894=( BOUNDED_SURFACE ( )  B_SPLINE_SURFACE ( 3, 2, ( 
 ( #1823, #73335, #97165 ),
 ( #65739, #89057, #28155 ),
 ( #81934, #82427, #50492 ),
 ( #27658, #57618, #98141 ),
 ( #59608, #42888, #81444 ),
 ( #73821, #20521, #59112 ),
 ( #3828, #34765, #43877 ),
 ( #27155, #58120, #35770 ),
 ( #4324, #82919, #3338 ),
 ( #90539, #26657, #96168 ),
 ( #28649, #74810, #11924 ),
 ( #88557, #21022, #35274 ) ),
 .UNSPECIFIED., .F., .F., .T. ) 
 B_SPLINE_SURFACE_WITH_KNOTS ( ( 4, 2, 2, 2, 2, 4 ),
 ( 3, 3 ),
 ( -3.428680950268159222E-15, 0.001642567453077259246, 0.003285134906157947173, 0.004106418632698291028, 0.004927702359238635317, 0.006570269812319323027 ),
 ( 0.000000000000000000, 1.000000000000000000 ),
 .UNSPECIFIED. ) 
 GEOMETRIC_REPRESENTATION_ITEM ( )  RATIONAL_B_SPLINE_SURFACE ( (
 ( 1.000000000000000000, 0.7071067811865476838, 1.000000000000000000),
 ( 1.000000000000000000, 0.7071067811865476838, 1.000000000000000000),
 ( 1.000000000000000000, 0.7071067811865476838, 1.000000000000000000),
 ( 1.000000000000000000, 0.7071067811865476838, 1.000000000000000000),
 ( 1.000000000000000000, 0.7071067811865476838, 1.000000000000000000),
 ( 1.000000000000000000, 0.7071067811865476838, 1.000000000000000000),
 ( 1.000000000000000000, 0.7071067811865476838, 1.000000000000000000),
 ( 1.000000000000000000, 0.7071067811865476838, 1.000000000000000000),
 ( 1.000000000000000000, 0.7071067811865476838, 1.000000000000000000),
 ( 1.000000000000000000, 0.7071067811865476838, 1.000000000000000000),
 ( 1.000000000000000000, 0.7071067811865476838, 1.000000000000000000),
 ( 1.000000000000000000, 0.7071067811865476838, 1.000000000000000000) ) ) 
 REPRESENTATION_ITEM ( '' )  SURFACE ( )  );
#47914=AXIS2_PLACEMENT_3D ( 'NONE', #80810, #29004, #89419 ) ;
#47925=CARTESIAN_POINT ( 'NONE',  ( 31.88667425545054002, 2.682774720514426559, -9.651215965565025812 ) ) ;
#47932=CARTESIAN_POINT ( 'NONE',  ( -20.77875734969026311, -6.143225279485574397, 27.31649921512899937 ) ) ;
#47942=CARTESIAN_POINT ( 'NONE',  ( 31.60706529141452137, 4.540774720514427543, 26.12024523944105070 ) ) ;
#47949=DIRECTION ( 'NONE',  ( 0.000000000000000000, 0.000000000000000000, -1.000000000000000000 ) ) ;
#47968=CARTESIAN_POINT ( 'NONE',  ( -19.80875734969026425, -5.965225279485572685, 31.02402280011862246 ) ) ;
#47984=LINE ( 'NONE', #17525, #31944 ) ;
#47985=AXIS2_PLACEMENT_3D ( 'NONE', #11474, #50053, #3386 ) ;
#47996=CARTESIAN_POINT ( 'NONE',  ( 26.73860345374794178, 5.356774720496559894, 19.84760796525321780 ) ) ;
#47999=CARTESIAN_POINT ( 'NONE',  ( 30.54636625424942764, 6.376774720514426065, 1.976438700016742045 ) ) ;
#48011=DIRECTION ( 'NONE',  ( -0.000000000000000000, -1.000000000000000000, -0.000000000000000000 ) ) ;
#48018=CARTESIAN_POINT ( 'NONE',  ( 30.53060340732036693, 4.132774720514426292, -5.153186819891554471 ) ) ;
#48026=CIRCLE ( 'NONE', #33449, 11.85241003308275864 ) ;
#48040=CARTESIAN_POINT ( 'NONE',  ( -0.02075734969026423599, 3.316774720514426456, -0.08597719988137648983 ) ) ;
#48069=VERTEX_POINT ( 'NONE', #94995 ) ;
#48077=CIRCLE ( 'NONE', #86951, 22.69500000000000384 ) ;
#48106=DIRECTION ( 'NONE',  ( -0.6451914333552788428, 0.000000000000000000, -0.7640209514960702997 ) ) ;
#48109=CIRCLE ( 'NONE', #39982, 252.4458649670781085 ) ;
#48110=LINE ( 'NONE', #2430, #14235 ) ;
#48112=ORIENTED_EDGE ( 'NONE', *, *, #63457, .T. ) ;
#48132=LINE ( 'NONE', #35888, #9087 ) ;
#48136=VECTOR ( 'NONE', #67788, 999.9999999999998863 ) ;
#48157=CARTESIAN_POINT ( 'NONE',  ( -28.98875734969026041, -5.965225279485572685, 15.62202280011862321 ) ) ;
#48161=CARTESIAN_POINT ( 'NONE',  ( 33.41145047975789595, 4.538943570064395416, -12.61568413423384172 ) ) ;
#48169=AXIS2_PLACEMENT_3D ( 'NONE', #67065, #29971, #98977 ) ;
#48177=VECTOR ( 'NONE', #11427, 1000.000000000000000 ) ;
#48180=DIRECTION ( 'NONE',  ( -0.7071067811865476838, 0.000000000000000000, 0.7071067811865474617 ) ) ;
#48216=CARTESIAN_POINT ( 'NONE',  ( 15.32643653063177958, 3.577630190450218350, -27.14485409495429380 ) ) ;
#48219=CARTESIAN_POINT ( 'NONE',  ( -29.49875734969026198, 0.3587747205144262708, 7.870022800118625206 ) ) ;
#48225=ORIENTED_EDGE ( 'NONE', *, *, #68929, .F. ) ;
#48228=ORIENTED_EDGE ( 'NONE', *, *, #12820, .T. ) ;
#48229=CARTESIAN_POINT ( 'NONE',  ( 0.000000000000000000, 2.682774720514426559, 0.000000000000000000 ) ) ;
#48238=DIRECTION ( 'NONE',  ( 0.000000000000000000, 0.000000000000000000, 1.000000000000000000 ) ) ;
#48244=VECTOR ( 'NONE', #3592, 1000.000000000000000 ) ;
#48266=LINE ( 'NONE', #79197, #33353 ) ;
#48273=VECTOR ( 'NONE', #17366, 1000.000000000000000 ) ;
#48279=CIRCLE ( 'NONE', #38557, 2.249999999999998668 ) ;
#48287=EDGE_CURVE ( 'NONE', #6012, #11676, #87091, .T. ) ;
#48304=DIRECTION ( 'NONE',  ( 0.000000000000000000, -1.000000000000000000, 0.000000000000000000 ) ) ;
#48320=ORIENTED_EDGE ( 'NONE', *, *, #99578, .F. ) ;
#48325=ADVANCED_FACE ( 'NONE', ( #37596 ), #68546, .T. ) ;
#48327=ORIENTED_EDGE ( 'NONE', *, *, #44459, .F. ) ;
#48334=CARTESIAN_POINT ( 'NONE',  ( 29.73860345376319358, 5.356774720514427379, 1.647607965253217399 ) ) ;
#48341=VECTOR ( 'NONE', #1537, 1000.000000000000000 ) ;
#48376=VERTEX_POINT ( 'NONE', #40099 ) ;
#48378=CARTESIAN_POINT ( 'NONE',  ( -27.25988310792305214, -5.965225279485572685, 30.32664379231667695 ) ) ;
#48402=EDGE_CURVE ( 'NONE', #79911, #35733, #77641, .T. ) ;
#48425=CARTESIAN_POINT ( 'NONE',  ( -10.11875734969026297, 3.316774720514426456, 30.51402280011862089 ) ) ;
#48433=CARTESIAN_POINT ( 'NONE',  ( 6.184520403203631389, 5.356774720514425603, -25.32021290018218451 ) ) ;
#48435=VERTEX_POINT ( 'NONE', #16256 ) ;
#48440=ORIENTED_EDGE ( 'NONE', *, *, #33554, .T. ) ;
#48443=ORIENTED_EDGE ( 'NONE', *, *, #16020, .T. ) ;
#48461=CARTESIAN_POINT ( 'NONE',  ( 5.265981236333619456E-16, -1.473225279485573802, -4.300000000000000711 ) ) ;
#48465=ORIENTED_EDGE ( 'NONE', *, *, #21599, .F. ) ;
#48468=EDGE_CURVE ( 'NONE', #19353, #71104, #56845, .T. ) ;
#48494=DIRECTION ( 'NONE',  ( 0.000000000000000000, 0.000000000000000000, -1.000000000000000000 ) ) ;
#48496=VECTOR ( 'NONE', #88240, 1000.000000000000000 ) ;
#48512=CARTESIAN_POINT ( 'NONE',  ( 30.09341516180546350, 1.682774720514426114, -11.39311774897855756 ) ) ;
#48513=CARTESIAN_POINT ( 'NONE',  ( 27.53860345374808105, 5.356774720496559894, 19.84760796525321780 ) ) ;
#48519=LINE ( 'NONE', #29157, #54785 ) ;
#48530=ADVANCED_FACE ( 'NONE', ( #27376 ), #58826, .F. ) ;
#48537=CARTESIAN_POINT ( 'NONE',  ( 29.73860345376319358, 5.356774720496559894, -0.3523920347467610070 ) ) ;
#48552=EDGE_CURVE ( 'NONE', #54184, #32574, #35492, .T. ) ;
#48554=DIRECTION ( 'NONE',  ( -1.000000000000000000, 0.000000000000000000, -0.000000000000000000 ) ) ;
#48579=EDGE_LOOP ( 'NONE', ( #7659, #18767, #54598, #80505 ) ) ;
#48584=FACE_OUTER_BOUND ( 'NONE', #11890, .T. ) ;
#48601=ORIENTED_EDGE ( 'NONE', *, *, #73938, .F. ) ;
#48606=CARTESIAN_POINT ( 'NONE',  ( 14.61581670307174008, 2.682774720514426559, -27.35847990810646024 ) ) ;
#48638=VECTOR ( 'NONE', #23816, 1000.000000000000000 ) ;
#48640=CARTESIAN_POINT ( 'NONE',  ( -10.58858228176428540, 0.3587747205144061202, -27.03148018517017803 ) ) ;
#48664=CARTESIAN_POINT ( 'NONE',  ( 28.20688450243577705, 4.772774720514425972, -7.073367244511738150 ) ) ;
#48668=CARTESIAN_POINT ( 'NONE',  ( -16.22218391600152643, 6.376774720514426953, -54.85883559227303863 ) ) ;
#48687=VECTOR ( 'NONE', #89871, 1000.000000000000000 ) ;
#48690=CARTESIAN_POINT ( 'NONE',  ( -28.84663072490566194, -5.965225279485572685, 28.73989617533406715 ) ) ;
#48700=FACE_OUTER_BOUND ( 'NONE', #66432, .T. ) ;
#48704=FACE_OUTER_BOUND ( 'NONE', #8041, .T. ) ;
#48721=DIRECTION ( 'NONE',  ( 0.000000000000000000, -1.000000000000000000, 0.000000000000000000 ) ) ;
#48755=CARTESIAN_POINT ( 'NONE',  ( 27.53860345374808105, 5.356774720514425603, -6.982392034746242260 ) ) ;
#48758=PLANE ( 'NONE',  #29711 ) ;
#48762=CARTESIAN_POINT ( 'NONE',  ( 12.90232279286373185, 3.316774720514426456, -28.14923833570356493 ) ) ;
#48784=B_SPLINE_CURVE_WITH_KNOTS ( 'NONE', 3,
 ( #11026, #73431, #41995, #88656, #34864, #58209, #19625, #50587 ),
 .UNSPECIFIED., .F., .F.,
 ( 4, 2, 2, 4 ),
 ( 0.06220205793350375156, 0.06492579111525004221, 0.06628765770612317365, 0.06764952429699631897 ),
 .UNSPECIFIED. ) ;
#48786=CARTESIAN_POINT ( 'NONE',  ( -10.40290173325841216, 6.376774720514426953, 27.45402280011861862 ) ) ;
#48796=VERTEX_POINT ( 'NONE', #47604 ) ;
#48803=CARTESIAN_POINT ( 'NONE',  ( 14.47435193431689449, 3.621805754985667036, -28.36943713370744646 ) ) ;
#48812=EDGE_CURVE ( 'NONE', #57023, #76713, #39453, .T. ) ;
#48845=ORIENTED_EDGE ( 'NONE', *, *, #42463, .F. ) ;
#48848=ORIENTED_EDGE ( 'NONE', *, *, #60145, .T. ) ;
#48855=PLANE ( 'NONE',  #32321 ) ;
#48860=DIRECTION ( 'NONE',  ( 0.000000000000000000, -1.000000000000000000, 0.000000000000000000 ) ) ;
#48861=DIRECTION ( 'NONE',  ( 0.000000000000000000, 1.000000000000000000, 0.000000000000000000 ) ) ;
#48864=ORIENTED_EDGE ( 'NONE', *, *, #40405, .T. ) ;
#48866=PLANE ( 'NONE',  #23819 ) ;
#48871=DIRECTION ( 'NONE',  ( 0.06916465693916194757, 0.000000000000000000, -0.9976052577199501226 ) ) ;
#48879=FACE_OUTER_BOUND ( 'NONE', #12727, .T. ) ;
#48906=ORIENTED_EDGE ( 'NONE', *, *, #88785, .T. ) ;
#48908=AXIS2_PLACEMENT_3D ( 'NONE', #54003, #77310, #38755 ) ;
#48914=CARTESIAN_POINT ( 'NONE',  ( -29.49875734969026198, 0.3587747205144265483, 10.11402280011862587 ) ) ;
#48919=VERTEX_POINT ( 'NONE', #57102 ) ;
#48921=EDGE_CURVE ( 'NONE', #14248, #37175, #54221, .T. ) ;
#48924=DIRECTION ( 'NONE',  ( 0.000000000000000000, 0.000000000000000000, -1.000000000000000000 ) ) ;
#48934=LINE ( 'NONE', #4255, #59277 ) ;
#48937=VECTOR ( 'NONE', #19013, 1000.000000000000000 ) ;
#48955=CARTESIAN_POINT ( 'NONE',  ( -41.32836283488544638, -2.803225279485573207, 39.26872235229541985 ) ) ;
#48956=VERTEX_POINT ( 'NONE', #85653 ) ;
#48958=DIRECTION ( 'NONE',  ( 0.000000000000000000, 0.000000000000000000, -1.000000000000000000 ) ) ;
#48968=ORIENTED_EDGE ( 'NONE', *, *, #94579, .T. ) ;
#48990=ADVANCED_FACE ( 'NONE', ( #20999 ), #20621, .F. ) ;
#49035=DIRECTION ( 'NONE',  ( -0.000000000000000000, -1.000000000000000000, -0.000000000000000000 ) ) ;
#49039=CARTESIAN_POINT ( 'NONE',  ( -2.704906987277324593, -5.965225279485572685, -28.92935364444904067 ) ) ;
#49046=LINE ( 'NONE', #78463, #7252 ) ;
#49055=CARTESIAN_POINT ( 'NONE',  ( -65.05438548721848235, -6.143225279485573509, 29.49402280011861777 ) ) ;
#49074=CIRCLE ( 'NONE', #37670, 28.45799999999999486 ) ;
#49077=ORIENTED_EDGE ( 'NONE', *, *, #20160, .F. ) ;
#49084=DIRECTION ( 'NONE',  ( 0.000000000000000000, -1.000000000000000000, 0.000000000000000000 ) ) ;
#49092=ORIENTED_EDGE ( 'NONE', *, *, #71219, .T. ) ;
#49093=DIRECTION ( 'NONE',  ( 0.000000000000000000, 1.000000000000000000, -0.000000000000000000 ) ) ;
#49094=ORIENTED_EDGE ( 'NONE', *, *, #20786, .T. ) ;
#49103=CARTESIAN_POINT ( 'NONE',  ( 31.93426202889373400, 6.376774720514426953, 6.907000118922836940 ) ) ;
#49121=ORIENTED_EDGE ( 'NONE', *, *, #41109, .T. ) ;
#49129=ADVANCED_FACE ( 'NONE', ( #31611 ), #69179, .T. ) ;
#49143=CYLINDRICAL_SURFACE ( 'NONE', #63270, 91.74549126261078413 ) ;
#49158=DIRECTION ( 'NONE',  ( -0.000000000000000000, 1.000000000000000000, -1.155373159085149695E-17 ) ) ;
#49169=CARTESIAN_POINT ( 'NONE',  ( -0.02075734969026423599, 0.3587747205144213303, -0.08597719988137648983 ) ) ;
#49172=CARTESIAN_POINT ( 'NONE',  ( 33.00535138976576377, 3.570691370340801640, -12.97242311383999791 ) ) ;
#49185=CARTESIAN_POINT ( 'NONE',  ( 33.00535138976592719, 3.570691370340881576, -12.97242311383975988 ) ) ;
#49197=EDGE_LOOP ( 'NONE', ( #14460, #84384 ) ) ;
#49207=ORIENTED_EDGE ( 'NONE', *, *, #93416, .F. ) ;
#49212=ORIENTED_EDGE ( 'NONE', *, *, #12403, .F. ) ;
#49219=AXIS2_PLACEMENT_3D ( 'NONE', #85803, #63490, #1069 ) ;
#49235=VERTEX_POINT ( 'NONE', #60595 ) ;
#49239=ADVANCED_FACE ( 'NONE', ( #70179 ), #664, .F. ) ;
#49242=DIRECTION ( 'NONE',  ( 0.000000000000000000, 0.000000000000000000, 1.000000000000000000 ) ) ;
#49264=CARTESIAN_POINT ( 'NONE',  ( 24.71017632900191074, 3.356774720514427379, 1.647607965253217621 ) ) ;
#49274=ORIENTED_EDGE ( 'NONE', *, *, #62145, .T. ) ;
#49275=CARTESIAN_POINT ( 'NONE',  ( 30.09341516180546350, 1.682774720514426114, -11.39311774897855756 ) ) ;
#49276=DIRECTION ( 'NONE',  ( -6.924038193813838377E-14, 0.000000000000000000, -1.000000000000000000 ) ) ;
#49300=LINE ( 'NONE', #17835, #58146 ) ;
#49303=VECTOR ( 'NONE', #11208, 1000.000000000000000 ) ;
#49316=VECTOR ( 'NONE', #17857, 1000.000000000000000 ) ;
#49323=ORIENTED_EDGE ( 'NONE', *, *, #84767, .F. ) ;
#49327=EDGE_CURVE ( 'NONE', #42928, #5789, #72195, .T. ) ;
#49344=CARTESIAN_POINT ( 'NONE',  ( -29.49875734969026198, -5.965225279485572685, 10.11402280011862587 ) ) ;
#49349=ORIENTED_EDGE ( 'NONE', *, *, #84088, .T. ) ;
#49367=ORIENTED_EDGE ( 'NONE', *, *, #69313, .T. ) ;
#49375=CIRCLE ( 'NONE', #2360, 1.835999999999931465 ) ;
#49385=EDGE_CURVE ( 'NONE', #62379, #50557, #19388, .T. ) ;
#49386=ORIENTED_EDGE ( 'NONE', *, *, #39279, .F. ) ;
#49413=ORIENTED_EDGE ( 'NONE', *, *, #14856, .F. ) ;
#49414=DIRECTION ( 'NONE',  ( 0.000000000000000000, -0.000000000000000000, -1.000000000000000000 ) ) ;
#49424=VERTEX_POINT ( 'NONE', #96516 ) ;
#49429=LINE ( 'NONE', #80863, #69563 ) ;
#49430=CARTESIAN_POINT ( 'NONE',  ( 33.13288845015618023, -5.965225279485572685, -0.1650522222209214185 ) ) ;
#49440=AXIS2_PLACEMENT_3D ( 'NONE', #58408, #66538, #82221 ) ;
#49458=CARTESIAN_POINT ( 'NONE',  ( -10.22357262723052784, 3.975302591317960044, 29.38944064375215248 ) ) ;
#49478=DIRECTION ( 'NONE',  ( 0.000000000000000000, 0.000000000000000000, -1.000000000000000000 ) ) ;
#49494=VECTOR ( 'NONE', #2228, 1000.000000000000000 ) ;
#49496=DIRECTION ( 'NONE',  ( -0.000000000000000000, -1.000000000000000000, -0.000000000000000000 ) ) ;
#49497=DIRECTION ( 'NONE',  ( 0.000000000000000000, -1.478457507934778393E-16, -1.000000000000000000 ) ) ;
#49511=ORIENTED_EDGE ( 'NONE', *, *, #57305, .T. ) ;
#49516=LINE ( 'NONE', #80450, #86049 ) ;
#49525=CARTESIAN_POINT ( 'NONE',  ( 5.092794675178905273, 3.306008726340172288, -27.56219045528442280 ) ) ;
#49533=CARTESIAN_POINT ( 'NONE',  ( 20.57455539870835182, 3.407774720514426647, -18.22080502500614330 ) ) ;
#49536=DIRECTION ( 'NONE',  ( 0.000000000000000000, -1.000000000000000000, 0.000000000000000000 ) ) ;
#49542=PLANE ( 'NONE',  #31846 ) ;
#49550=EDGE_CURVE ( 'NONE', #81022, #24863, #72518, .T. ) ;
#49555=FACE_OUTER_BOUND ( 'NONE', #69021, .T. ) ;
#49559=ORIENTED_EDGE ( 'NONE', *, *, #83909, .T. ) ;
#49568=ORIENTED_EDGE ( 'NONE', *, *, #8636, .T. ) ;
#49572=ORIENTED_EDGE ( 'NONE', *, *, #27171, .T. ) ;
#49590=ADVANCED_FACE ( 'NONE', ( #32443 ), #94336, .T. ) ;
#49593=ORIENTED_EDGE ( 'NONE', *, *, #2599, .F. ) ;
#49599=ORIENTED_EDGE ( 'NONE', *, *, #4337, .T. ) ;
#49603=VECTOR ( 'NONE', #38253, 1000.000000000000114 ) ;
#49612=EDGE_CURVE ( 'NONE', #20569, #68532, #3905, .T. ) ;
#49616=DIRECTION ( 'NONE',  ( 0.000000000000000000, 0.000000000000000000, -1.000000000000000000 ) ) ;
#49626=EDGE_LOOP ( 'NONE', ( #28954, #6628, #29487, #93980 ) ) ;
#49630=FACE_OUTER_BOUND ( 'NONE', #77103, .T. ) ;
#49652=VECTOR ( 'NONE', #22773, 1000.000000000000000 ) ;
#49661=ADVANCED_FACE ( 'NONE', ( #28324 ), #35449, .T. ) ;
#49662=ORIENTED_EDGE ( 'NONE', *, *, #4601, .F. ) ;
#49664=CARTESIAN_POINT ( 'NONE',  ( 30.93860345374796239, -5.965225279485572685, 28.07639619989137003 ) ) ;
#49666=DIRECTION ( 'NONE',  ( -0.1254312216594016538, -0.000000000000000000, -0.9921023176230513441 ) ) ;
#49669=ORIENTED_EDGE ( 'NONE', *, *, #49, .T. ) ;
#49686=DIRECTION ( 'NONE',  ( 0.000000000000000000, 0.000000000000000000, 1.000000000000000000 ) ) ;
#49688=EDGE_LOOP ( 'NONE', ( #59602, #17236, #17996, #10790 ) ) ;
#49707=EDGE_LOOP ( 'NONE', ( #81641, #64689, #9276, #97170 ) ) ;
#49756=LINE ( 'NONE', #50245, #49852 ) ;
#49761=CARTESIAN_POINT ( 'NONE',  ( 32.16024265030974050, -5.965225279485572685, 16.27760796525321751 ) ) ;
#49765=DIRECTION ( 'NONE',  ( -0.000000000000000000, 1.000000000000000000, -0.000000000000000000 ) ) ;
#49770=ORIENTED_EDGE ( 'NONE', *, *, #49550, .F. ) ;
#49775=CIRCLE ( 'NONE', #41658, 3.570000000000003837 ) ;
#49785=CARTESIAN_POINT ( 'NONE',  ( 11.22265027773143231, 6.376774720513926908, -28.06709888789093554 ) ) ;
#49793=EDGE_CURVE ( 'NONE', #36340, #97022, #3259, .T. ) ;
#49794=DIRECTION ( 'NONE',  ( 4.089440751051245812E-15, -1.000000000000000000, -1.042451643221144600E-15 ) ) ;
#49797=DIRECTION ( 'NONE',  ( -0.000000000000000000, -1.000000000000000000, -0.000000000000000000 ) ) ;
#49803=FACE_OUTER_BOUND ( 'NONE', #15610, .T. ) ;
#49805=DIRECTION ( 'NONE',  ( 0.000000000000000000, 0.000000000000000000, 1.000000000000000000 ) ) ;
#49807=CARTESIAN_POINT ( 'NONE',  ( 14.78821595474961192, 4.792189181182580526, -27.68628040864189899 ) ) ;
#49809=ORIENTED_EDGE ( 'NONE', *, *, #14470, .T. ) ;
#49816=CARTESIAN_POINT ( 'NONE',  ( 31.62831224182126988, 4.127879075750807480, 27.04291028225966542 ) ) ;
#49834=VERTEX_POINT ( 'NONE', #69881 ) ;
#49848=CARTESIAN_POINT ( 'NONE',  ( 29.58031977903354459, 3.717801497966991775, 29.19834312781581076 ) ) ;
#49852=VECTOR ( 'NONE', #26897, 1000.000000000000000 ) ;
#49872=CARTESIAN_POINT ( 'NONE',  ( 30.53060340732035982, -1.477225279485574028, 19.84760796525321780 ) ) ;
#49878=DIRECTION ( 'NONE',  ( 0.000000000000000000, 0.000000000000000000, -1.000000000000000000 ) ) ;
#49880=VECTOR ( 'NONE', #12613, 1000.000000000000000 ) ;
#49945=VECTOR ( 'NONE', #11871, 1000.000000000000000 ) ;
#49955=DIRECTION ( 'NONE',  ( 0.000000000000000000, 0.000000000000000000, -1.000000000000000000 ) ) ;
#49956=DIRECTION ( 'NONE',  ( -0.9913618264504693300, 5.365801633547209345E-16, 0.1311553622875920033 ) ) ;
#49964=DIRECTION ( 'NONE',  ( 0.6599726524652365089, 0.000000000000000000, -0.7512896232465879898 ) ) ;
#49968=CARTESIAN_POINT ( 'NONE',  ( 31.13513474936814163, 4.540774720514427543, 3.331262582247520143 ) ) ;
#49969=VECTOR ( 'NONE', #6586, 1000.000000000000000 ) ;
#49971=VERTEX_POINT ( 'NONE', #77968 ) ;
#49979=ORIENTED_EDGE ( 'NONE', *, *, #89971, .F. ) ;
#49990=CARTESIAN_POINT ( 'NONE',  ( 15.01415361830771467, 3.567044333682583890, -27.41917996821035430 ) ) ;
#49991=LINE ( 'NONE', #26639, #10034 ) ;
#49992=ORIENTED_EDGE ( 'NONE', *, *, #44919, .F. ) ;
#49995=ORIENTED_EDGE ( 'NONE', *, *, #49793, .F. ) ;
#49996=CARTESIAN_POINT ( 'NONE',  ( -53.01255352321339842, 2.682774720514426559, 35.59556822165056644 ) ) ;
#50018=DIRECTION ( 'NONE',  ( 0.000000000000000000, 0.000000000000000000, -1.000000000000000000 ) ) ;
#50028=CARTESIAN_POINT ( 'NONE',  ( 31.41423154468143153, 4.132774720514426292, -0.3119954678742140053 ) ) ;
#50053=DIRECTION ( 'NONE',  ( 0.000000000000000000, 0.000000000000000000, -1.000000000000000000 ) ) ;
#50057=DIRECTION ( 'NONE',  ( -1.000000000000000000, 0.000000000000000000, 0.000000000000000000 ) ) ;
#50082=DIRECTION ( 'NONE',  ( 1.000000000000000000, -0.000000000000000000, -0.000000000000000000 ) ) ;
#50093=LINE ( 'NONE', #1916, #84350 ) ;
#50096=ORIENTED_EDGE ( 'NONE', *, *, #15189, .F. ) ;
#50097=DIRECTION ( 'NONE',  ( 1.000000000000000000, -0.000000000000000000, -0.000000000000000000 ) ) ;
#50117=CARTESIAN_POINT ( 'NONE',  ( 3.252401863874215593, 0.3587747205143964613, -29.35688408629929214 ) ) ;
#50118=VERTEX_POINT ( 'NONE', #28079 ) ;
#50122=CARTESIAN_POINT ( 'NONE',  ( 15.63605935613269438, -5.965225279485572685, -27.55169773172585934 ) ) ;
#50128=DIRECTION ( 'NONE',  ( 0.000000000000000000, 0.000000000000000000, -1.000000000000000000 ) ) ;
#50136=AXIS2_PLACEMENT_3D ( 'NONE', #84668, #15156, #46122 ) ;
#50149=AXIS2_PLACEMENT_3D ( 'NONE', #43191, #58909, #25953 ) ;
#50154=CARTESIAN_POINT ( 'NONE',  ( 5.097264368846952998, -6.475225279485573360, -27.56135813788808164 ) ) ;
#50189=CARTESIAN_POINT ( 'NONE',  ( 32.45853543194704116, -5.965225279485572685, 9.169203677920338080 ) ) ;
#50206=ORIENTED_EDGE ( 'NONE', *, *, #96456, .F. ) ;
#50212=AXIS2_PLACEMENT_3D ( 'NONE', #18747, #44596, #36978 ) ;
#50218=ORIENTED_EDGE ( 'NONE', *, *, #87945, .T. ) ;
#50223=ORIENTED_EDGE ( 'NONE', *, *, #50357, .F. ) ;
#50245=CARTESIAN_POINT ( 'NONE',  ( -4.993225604111835914, -5.965225279485592225, -29.11654937215278593 ) ) ;
#50260=VERTEX_POINT ( 'NONE', #53912 ) ;
#50265=CARTESIAN_POINT ( 'NONE',  ( -6.741682653110981249, -5.965225279485572685, 30.62569541381301619 ) ) ;
#50276=VERTEX_POINT ( 'NONE', #75721 ) ;
#50279=CARTESIAN_POINT ( 'NONE',  ( 29.80070917940689412, -6.475225279485573360, 27.39560796525321607 ) ) ;
#50282=DIRECTION ( 'NONE',  ( 1.000000000000000000, 0.000000000000000000, -0.000000000000000000 ) ) ;
#50291=DIRECTION ( 'NONE',  ( -1.000000000000000000, 0.000000000000000000, -0.000000000000000000 ) ) ;
#50293=VECTOR ( 'NONE', #65434, 1000.000000000000000 ) ;
#50297=CARTESIAN_POINT ( 'NONE',  ( 15.35137209921619572, 4.335618847589792324, -28.31916638425222033 ) ) ;
#50304=CARTESIAN_POINT ( 'NONE',  ( 31.61913385939691423, 4.417689821282788643, 26.66246549260776177 ) ) ;
#50307=CARTESIAN_POINT ( 'NONE',  ( 14.99280666621547731, 3.498378956622122615, -27.33228583850618065 ) ) ;
#50314=EDGE_LOOP ( 'NONE', ( #57682, #66472, #84615, #27496 ) ) ;
#50332=CARTESIAN_POINT ( 'NONE',  ( -4.926336369345164279, -5.965225279485592225, -28.61095484066304451 ) ) ;
#50354=CARTESIAN_POINT ( 'NONE',  ( 25.97917928778648999, 4.259874112196678553, -11.44717982150283220 ) ) ;
#50357=EDGE_CURVE ( 'NONE', #80017, #9599, #8732, .T. ) ;
#50380=DIRECTION ( 'NONE',  ( 0.000000000000000000, 0.000000000000000000, -1.000000000000000000 ) ) ;
#50385=VERTEX_POINT ( 'NONE', #55414 ) ;
#50387=LINE ( 'NONE', #11809, #2587 ) ;
#50402=FACE_OUTER_BOUND ( 'NONE', #38713, .T. ) ;
#50409=EDGE_CURVE ( 'NONE', #16877, #76855, #68712, .T. ) ;
#50449=LINE ( 'NONE', #88513, #20925 ) ;
#50460=DIRECTION ( 'NONE',  ( -0.3133898629642195011, 5.365801633547207373E-16, 0.9496245541219264785 ) ) ;
#50461=CARTESIAN_POINT ( 'NONE',  ( 29.73860345376319003, 5.356774720496559894, 19.84760796525321780 ) ) ;
#50483=DIRECTION ( 'NONE',  ( -0.000000000000000000, -0.000000000000000000, -1.000000000000000000 ) ) ;
#50485=CARTESIAN_POINT ( 'NONE',  ( 31.64143112576189765, 6.376774720514426953, 14.03360796525321774 ) ) ;
#50492=CARTESIAN_POINT ( 'NONE',  ( 6.190876379677949792, 3.316774720513832708, -27.38145114071290465 ) ) ;
#50506=CARTESIAN_POINT ( 'NONE',  ( 3.176458874063926352, -5.965225279485592225, -28.85257003503889095 ) ) ;
#50509=DIRECTION ( 'NONE',  ( -0.1254312216594016538, -0.000000000000000000, -0.9921023176230513441 ) ) ;
#50510=DIRECTION ( 'NONE',  ( 0.000000000000000000, 0.000000000000000000, -1.000000000000000000 ) ) ;
#50512=CARTESIAN_POINT ( 'NONE',  ( 13.86067930709089602, 5.152774720507880879, -28.23766061414428208 ) ) ;
#50513=CARTESIAN_POINT ( 'NONE',  ( 14.73162737928355170, 2.682774720514426559, -27.37940951657878941 ) ) ;
#50535=VERTEX_POINT ( 'NONE', #43682 ) ;
#50557=VERTEX_POINT ( 'NONE', #5614 ) ;
#50567=EDGE_CURVE ( 'NONE', #70059, #61929, #67526, .T. ) ;
#50576=ORIENTED_EDGE ( 'NONE', *, *, #60941, .T. ) ;
#50585=CARTESIAN_POINT ( 'NONE',  ( -29.49875734969025842, -5.965225279485572685, 15.62202280011862321 ) ) ;
#50587=CARTESIAN_POINT ( 'NONE',  ( 10.46399479596398052, 3.316774720514422903, -27.03001098546561209 ) ) ;
#50604=VERTEX_POINT ( 'NONE', #3 ) ;
#50606=CARTESIAN_POINT ( 'NONE',  ( 32.84232313084854837, 4.840274619473185602, -11.71291885348858663 ) ) ;
#50609=CARTESIAN_POINT ( 'NONE',  ( 7.526024287269984292, 1.682774720514426114, 9.032262774691707463 ) ) ;
#50610=ADVANCED_FACE ( 'NONE', ( #7613 ), #85233, .F. ) ;
#50622=PLANE ( 'NONE',  #24923 ) ;
#50640=VECTOR ( 'NONE', #12911, 1000.000000000000000 ) ;
#50681=VERTEX_POINT ( 'NONE', #2517 ) ;
#50691=ORIENTED_EDGE ( 'NONE', *, *, #79919, .T. ) ;
#50692=CARTESIAN_POINT ( 'NONE',  ( -24.90875734969025501, -5.965225279485572685, 19.84760796525321780 ) ) ;
#50697=VERTEX_POINT ( 'NONE', #62414 ) ;
#50712=VECTOR ( 'NONE', #30276, 1000.000000000000000 ) ;
#50716=ADVANCED_FACE ( 'NONE', ( #41582 ), #9114, .F. ) ;
#50751=ORIENTED_EDGE ( 'NONE', *, *, #74622, .F. ) ;
#50753=CARTESIAN_POINT ( 'NONE',  ( 25.61870917940689196, 0.3587747205144265483, 29.49402280011862487 ) ) ;
#50759=DIRECTION ( 'NONE',  ( 1.000000000000000000, -0.000000000000000000, -0.000000000000000000 ) ) ;
#50761=VECTOR ( 'NONE', #96883, 1000.000000000000000 ) ;
#50766=LINE ( 'NONE', #44146, #20504 ) ;
#50779=CARTESIAN_POINT ( 'NONE',  ( 33.61456970919605425, 3.316774720514426900, -11.35828564741663449 ) ) ;
#50784=CARTESIAN_POINT ( 'NONE',  ( 13.91401389203221406, -5.965225279485572685, 158.0376437107427137 ) ) ;
#50791=ADVANCED_FACE ( 'NONE', ( #48700 ), #32961, .F. ) ;
#50793=CARTESIAN_POINT ( 'NONE',  ( 14.43441819133292370, 3.316774720514429120, -28.36222020317234183 ) ) ;
#50796=ORIENTED_EDGE ( 'NONE', *, *, #84088, .F. ) ;
#50801=CARTESIAN_POINT ( 'NONE',  ( 29.68632914399157130, 6.069062472358077720, 27.51067976151145800 ) ) ;
#50826=VECTOR ( 'NONE', #33986, 1000.000000000000000 ) ;
#50827=CARTESIAN_POINT ( 'NONE',  ( -10.59832330691884295, -5.965225279485572685, -27.05373799718300987 ) ) ;
#50838=EDGE_LOOP ( 'NONE', ( #41754, #29327, #20378, #26218 ) ) ;
#50853=VERTEX_POINT ( 'NONE', #73031 ) ;
#50857=EDGE_CURVE ( 'NONE', #84112, #91875, #52563, .T. ) ;
#50868=VECTOR ( 'NONE', #23798, 1000.000000000000000 ) ;
#50884=ORIENTED_EDGE ( 'NONE', *, *, #84767, .T. ) ;
#50895=LINE ( 'NONE', #2728, #49494 ) ;
#50901=DIRECTION ( 'NONE',  ( -0.000000000000000000, -1.000000000000000000, -0.000000000000000000 ) ) ;
#50909=ORIENTED_EDGE ( 'NONE', *, *, #98392, .F. ) ;
#50910=ADVANCED_FACE ( 'NONE', ( #26844 ), #19222, .F. ) ;
#50962=DIRECTION ( 'NONE',  ( 0.7071067811865474617, -0.000000000000000000, 0.7071067811865474617 ) ) ;
#50980=FACE_OUTER_BOUND ( 'NONE', #64088, .T. ) ;
#50981=EDGE_CURVE ( 'NONE', #88881, #57483, #83618, .T. ) ;
#50982=ORIENTED_EDGE ( 'NONE', *, *, #17827, .F. ) ;
#50989=LINE ( 'NONE', #94268, #61181 ) ;
#50998=DIRECTION ( 'NONE',  ( 0.000000000000000000, -1.000000000000000000, 0.000000000000000000 ) ) ;
#51005=CIRCLE ( 'NONE', #72088, 28.96799999999999642 ) ;
#51019=CARTESIAN_POINT ( 'NONE',  ( -0.02075734969026423599, 5.866774720514426278, -0.08597719988137648983 ) ) ;
#51025=DIRECTION ( 'NONE',  ( 0.000000000000000000, 0.000000000000000000, 1.000000000000000000 ) ) ;
#51029=B_SPLINE_CURVE_WITH_KNOTS ( 'NONE', 3,
 ( #62734, #76421, #15527, #61731 ),
 .UNSPECIFIED., .F., .F.,
 ( 4, 4 ),
 ( 0.000000000000000000, 0.001096191829319139886 ),
 .UNSPECIFIED. ) ;
#51035=CARTESIAN_POINT ( 'NONE',  ( 30.62555539057593634, 4.734697315945937568, 27.74929510164747981 ) ) ;
#51044=EDGE_CURVE ( 'NONE', #38058, #5126, #52662, .T. ) ;
#51045=ORIENTED_EDGE ( 'NONE', *, *, #66774, .F. ) ;
#51066=DIRECTION ( 'NONE',  ( 0.000000000000000000, 0.000000000000000000, -1.000000000000000000 ) ) ;
#51068=DIRECTION ( 'NONE',  ( 0.000000000000000000, 0.000000000000000000, 1.000000000000000000 ) ) ;
#51076=ORIENTED_EDGE ( 'NONE', *, *, #57246, .F. ) ;
#51077=LINE ( 'NONE', #82018, #27399 ) ;
#51100=ORIENTED_EDGE ( 'NONE', *, *, #51559, .F. ) ;
#51120=CARTESIAN_POINT ( 'NONE',  ( 30.93860345374796594, 0.6647747205144264315, 20.86760796525322093 ) ) ;
#51129=LINE ( 'NONE', #82568, #73149 ) ;
#51130=ORIENTED_EDGE ( 'NONE', *, *, #91023, .T. ) ;
#51148=DIRECTION ( 'NONE',  ( -1.000000000000000000, 2.464095846557964090E-17, -0.000000000000000000 ) ) ;
#51163=EDGE_CURVE ( 'NONE', #89486, #99675, #54687, .T. ) ;
#51170=DIRECTION ( 'NONE',  ( 5.328431011793917330E-15, 0.000000000000000000, 1.000000000000000000 ) ) ;
#51183=AXIS2_PLACEMENT_3D ( 'NONE', #54480, #13528, #73954 ) ;
#51186=LINE ( 'NONE', #3518, #66039 ) ;
#51187=AXIS2_PLACEMENT_3D ( 'NONE', #38541, #16199, #93830 ) ;
#51194=VERTEX_POINT ( 'NONE', #8504 ) ;
#51225=CARTESIAN_POINT ( 'NONE',  ( 11.80640562518893866, 3.316774720514426011, -27.06722565682295567 ) ) ;
#51238=FACE_OUTER_BOUND ( 'NONE', #32061, .T. ) ;
#51243=CIRCLE ( 'NONE', #10752, 252.4458649670781085 ) ;
#51257=CARTESIAN_POINT ( 'NONE',  ( 31.88667425545054002, -1.477225279485574028, -9.651215965565025812 ) ) ;
#51264=VERTEX_POINT ( 'NONE', #42474 ) ;
#51266=CARTESIAN_POINT ( 'NONE',  ( 6.875727764383598561, 6.376774720514445605, -25.57138887952572404 ) ) ;
#51271=CYLINDRICAL_SURFACE ( 'NONE', #80804, 2.499999999999995115 ) ;
#51275=CARTESIAN_POINT ( 'NONE',  ( 32.45853543194704116, 0.3587747205144265483, 9.169203677920338080 ) ) ;
#51287=ORIENTED_EDGE ( 'NONE', *, *, #25140, .F. ) ;
#51289=ORIENTED_EDGE ( 'NONE', *, *, #71711, .T. ) ;
#51309=ORIENTED_EDGE ( 'NONE', *, *, #88162, .F. ) ;
#51332=VERTEX_POINT ( 'NONE', #26229 ) ;
#51351=EDGE_LOOP ( 'NONE', ( #77587, #79306, #34967, #68654, #40460, #53071, #44821, #11575, #20305, #27278, #78489, #36997, #8512, #17264, #88504, #17088, #13729, #8465, #22625, #38810, #95082, #1931, #79262, #29647, #81531, #84377, #71651, #21972, #60101, #62389, #65302, #48465, #76140, #38484, #6305, #77231, #94603, #17104, #49511, #72415, #34215, #53736, #81343, #4012, #93531, #11029, #10873, #42856, #42118, #71820, #3869, #31675, #86209, #50982, #71535, #69745, #43980, #3815, #9919, #29087, #39720, #1000, #82347, #95984, #20997, #58950, #7034, #83903, #73603, #2434, #1661, #2324, #54322, #60198, #32215, #7485, #90233, #47094, #33174, #24963, #88435, #14732, #63720, #68966, #64391, #80048, #16802, #49092, #10573, #53846, #46301, #73806, #98452, #54586, #66156, #40868, #94996, #81552, #97253, #40734, #19819 ) ) ;
#51376=ORIENTED_EDGE ( 'NONE', *, *, #57239, .F. ) ;
#51377=DIRECTION ( 'NONE',  ( 0.000000000000000000, 0.000000000000000000, -1.000000000000000000 ) ) ;
#51379=AXIS2_PLACEMENT_3D ( 'NONE', #20813, #6098, #45672 ) ;
#51390=ADVANCED_FACE ( 'NONE', ( #65814 ), #88137, .F. ) ;
#51414=CARTESIAN_POINT ( 'NONE',  ( 15.03086228770605004, 5.128928118853486318, -26.95277610321158335 ) ) ;
#51415=AXIS2_PLACEMENT_3D ( 'NONE', #47344, #1674, #47845 ) ;
#51486=VERTEX_POINT ( 'NONE', #61683 ) ;
#51496=EDGE_CURVE ( 'NONE', #22449, #60562, #40329, .T. ) ;
#51511=CARTESIAN_POINT ( 'NONE',  ( 32.60294298177590377, 2.682774720514426559, -11.48871326860665931 ) ) ;
#51520=EDGE_CURVE ( 'NONE', #39655, #50276, #93102, .T. ) ;
#51531=CARTESIAN_POINT ( 'NONE',  ( 31.30917625415073502, 4.464831821618584051, 0.9454093304329914682 ) ) ;
#51533=ORIENTED_EDGE ( 'NONE', *, *, #87828, .T. ) ;
#51542=EDGE_CURVE ( 'NONE', #73142, #59834, #39821, .T. ) ;
#51549=AXIS2_PLACEMENT_3D ( 'NONE', #93541, #78810, #1217 ) ;
#51559=EDGE_CURVE ( 'NONE', #16105, #99116, #31613, .T. ) ;
#51584=CARTESIAN_POINT ( 'NONE',  ( 30.53060340732036337, 5.297812262124996785, 1.539714685317421505 ) ) ;
#51585=PLANE ( 'NONE',  #13034 ) ;
#51603=ORIENTED_EDGE ( 'NONE', *, *, #17223, .T. ) ;
#51615=ADVANCED_FACE ( 'NONE', ( #12362 ), #25601, .F. ) ;
#51628=DIRECTION ( 'NONE',  ( 0.000000000000000000, 0.000000000000000000, 1.000000000000000000 ) ) ;
#51647=CARTESIAN_POINT ( 'NONE',  ( 26.73860345374794178, 5.236715237616461849, -5.784298989603305685 ) ) ;
#51649=CARTESIAN_POINT ( 'NONE',  ( 9.451856243913134392, -6.475225279485569807, -27.03492916892036746 ) ) ;
#51659=AXIS2_PLACEMENT_3D ( 'NONE', #52190, #67926, #45084 ) ;
#51684=DIRECTION ( 'NONE',  ( 0.000000000000000000, -1.000000000000000000, -0.000000000000000000 ) ) ;
#51693=CARTESIAN_POINT ( 'NONE',  ( 32.16024265030974050, -5.965225279485572685, 14.03360796525321774 ) ) ;
#51701=LINE ( 'NONE', #89260, #57502 ) ;
#51713=ORIENTED_EDGE ( 'NONE', *, *, #17001, .F. ) ;
#51733=DIRECTION ( 'NONE',  ( 1.000000000000000000, 0.000000000000000000, 0.000000000000000000 ) ) ;
#51740=AXIS2_PLACEMENT_3D ( 'NONE', #31441, #23314, #14203 ) ;
#51743=EDGE_CURVE ( 'NONE', #45940, #42876, #7273, .T. ) ;
#51748=VERTEX_POINT ( 'NONE', #89005 ) ;
#51758=DIRECTION ( 'NONE',  ( 0.000000000000000000, 1.000000000000000000, 0.000000000000000000 ) ) ;
#51763=DIRECTION ( 'NONE',  ( 0.7682573101345366862, 0.000000000000000000, -0.6401411605457395515 ) ) ;
#51785=CARTESIAN_POINT ( 'NONE',  ( 30.54125281784916268, 0.6647747205144264315, 23.11160796525322070 ) ) ;
#51799=ORIENTED_EDGE ( 'NONE', *, *, #93664, .F. ) ;
#51800=AXIS2_PLACEMENT_3D ( 'NONE', #46223, #9159, #1058 ) ;
#51815=CARTESIAN_POINT ( 'NONE',  ( 7.347880794884120722E-16, 1.826774720514426464, -6.000000000000000888 ) ) ;
#51818=VERTEX_POINT ( 'NONE', #12858 ) ;
#51834=EDGE_LOOP ( 'NONE', ( #31733, #46863, #84564, #18496 ) ) ;
#51839=ORIENTED_EDGE ( 'NONE', *, *, #16723, .T. ) ;
#51844=EDGE_CURVE ( 'NONE', #57584, #23928, #25088, .T. ) ;
#51859=DIRECTION ( 'NONE',  ( 0.000000000000000000, -1.000000000000000000, 0.000000000000000000 ) ) ;
#51869=AXIS2_PLACEMENT_3D ( 'NONE', #4643, #80768, #11250 ) ;
#51880=ORIENTED_EDGE ( 'NONE', *, *, #30058, .T. ) ;
#51882=CARTESIAN_POINT ( 'NONE',  ( -24.90875734969025501, -5.965225279485572685, 30.00402280011862288 ) ) ;
#51897=CARTESIAN_POINT ( 'NONE',  ( -23.29179552176161749, -5.965225279485594001, -17.29637630388738501 ) ) ;
#51898=ORIENTED_EDGE ( 'NONE', *, *, #79548, .F. ) ;
#51914=LINE ( 'NONE', #83843, #37104 ) ;
#51917=ORIENTED_EDGE ( 'NONE', *, *, #80387, .F. ) ;
#51930=ORIENTED_EDGE ( 'NONE', *, *, #52595, .T. ) ;
#51944=CARTESIAN_POINT ( 'NONE',  ( -10.11875734969026297, -5.965225279485572685, 30.51402280011862089 ) ) ;
#51955=ORIENTED_EDGE ( 'NONE', *, *, #20317, .F. ) ;
#51956=VERTEX_POINT ( 'NONE', #10130 ) ;
#51974=ORIENTED_EDGE ( 'NONE', *, *, #67611, .T. ) ;
#51992=DIRECTION ( 'NONE',  ( 0.000000000000000000, 0.000000000000000000, -1.000000000000000000 ) ) ;
#52011=CARTESIAN_POINT ( 'NONE',  ( 9.843544857143434967, -6.475225279485573360, -27.49819965379373343 ) ) ;
#52012=CARTESIAN_POINT ( 'NONE',  ( -29.49875734969025842, 0.3587747205144265483, 17.86602280011862476 ) ) ;
#52023=DIRECTION ( 'NONE',  ( 0.000000000000000000, -1.000000000000000000, 0.000000000000000000 ) ) ;
#52025=DIRECTION ( 'NONE',  ( 0.000000000000000000, -1.000000000000000000, 0.000000000000000000 ) ) ;
#52026=CARTESIAN_POINT ( 'NONE',  ( 31.13513474936813807, 5.356774720514427379, 3.331262582247329185 ) ) ;
#52030=ORIENTED_EDGE ( 'NONE', *, *, #51559, .T. ) ;
#52035=EDGE_LOOP ( 'NONE', ( #85413, #69044, #85893, #41443, #1057, #59281, #1375 ) ) ;
#52042=CARTESIAN_POINT ( 'NONE',  ( 31.04236049493789906, -6.475225279485573360, 19.84760796525321780 ) ) ;
#52061=DIRECTION ( 'NONE',  ( -0.000000000000000000, -1.000000000000000000, -0.000000000000000000 ) ) ;
#52075=ADVANCED_FACE ( 'NONE', ( #57827 ), #74528, .F. ) ;
#52083=ORIENTED_EDGE ( 'NONE', *, *, #71219, .F. ) ;
#52088=EDGE_CURVE ( 'NONE', #80349, #58159, #65620, .T. ) ;
#52090=VERTEX_POINT ( 'NONE', #20232 ) ;
#52113=EDGE_CURVE ( 'NONE', #63837, #78861, #51701, .T. ) ;
#52114=PLANE ( 'NONE',  #51183 ) ;
#52126=CARTESIAN_POINT ( 'NONE',  ( -27.86046284349298219, 0.3587747205143967943, -8.091963836038763347 ) ) ;
#52151=EDGE_LOOP ( 'NONE', ( #18598, #12610, #80541, #94355 ) ) ;
#52164=EDGE_CURVE ( 'NONE', #38058, #45825, #62412, .T. ) ;
#52175=VERTEX_POINT ( 'NONE', #96370 ) ;
#52178=B_SPLINE_CURVE_WITH_KNOTS ( 'NONE', 3,
 ( #59888, #51266, #11689, #5581, #66020, #90820, #74590, #81215, #13181, #73605, #4600, #82702 ),
 .UNSPECIFIED., .F., .F.,
 ( 4, 2, 2, 2, 2, 4 ),
 ( -0.003357017750235514672, -0.001150730439442379169, 0.001055556871350756334, 0.002158700526747327555, 0.003261844182143899644, 0.005468131492937042953 ),
 .UNSPECIFIED. ) ;
#52185=EDGE_CURVE ( 'NONE', #97904, #89884, #81649, .T. ) ;
#52190=CARTESIAN_POINT ( 'NONE',  ( 27.86270917940689174, 0.3587747205144265483, 29.49402280011862487 ) ) ;
#52195=ORIENTED_EDGE ( 'NONE', *, *, #4476, .T. ) ;
#52214=ORIENTED_EDGE ( 'NONE', *, *, #26470, .F. ) ;
#52227=CARTESIAN_POINT ( 'NONE',  ( 6.620851319379956301, 3.316774720514426011, -27.30756699305372592 ) ) ;
#52235=EDGE_CURVE ( 'NONE', #46666, #36769, #23735, .T. ) ;
#52255=CARTESIAN_POINT ( 'NONE',  ( 0.000000000000000000, 1.826774720514426464, 0.000000000000000000 ) ) ;
#52258=CARTESIAN_POINT ( 'NONE',  ( -13.89275734969026566, -5.965225279485572685, 30.51402280011862089 ) ) ;
#52275=DIRECTION ( 'NONE',  ( 0.000000000000000000, -1.000000000000000000, 0.000000000000000000 ) ) ;
#52277=LINE ( 'NONE', #34179, #73855 ) ;
#52294=EDGE_CURVE ( 'NONE', #71759, #57678, #32865, .T. ) ;
#52296=CARTESIAN_POINT ( 'NONE',  ( 32.98733314340959311, -5.965225279485572685, 2.074222136288530027 ) ) ;
#52339=CARTESIAN_POINT ( 'NONE',  ( 30.53060340732036337, -1.477225279485574028, -1.352392034746782823 ) ) ;
#52350=CIRCLE ( 'NONE', #94496, 129.7684398600581517 ) ;
#52352=CARTESIAN_POINT ( 'NONE',  ( 22.02124265030973760, 3.456774720514426136, 16.20402280011862217 ) ) ;
#52365=VERTEX_POINT ( 'NONE', #48606 ) ;
#52391=ORIENTED_EDGE ( 'NONE', *, *, #39411, .F. ) ;
#52408=AXIS2_PLACEMENT_3D ( 'NONE', #93004, #85395, #21491 ) ;
#52409=EDGE_CURVE ( 'NONE', #99116, #92497, #18134, .T. ) ;
#52412=ORIENTED_EDGE ( 'NONE', *, *, #86332, .T. ) ;
#52417=ADVANCED_FACE ( 'NONE', ( #20127 ), #42984, .T. ) ;
#52429=CARTESIAN_POINT ( 'NONE',  ( -4.568292318365942073, -5.965225279485572685, 30.06720597538392425 ) ) ;
#52430=ORIENTED_EDGE ( 'NONE', *, *, #58026, .F. ) ;
#52446=DIRECTION ( 'NONE',  ( -0.000000000000000000, -1.000000000000000000, -0.000000000000000000 ) ) ;
#52449=ORIENTED_EDGE ( 'NONE', *, *, #53172, .T. ) ;
#52451=ORIENTED_EDGE ( 'NONE', *, *, #86302, .F. ) ;
#52453=AXIS2_PLACEMENT_3D ( 'NONE', #81077, #89192, #58247 ) ;
#52461=VECTOR ( 'NONE', #58855, 1000.000000000000000 ) ;
#52472=EDGE_LOOP ( 'NONE', ( #28552, #72489, #41468, #82535 ) ) ;
#52477=CARTESIAN_POINT ( 'NONE',  ( -20.27875734969026311, 3.456774720514426136, 25.15402280011862146 ) ) ;
#52490=DIRECTION ( 'NONE',  ( 0.000000000000000000, 1.000000000000000000, 0.000000000000000000 ) ) ;
#52511=DIRECTION ( 'NONE',  ( 0.000000000000000000, 0.000000000000000000, -1.000000000000000000 ) ) ;
#52517=CARTESIAN_POINT ( 'NONE',  ( 30.00738719773716312, -1.477225279485574028, -9.049252915307087974 ) ) ;
#52522=DIRECTION ( 'NONE',  ( -8.503546450866701308E-16, 0.000000000000000000, 1.000000000000000000 ) ) ;
#52542=ORIENTED_EDGE ( 'NONE', *, *, #70205, .F. ) ;
#52560=EDGE_CURVE ( 'NONE', #77258, #46666, #26748, .T. ) ;
#52563=CIRCLE ( 'NONE', #15307, 3.060000000000000053 ) ;
#52584=ORIENTED_EDGE ( 'NONE', *, *, #85027, .T. ) ;
#52591=AXIS2_PLACEMENT_3D ( 'NONE', #1708, #94039, #92534 ) ;
#52594=EDGE_CURVE ( 'NONE', #91590, #75060, #19124, .T. ) ;
#52595=EDGE_CURVE ( 'NONE', #97022, #43843, #55976, .T. ) ;
#52606=DIRECTION ( 'NONE',  ( -0.9978940991575084851, -0.000000000000000000, -0.06486421869277853025 ) ) ;
#52608=DIRECTION ( 'NONE',  ( 0.6599726524652352877, 0.000000000000000000, -0.7512896232465891000 ) ) ;
#52624=CARTESIAN_POINT ( 'NONE',  ( -17.66201745896767505, 0.3587747205144061202, -23.06272557202527906 ) ) ;
#52637=CARTESIAN_POINT ( 'NONE',  ( 14.52511747680497933, -5.965225279485572685, -27.86035006098926559 ) ) ;
#52645=CYLINDRICAL_SURFACE ( 'NONE', #73693, 1.325999999999990298 ) ;
#52647=ADVANCED_FACE ( 'NONE', ( #99721 ), #13502, .F. ) ;
#52650=LINE ( 'NONE', #68870, #62553 ) ;
#52657=DIRECTION ( 'NONE',  ( 0.000000000000000000, 1.000000000000000000, -0.000000000000000000 ) ) ;
#52662=B_SPLINE_CURVE_WITH_KNOTS ( 'NONE', 3,
 ( #83113, #44569, #77495, #9499, #24716, #17615, #18117, #70404, #78497, #1402, #40461, #33330, #47076, #55195 ),
 .UNSPECIFIED., .F., .F.,
 ( 4, 2, 2, 2, 2, 2, 4 ),
 ( 3.469446951953614189E-18, 0.0003991292329371358004, 0.0007982584658742681314, 0.001197387698811397914, 0.001596516931748527806, 0.002394775397622781951, 0.003193033863497036530 ),
 .UNSPECIFIED. ) ;
#52686=VERTEX_POINT ( 'NONE', #67313 ) ;
#52688=DIRECTION ( 'NONE',  ( -4.163336342344339393E-15, 0.000000000000000000, -1.000000000000000000 ) ) ;
#52689=EDGE_LOOP ( 'NONE', ( #76265, #14240, #46420, #35753 ) ) ;
#52696=VERTEX_POINT ( 'NONE', #44974 ) ;
#52712=EDGE_LOOP ( 'NONE', ( #76492, #71917, #40657, #84207, #78981, #59053 ) ) ;
#52721=DIRECTION ( 'NONE',  ( 0.000000000000000000, 0.000000000000000000, 1.000000000000000000 ) ) ;
#52729=CARTESIAN_POINT ( 'NONE',  ( 12.46431485231495806, 4.283161447665844612, -27.85634418129429690 ) ) ;
#52731=CYLINDRICAL_SURFACE ( 'NONE', #83539, 6.000000000000000888 ) ;
#52750=EDGE_CURVE ( 'NONE', #23691, #74060, #83515, .T. ) ;
#52757=CARTESIAN_POINT ( 'NONE',  ( -27.83739072329610664, 0.3587747205143967943, -8.084349702057700426 ) ) ;
#52770=CARTESIAN_POINT ( 'NONE',  ( -28.32169924589829080, -5.965225279485592225, -8.244178532169447848 ) ) ;
#52771=AXIS2_PLACEMENT_3D ( 'NONE', #6038, #44112, #52721 ) ;
#52776=AXIS2_PLACEMENT_3D ( 'NONE', #4503, #94901, #92891 ) ;
#52791=ORIENTED_EDGE ( 'NONE', *, *, #86089, .F. ) ;
#52814=DIRECTION ( 'NONE',  ( 0.000000000000000000, 0.000000000000000000, -1.000000000000000000 ) ) ;
#52823=CARTESIAN_POINT ( 'NONE',  ( 15.14080536460164517, 5.152774720514427642, -26.62908960815038384 ) ) ;
#52824=CARTESIAN_POINT ( 'NONE',  ( 32.33408272158504815, 4.458032690740698634, 0.9207958043952065852 ) ) ;
#52833=VECTOR ( 'NONE', #52839, 1000.000000000000000 ) ;
#52839=DIRECTION ( 'NONE',  ( -0.9496245541219264785, -6.845827386180410961E-16, -0.3133898629642195011 ) ) ;
#52850=CARTESIAN_POINT ( 'NONE',  ( -20.77875734969026311, -6.143225279485574397, 27.35402280011862430 ) ) ;
#52878=MECHANICAL_CONTEXT ( 'NONE', #9663, 'mechanical' ) ;
#52883=DIRECTION ( 'NONE',  ( 0.000000000000000000, -1.000000000000000000, 0.000000000000000000 ) ) ;
#52891=ORIENTED_EDGE ( 'NONE', *, *, #665, .F. ) ;
#52912=CIRCLE ( 'NONE', #78821, 4.080000000000000071 ) ;
#52917=CARTESIAN_POINT ( 'NONE',  ( 22.02124265030973760, -6.143225279485574397, 18.45402280011862217 ) ) ;
#52927=EDGE_LOOP ( 'NONE', ( #99830, #41767, #68792, #95630 ) ) ;
#52929=ORIENTED_EDGE ( 'NONE', *, *, #57370, .F. ) ;
#52935=DIRECTION ( 'NONE',  ( 0.06283980576413537855, 0.000000000000000000, 0.9980236263794188822 ) ) ;
#52986=VERTEX_POINT ( 'NONE', #10900 ) ;
#52997=CIRCLE ( 'NONE', #47914, 1.150000000000003464 ) ;
#53024=LINE ( 'NONE', #52517, #45939 ) ;
#53031=CARTESIAN_POINT ( 'NONE',  ( -0.02075734969026423599, 6.376774720514426953, -0.08597719988137648983 ) ) ;
#53032=CARTESIAN_POINT ( 'NONE',  ( -24.90875734969025501, 3.316774720514426456, 26.43402280011862615 ) ) ;
#53053=ADVANCED_FACE ( 'NONE', ( #65709 ), #96622, .F. ) ;
#53062=CARTESIAN_POINT ( 'NONE',  ( -28.98875734969026041, 6.376774720514426953, 0.7300228001186309656 ) ) ;
#53064=CIRCLE ( 'NONE', #20661, 4.080000000000000071 ) ;
#53071=ORIENTED_EDGE ( 'NONE', *, *, #66764, .F. ) ;
#53077=PLANE ( 'NONE',  #90542 ) ;
#53098=CARTESIAN_POINT ( 'NONE',  ( 5.184553252003285984, -5.965225279485572685, -28.06387035751381731 ) ) ;
#53110=CARTESIAN_POINT ( 'NONE',  ( -10.40290173325841216, 5.356774720514425603, 27.45402280011861862 ) ) ;
#53119=CIRCLE ( 'NONE', #17396, 251.4258649670780699 ) ;
#53120=FACE_OUTER_BOUND ( 'NONE', #60931, .T. ) ;
#53172=EDGE_CURVE ( 'NONE', #60950, #86083, #67695, .T. ) ;
#53178=DIRECTION ( 'NONE',  ( -0.000000000000000000, 1.000000000000000000, -0.000000000000000000 ) ) ;
#53190=VECTOR ( 'NONE', #78053, 1000.000000000000114 ) ;
#53197=DIRECTION ( 'NONE',  ( 0.000000000000000000, -1.000000000000000000, 0.000000000000000000 ) ) ;
#53208=LINE ( 'NONE', #913, #78889 ) ;
#53212=EDGE_CURVE ( 'NONE', #89486, #17142, #23552, .T. ) ;
#53217=AXIS2_PLACEMENT_3D ( 'NONE', #21054, #52025, #9833 ) ;
#53229=CARTESIAN_POINT ( 'NONE',  ( 14.61581676225068449, -6.475225279485576912, -27.35847991880143226 ) ) ;
#53237=DIRECTION ( 'NONE',  ( -0.000000000000000000, -1.000000000000000000, -0.000000000000000000 ) ) ;
#53238=DIRECTION ( 'NONE',  ( 0.000000000000000000, 1.000000000000000000, 0.000000000000000000 ) ) ;
#53249=EDGE_LOOP ( 'NONE', ( #82762, #35768, #13914, #31843, #82433, #90994, #89660 ) ) ;
#53298=LINE ( 'NONE', #59407, #17747 ) ;
#53303=ORIENTED_EDGE ( 'NONE', *, *, #24387, .T. ) ;
#53327=VECTOR ( 'NONE', #90131, 1000.000000000000000 ) ;
#53335=AXIS2_PLACEMENT_3D ( 'NONE', #60653, #4366, #66780 ) ;
#53336=ORIENTED_EDGE ( 'NONE', *, *, #77510, .T. ) ;
#53359=ADVANCED_FACE ( 'NONE', ( #56469 ), #87394, .T. ) ;
#53365=EDGE_LOOP ( 'NONE', ( #96773, #38468, #40293, #36454, #71799 ) ) ;
#53369=PLANE ( 'NONE',  #9090 ) ;
#53376=EDGE_CURVE ( 'NONE', #48796, #1553, #7334, .T. ) ;
#53380=CARTESIAN_POINT ( 'NONE',  ( 10.74487964110493188, 6.376774720514429617, -24.99341878722455235 ) ) ;
#53385=CARTESIAN_POINT ( 'NONE',  ( -12.84880425037202656, 0.3587747205143964613, -26.59900746623529244 ) ) ;
#53386=LINE ( 'NONE', #30532, #92841 ) ;
#53402=CARTESIAN_POINT ( 'NONE',  ( 20.13489193910630703, 2.682774720514426559, -22.92085183005112370 ) ) ;
#53415=CARTESIAN_POINT ( 'NONE',  ( -41.32836283488544638, 6.376774720514426953, 39.26872235229541985 ) ) ;
#53491=CARTESIAN_POINT ( 'NONE',  ( -28.32169924589829080, -5.965225279485592225, -8.244178532169447848 ) ) ;
#53510=DIRECTION ( 'NONE',  ( -0.06486421869277853025, 0.000000000000000000, 0.9978940991575085961 ) ) ;
#53519=CARTESIAN_POINT ( 'NONE',  ( -0.02075734969026423599, 3.316774720514426456, -0.08597719988137648983 ) ) ;
#53552=DIRECTION ( 'NONE',  ( 0.000000000000000000, 0.000000000000000000, -1.000000000000000000 ) ) ;
#53559=LINE ( 'NONE', #7354, #60619 ) ;
#53564=EDGE_CURVE ( 'NONE', #23842, #34210, #88235, .T. ) ;
#53601=DIRECTION ( 'NONE',  ( -1.000000000000000000, 0.000000000000000000, -7.994117400814786717E-16 ) ) ;
#53611=ORIENTED_EDGE ( 'NONE', *, *, #54512, .F. ) ;
#53618=CARTESIAN_POINT ( 'NONE',  ( 31.64143112576189765, 0.3587747205144265483, 14.03360796525321774 ) ) ;
#53620=PLANE ( 'NONE',  #40057 ) ;
#53622=AXIS2_PLACEMENT_3D ( 'NONE', #82916, #74321, #91532 ) ;
#53625=AXIS2_PLACEMENT_3D ( 'NONE', #95372, #48721, #80149 ) ;
#53639=CARTESIAN_POINT ( 'NONE',  ( 0.000000000000000000, 1.826774720514426464, 0.000000000000000000 ) ) ;
#53652=CARTESIAN_POINT ( 'NONE',  ( 30.61643171304413613, 3.316774720514426456, 27.37433008668288181 ) ) ;
#53681=ORIENTED_EDGE ( 'NONE', *, *, #14856, .T. ) ;
#53683=ORIENTED_EDGE ( 'NONE', *, *, #49385, .F. ) ;
#53699=DIRECTION ( 'NONE',  ( -1.334402673828313093E-16, -0.000000000000000000, -1.000000000000000000 ) ) ;
#53725=VERTEX_POINT ( 'NONE', #36429 ) ;
#53735=EDGE_CURVE ( 'NONE', #12600, #85772, #60894, .T. ) ;
#53736=ORIENTED_EDGE ( 'NONE', *, *, #65667, .F. ) ;
#53755=FACE_OUTER_BOUND ( 'NONE', #87138, .T. ) ;
#53786=DIRECTION ( 'NONE',  ( 0.000000000000000000, -0.000000000000000000, -1.000000000000000000 ) ) ;
#53812=ORIENTED_EDGE ( 'NONE', *, *, #69436, .F. ) ;
#53818=ORIENTED_EDGE ( 'NONE', *, *, #99578, .T. ) ;
#53834=ORIENTED_EDGE ( 'NONE', *, *, #23185, .T. ) ;
#53846=ORIENTED_EDGE ( 'NONE', *, *, #43413, .T. ) ;
#53849=ADVANCED_FACE ( 'NONE', ( #92210 ), #22683, .F. ) ;
#53856=EDGE_CURVE ( 'NONE', #76588, #69379, #75495, .T. ) ;
#53874=VECTOR ( 'NONE', #39394, 1000.000000000000000 ) ;
#53875=CARTESIAN_POINT ( 'NONE',  ( 8.422997646657599091, 6.376774720514429617, -25.04887774224060237 ) ) ;
#53883=CARTESIAN_POINT ( 'NONE',  ( 31.79364159983995464, -6.475225279485573360, -11.59305536555894278 ) ) ;
#53887=DIRECTION ( 'NONE',  ( 0.000000000000000000, 1.000000000000000000, 0.000000000000000000 ) ) ;
#53894=AXIS2_PLACEMENT_3D ( 'NONE', #84543, #21633, #22133 ) ;
#53898=CARTESIAN_POINT ( 'NONE',  ( 29.73860345376319003, 5.356471260711259674, 19.84760796525321780 ) ) ;
#53912=CARTESIAN_POINT ( 'NONE',  ( -4.993225604111835914, -5.965225279485592225, -29.11654937215278593 ) ) ;
#53931=EDGE_LOOP ( 'NONE', ( #8406, #60909, #36373, #28371 ) ) ;
#53942=CARTESIAN_POINT ( 'NONE',  ( 4.784292611718075072, 6.376774720514426953, -25.54547254883186014 ) ) ;
#53958=ORIENTED_EDGE ( 'NONE', *, *, #44609, .F. ) ;
#53974=ADVANCED_FACE ( 'NONE', ( #43624 ), #52731, .T. ) ;
#53997=B_SPLINE_SURFACE_WITH_KNOTS ( 'NONE', 3, 1, ( 
 ( #24270, #62347 ),
 ( #54738, #31888 ),
 ( #16152, #85166 ),
 ( #32385, #47123 ),
 ( #100367, #30884 ),
 ( #78036, #55243 ) ),
 .UNSPECIFIED., .F., .F., .F.,
 ( 4, 1, 1, 4 ),
 ( 2, 2 ),
 ( 0.3456157426780491759, 0.5751927948816943914, 0.7454075661435733968, 0.9439799182910603159 ),
 ( 0.000000000000000000, 1.000000000000000000 ),
 .UNSPECIFIED. ) ;
#54003=CARTESIAN_POINT ( 'NONE',  ( 22.81105451610979173, -1.477225279485574028, -18.46691820600746681 ) ) ;
#54022=VECTOR ( 'NONE', #58148, 1000.000000000000000 ) ;
#54025=CARTESIAN_POINT ( 'NONE',  ( 282.9764569301858046, 0.3587747205144265483, 20.79159422840526616 ) ) ;
#54039=ORIENTED_EDGE ( 'NONE', *, *, #51542, .F. ) ;
#54047=FACE_OUTER_BOUND ( 'NONE', #69789, .T. ) ;
#54071=CARTESIAN_POINT ( 'NONE',  ( -10.31943567505730996, 5.151096386430394247, 28.35664311630200984 ) ) ;
#54074=ADVANCED_FACE ( 'NONE', ( #55246 ), #63366, .F. ) ;
#54087=ORIENTED_EDGE ( 'NONE', *, *, #12820, .F. ) ;
#54097=LINE ( 'NONE', #45978, #76431 ) ;
#54105=EDGE_LOOP ( 'NONE', ( #30053, #79980, #68411, #27334, #10286, #1640, #81638, #20613, #86253, #22400 ) ) ;
#54118=CARTESIAN_POINT ( 'NONE',  ( 30.45304879119406039, -1.477225279485574028, -10.07140455160086390 ) ) ;
#54122=CARTESIAN_POINT ( 'NONE',  ( 32.98733314340959311, 0.3587747205144265483, 2.074222136288530027 ) ) ;
#54127=CARTESIAN_POINT ( 'NONE',  ( 0.000000000000000000, -6.943225279485572443, 0.000000000000000000 ) ) ;
#54136=EDGE_CURVE ( 'NONE', #62785, #74167, #5049, .T. ) ;
#54137=CARTESIAN_POINT ( 'NONE',  ( -29.49975734969026320, -6.475225279485573360, 25.41160796525322141 ) ) ;
#54165=CARTESIAN_POINT ( 'NONE',  ( 32.24176898385614720, 6.243294140736224129, 2.116998906223433341 ) ) ;
#54182=CARTESIAN_POINT ( 'NONE',  ( 12.40597316965629560, 5.152774720514427642, -26.28458722401733993 ) ) ;
#54184=VERTEX_POINT ( 'NONE', #50122 ) ;
#54202=CARTESIAN_POINT ( 'NONE',  ( 15.38791554121727678, 3.579805417253320687, -28.27843079449247199 ) ) ;
#54212=ORIENTED_EDGE ( 'NONE', *, *, #2398, .T. ) ;
#54217=DIRECTION ( 'NONE',  ( 0.000000000000000000, 0.000000000000000000, 1.000000000000000000 ) ) ;
#54221=LINE ( 'NONE', #85146, #10327 ) ;
#54225=VECTOR ( 'NONE', #96819, 1000.000000000000000 ) ;
#54228=VERTEX_POINT ( 'NONE', #33382 ) ;
#54230=LINE ( 'NONE', #45610, #14141 ) ;
#54266=CARTESIAN_POINT ( 'NONE',  ( 282.9764569301858046, 0.6647747205144264315, 20.79159422840526616 ) ) ;
#54267=CARTESIAN_POINT ( 'NONE',  ( -19.80875734969026425, -5.965225279485572685, 30.51402280011862089 ) ) ;
#54271=AXIS2_PLACEMENT_3D ( 'NONE', #43269, #39015, #21392 ) ;
#54299=ORIENTED_EDGE ( 'NONE', *, *, #59473, .F. ) ;
#54306=DIRECTION ( 'NONE',  ( -0.9978940991575084851, 0.000000000000000000, -0.06486421869277853025 ) ) ;
#54307=VECTOR ( 'NONE', #750, 1000.000000000000000 ) ;
#54316=ORIENTED_EDGE ( 'NONE', *, *, #93792, .T. ) ;
#54320=VERTEX_POINT ( 'NONE', #187 ) ;
#54322=ORIENTED_EDGE ( 'NONE', *, *, #41188, .T. ) ;
#54334=VECTOR ( 'NONE', #40667, 1000.000000000000000 ) ;
#54336=ORIENTED_EDGE ( 'NONE', *, *, #60037, .T. ) ;
#54356=CARTESIAN_POINT ( 'NONE',  ( -29.49875734969026198, -5.965225279485572685, 7.870022800118625206 ) ) ;
#54362=AXIS2_PLACEMENT_3D ( 'NONE', #64177, #23569, #55046 ) ;
#54363=DIRECTION ( 'NONE',  ( 1.000000000000000000, -0.000000000000000000, 0.000000000000000000 ) ) ;
#54364=ORIENTED_EDGE ( 'NONE', *, *, #44609, .T. ) ;
#54365=DIRECTION ( 'NONE',  ( 0.7512896232465892110, -0.000000000000000000, 0.6599726524652352877 ) ) ;
#54369=ORIENTED_EDGE ( 'NONE', *, *, #87417, .F. ) ;
#54374=CIRCLE ( 'NONE', #51187, 1.149999999999999911 ) ;
#54378=CARTESIAN_POINT ( 'NONE',  ( 8.817327481837082814, 3.316774720514257702, -28.08864864913269699 ) ) ;
#54382=DIRECTION ( 'NONE',  ( -0.7512896232465891000, 0.000000000000000000, -0.6599726524652351767 ) ) ;
#54385=DIRECTION ( 'NONE',  ( 0.000000000000000000, 0.000000000000000000, -1.000000000000000000 ) ) ;
#54390=ADVANCED_FACE ( 'NONE', ( #90666 ), #52114, .F. ) ;
#54402=DIRECTION ( 'NONE',  ( 0.000000000000000000, 0.000000000000000000, 1.000000000000000000 ) ) ;
#54405=DIRECTION ( 'NONE',  ( 0.000000000000000000, 0.000000000000000000, -1.000000000000000000 ) ) ;
#54409=ADVANCED_FACE ( 'NONE', ( #76789 ), #27773, .T. ) ;
#54435=CARTESIAN_POINT ( 'NONE',  ( 6.184520403203634942, 6.376774720514426953, -25.32021290018218451 ) ) ;
#54448=DIRECTION ( 'NONE',  ( 5.328431011793917330E-15, 0.000000000000000000, 1.000000000000000000 ) ) ;
#54458=ORIENTED_EDGE ( 'NONE', *, *, #93418, .F. ) ;
#54463=ADVANCED_FACE ( 'NONE', ( #26025 ), #85928, .F. ) ;
#54468=DIRECTION ( 'NONE',  ( 0.000000000000000000, -1.000000000000000000, 0.000000000000000000 ) ) ;
#54472=FACE_OUTER_BOUND ( 'NONE', #62301, .T. ) ;
#54480=CARTESIAN_POINT ( 'NONE',  ( 13.10664265030973930, -5.965225279485574461, -27.62597719988137612 ) ) ;
#54507=ADVANCED_FACE ( 'NONE', ( #48879 ), #77790, .T. ) ;
#54512=EDGE_CURVE ( 'NONE', #49424, #52090, #7412, .T. ) ;
#54513=DIRECTION ( 'NONE',  ( 0.7512896232465892110, -0.000000000000000000, 0.6599726524652351767 ) ) ;
#54536=DIRECTION ( 'NONE',  ( 0.000000000000000000, 0.000000000000000000, -1.000000000000000000 ) ) ;
#54542=CARTESIAN_POINT ( 'NONE',  ( -12.84880425037203011, -5.965225279485592225, -26.59900746623528534 ) ) ;
#54547=VERTEX_POINT ( 'NONE', #1702 ) ;
#54557=CIRCLE ( 'NONE', #10809, 251.4258649670780699 ) ;
#54573=VERTEX_POINT ( 'NONE', #95037 ) ;
#54579=DIRECTION ( 'NONE',  ( -0.000000000000000000, -1.000000000000000000, -0.000000000000000000 ) ) ;
#54586=ORIENTED_EDGE ( 'NONE', *, *, #58858, .F. ) ;
#54594=ADVANCED_FACE ( 'NONE', ( #31631 ), #40752, .F. ) ;
#54598=ORIENTED_EDGE ( 'NONE', *, *, #73938, .T. ) ;
#54603=ORIENTED_EDGE ( 'NONE', *, *, #65989, .T. ) ;
#54604=CARTESIAN_POINT ( 'NONE',  ( 22.81105451610979173, -1.475225279485572916, -18.46691820600746681 ) ) ;
#54611=CARTESIAN_POINT ( 'NONE',  ( -53.01255352321339842, 2.682774720514426559, 35.59556822165056644 ) ) ;
#54645=CARTESIAN_POINT ( 'NONE',  ( 30.58729439590577570, 4.540774720514427543, 26.14186284044645703 ) ) ;
#54653=CARTESIAN_POINT ( 'NONE',  ( 22.02124265030973760, 3.456774720514426136, 15.05402280011862004 ) ) ;
#54674=CARTESIAN_POINT ( 'NONE',  ( -25.92875734969025814, 3.316774720514426456, 30.51402280011862089 ) ) ;
#54678=EDGE_LOOP ( 'NONE', ( #96977, #16176, #19703, #16257 ) ) ;
#54679=ORIENTED_EDGE ( 'NONE', *, *, #92934, .T. ) ;
#54687=LINE ( 'NONE', #85618, #8807 ) ;
#54702=ADVANCED_FACE ( 'NONE', ( #87932 ), #41773, .F. ) ;
#54703=B_SPLINE_SURFACE_WITH_KNOTS ( 'NONE', 3, 1, ( 
 ( #96679, #10444 ),
 ( #20058, #72861 ),
 ( #18557, #87575 ),
 ( #80461, #19554 ),
 ( #50513, #73848 ),
 ( #97186, #18059 ) ),
 .UNSPECIFIED., .F., .F., .F.,
 ( 4, 2, 4 ),
 ( 2, 2 ),
 ( 0.000000000000000000, 0.5000000000000000000, 1.000000000000000000 ),
 ( 0.000000000000000000, 1.000000000000000000 ),
 .UNSPECIFIED. ) ;
#54724=AXIS2_PLACEMENT_3D ( 'NONE', #19223, #35465, #73524 ) ;
#54726=ORIENTED_EDGE ( 'NONE', *, *, #73493, .F. ) ;
#54738=CARTESIAN_POINT ( 'NONE',  ( 6.437068816671457583, 3.316774720514427344, -28.37834077173919667 ) ) ;
#54749=CARTESIAN_POINT ( 'NONE',  ( -28.84663072490566194, 0.3587747205144265483, 28.73989617533406715 ) ) ;
#54760=DIRECTION ( 'NONE',  ( -0.000000000000000000, -1.000000000000000000, 0.000000000000000000 ) ) ;
#54763=AXIS2_PLACEMENT_3D ( 'NONE', #24866, #84889, #55841 ) ;
#54767=EDGE_CURVE ( 'NONE', #11050, #80312, #46390, .T. ) ;
#54785=VECTOR ( 'NONE', #60131, 1000.000000000000000 ) ;
#54788=ORIENTED_EDGE ( 'NONE', *, *, #78685, .T. ) ;
#54827=ADVANCED_FACE ( 'NONE', ( #76668 ), #53369, .T. ) ;
#54861=LINE ( 'NONE', #2574, #55231 ) ;
#54876=FACE_OUTER_BOUND ( 'NONE', #91085, .T. ) ;
#54884=ORIENTED_EDGE ( 'NONE', *, *, #57699, .F. ) ;
#54892=DIRECTION ( 'NONE',  ( 0.000000000000000000, 0.000000000000000000, 1.000000000000000000 ) ) ;
#54908=CARTESIAN_POINT ( 'NONE',  ( 22.81105451610979173, 2.682774720514426559, -18.46691820600746681 ) ) ;
#54922=ORIENTED_EDGE ( 'NONE', *, *, #13967, .T. ) ;
#54935=ORIENTED_EDGE ( 'NONE', *, *, #39012, .F. ) ;
#54951=CARTESIAN_POINT ( 'NONE',  ( -20.27875734969026311, -4.543225279485573864, 24.00402280011862288 ) ) ;
#54952=VERTEX_POINT ( 'NONE', #93407 ) ;
#54955=ORIENTED_EDGE ( 'NONE', *, *, #90530, .T. ) ;
#54964=ADVANCED_FACE ( 'NONE', ( #9687 ), #71597, .T. ) ;
#54976=CARTESIAN_POINT ( 'NONE',  ( 30.32108885906865936, 4.540774720514427543, 3.274824222184972822 ) ) ;
#54989=VECTOR ( 'NONE', #88014, 1000.000000000000000 ) ;
#54994=AXIS2_PLACEMENT_3D ( 'NONE', #53062, #29708, #92590 ) ;
#54996=ORIENTED_EDGE ( 'NONE', *, *, #15857, .F. ) ;
#55005=EDGE_CURVE ( 'NONE', #22611, #74525, #56385, .T. ) ;
#55026=DIRECTION ( 'NONE',  ( -0.9888510809027408754, 5.365801633547210331E-16, -0.1489078231574191558 ) ) ;
#55034=ORIENTED_EDGE ( 'NONE', *, *, #59098, .T. ) ;
#55046=DIRECTION ( 'NONE',  ( 8.503546450866693616E-15, 0.000000000000000000, 1.000000000000000000 ) ) ;
#55050=ORIENTED_EDGE ( 'NONE', *, *, #1627, .F. ) ;
#55052=ORIENTED_EDGE ( 'NONE', *, *, #17760, .T. ) ;
#55061=DIRECTION ( 'NONE',  ( 0.000000000000000000, 0.000000000000000000, -1.000000000000000000 ) ) ;
#55062=CARTESIAN_POINT ( 'NONE',  ( -10.26072176705811145, 4.666310954396869271, 28.98969649327457532 ) ) ;
#55067=VERTEX_POINT ( 'NONE', #15787 ) ;
#55068=CARTESIAN_POINT ( 'NONE',  ( -28.98875734969026396, -5.965225279485572685, 7.870022800118628759 ) ) ;
#55072=CIRCLE ( 'NONE', #27546, 84.48086791635431325 ) ;
#55079=CIRCLE ( 'NONE', #12969, 3.349999999999998757 ) ;
#55086=CARTESIAN_POINT ( 'NONE',  ( 29.73860345376319003, -1.477225279485574028, 19.84760796525321780 ) ) ;
#55101=DIRECTION ( 'NONE',  ( 1.000000000000000000, -0.000000000000000000, -0.000000000000000000 ) ) ;
#55140=CARTESIAN_POINT ( 'NONE',  ( 15.98182857103851795, 3.492575169077971609, -27.92678846288758976 ) ) ;
#55151=DIRECTION ( 'NONE',  ( 0.000000000000000000, -1.000000000000000000, 0.000000000000000000 ) ) ;
#55157=SHAPE_REPRESENTATION_RELATIONSHIP ( 'NONE' , 'NONE' ,  #44034, #7692 ) ;
#55167=ORIENTED_EDGE ( 'NONE', *, *, #56423, .T. ) ;
#55182=DIRECTION ( 'NONE',  ( 0.000000000000000000, -1.000000000000000000, 0.000000000000000000 ) ) ;
#55184=ORIENTED_EDGE ( 'NONE', *, *, #95508, .T. ) ;
#55186=VERTEX_POINT ( 'NONE', #99406 ) ;
#55195=CARTESIAN_POINT ( 'NONE',  ( 29.77147767949874790, 5.356774720514425603, 26.15915692125051706 ) ) ;
#55196=CARTESIAN_POINT ( 'NONE',  ( 22.81105451610979173, 4.772774720514425972, -18.46691820600746681 ) ) ;
#55202=LINE ( 'NONE', #393, #58794 ) ;
#55219=ADVANCED_FACE ( 'NONE', ( #53755 ), #36015, .T. ) ;
#55225=CARTESIAN_POINT ( 'NONE',  ( -20.77875734969026311, -6.143225279485574397, 29.49402280011862487 ) ) ;
#55228=CIRCLE ( 'NONE', #45507, 3.979149600822063704 ) ;
#55229=VERTEX_POINT ( 'NONE', #67477 ) ;
#55231=VECTOR ( 'NONE', #23889, 1000.000000000000000 ) ;
#55232=DIRECTION ( 'NONE',  ( -0.1875268396392987258, -0.000000000000000000, -0.9822594791677485837 ) ) ;
#55243=CARTESIAN_POINT ( 'NONE',  ( 14.43441819135927950, -5.965225279485592225, -28.36222020317712378 ) ) ;
#55246=FACE_OUTER_BOUND ( 'NONE', #81717, .T. ) ;
#55309=EDGE_CURVE ( 'NONE', #68317, #99683, #71481, .T. ) ;
#55325=CARTESIAN_POINT ( 'NONE',  ( 11.78947449592735275, 0.3587747205144256601, -28.08498176919931666 ) ) ;
#55334=DIRECTION ( 'NONE',  ( 0.000000000000000000, -1.000000000000000000, 0.000000000000000000 ) ) ;
#55351=CARTESIAN_POINT ( 'NONE',  ( -17.97250661212648026, -5.965225279485594001, -23.43622901028613015 ) ) ;
#55360=DIRECTION ( 'NONE',  ( -7.994117400814786717E-16, -0.000000000000000000, 1.000000000000000000 ) ) ;
#55367=DIRECTION ( 'NONE',  ( -1.000000000000000000, 0.000000000000000000, -7.994117400814786717E-16 ) ) ;
#55374=ORIENTED_EDGE ( 'NONE', *, *, #98468, .T. ) ;
#55382=CARTESIAN_POINT ( 'NONE',  ( 10.16119454606818984, 3.316774720514931829, -28.04611093432389524 ) ) ;
#55383=VECTOR ( 'NONE', #14135, 1000.000000000000227 ) ;
#55387=DIRECTION ( 'NONE',  ( 0.000000000000000000, 1.000000000000000000, 0.000000000000000000 ) ) ;
#55401=CARTESIAN_POINT ( 'NONE',  ( 26.73860345374794534, -1.477225279485574028, -1.352392034746782823 ) ) ;
#55402=DIRECTION ( 'NONE',  ( -1.000000000000000000, 0.000000000000000000, -0.000000000000000000 ) ) ;
#55403=CARTESIAN_POINT ( 'NONE',  ( 30.53060340732035982, 6.376774720514426953, 20.86760796525322093 ) ) ;
#55407=CARTESIAN_POINT ( 'NONE',  ( -29.49875734969025842, -5.965225279485572685, 15.62202280011862321 ) ) ;
#55414=CARTESIAN_POINT ( 'NONE',  ( 32.59332756141814258, 1.682774720514426114, -11.41404606144462797 ) ) ;
#55425=ORIENTED_EDGE ( 'NONE', *, *, #29941, .T. ) ;
#55477=DIRECTION ( 'NONE',  ( -0.000000000000000000, 1.000000000000000000, -0.000000000000000000 ) ) ;
#55492=FACE_OUTER_BOUND ( 'NONE', #47773, .T. ) ;
#55502=CIRCLE ( 'NONE', #7106, 1.325999999999990298 ) ;
#55515=B_SPLINE_CURVE_WITH_KNOTS ( 'NONE', 3,
 ( #48018, #100261, #8942, #70851, #9943, #71354 ),
 .UNSPECIFIED., .F., .F.,
 ( 4, 2, 4 ),
 ( 0.001468967764902712192, 0.004864447352129883453, 0.008259926939357054715 ),
 .UNSPECIFIED. ) ;
#55518=VERTEX_POINT ( 'NONE', #11556 ) ;
#55547=DIRECTION ( 'NONE',  ( 4.835261319396784738E-10, 0.000000000000000000, -1.000000000000000000 ) ) ;
#55557=VERTEX_POINT ( 'NONE', #96802 ) ;
#55559=DIRECTION ( 'NONE',  ( 0.1311553622875919756, 0.000000000000000000, 0.9913618264504692190 ) ) ;
#55565=DIRECTION ( 'NONE',  ( -0.9997753877537052247, 0.000000000000000000, 0.02119372647573814633 ) ) ;
#55568=ADVANCED_FACE ( 'NONE', ( #3965 ), #72479, .F. ) ;
#55569=AXIS2_PLACEMENT_3D ( 'NONE', #88204, #49158, #26796 ) ;
#55589=VECTOR ( 'NONE', #49093, 1000.000000000000000 ) ;
#55618=PLANE ( 'NONE',  #43315 ) ;
#55622=AXIS2_PLACEMENT_3D ( 'NONE', #32294, #8459, #77946 ) ;
#55627=DIRECTION ( 'NONE',  ( 0.000000000000000000, 0.000000000000000000, 1.000000000000000000 ) ) ;
#55638=CARTESIAN_POINT ( 'NONE',  ( 5.097264368846952998, -6.475225279485573360, -27.56135813788808164 ) ) ;
#55646=VECTOR ( 'NONE', #74479, 1000.000000000000000 ) ;
#55666=CARTESIAN_POINT ( 'NONE',  ( -2.872281323269014752, 4.293056017849825601, 1.999999999999999556 ) ) ;
#55713=CARTESIAN_POINT ( 'NONE',  ( -20.27875734969026311, -4.543225279485573864, 24.00402280011862288 ) ) ;
#55715=ORIENTED_EDGE ( 'NONE', *, *, #43205, .T. ) ;
#55716=CARTESIAN_POINT ( 'NONE',  ( -28.98875734969026396, 0.3587747205144265483, 2.362022800118626531 ) ) ;
#55726=VERTEX_POINT ( 'NONE', #85060 ) ;
#55728=ADVANCED_FACE ( 'NONE', ( #8943 ), #24657, .F. ) ;
#55769=CYLINDRICAL_SURFACE ( 'NONE', #9137, 91.74549126261076992 ) ;
#55775=DIRECTION ( 'NONE',  ( -0.6599726524652352877, 0.000000000000000000, 0.7512896232465892110 ) ) ;
#55781=CARTESIAN_POINT ( 'NONE',  ( 33.37790122608239329, 4.268345726061002487, -11.54778842029335806 ) ) ;
#55784=LINE ( 'NONE', #35805, #8975 ) ;
#55786=EDGE_CURVE ( 'NONE', #5789, #32299, #92173, .T. ) ;
#55787=B_SPLINE_CURVE_WITH_KNOTS ( 'NONE', 3,
 ( #43538, #11570, #42549, #90200 ),
 .UNSPECIFIED., .F., .F.,
 ( 4, 4 ),
 ( 0.000000000000000000, 0.0002088004239042353695 ),
 .UNSPECIFIED. ) ;
#55821=EDGE_CURVE ( 'NONE', #84008, #628, #9442, .T. ) ;
#55841=DIRECTION ( 'NONE',  ( 0.000000000000000000, -1.478457507934778393E-16, -1.000000000000000000 ) ) ;
#55843=ADVANCED_FACE ( 'NONE', ( #31785 ), #93672, .T. ) ;
#55846=EDGE_LOOP ( 'NONE', ( #74130, #2052, #10153, #13890 ) ) ;
#55852=ADVANCED_FACE ( 'NONE', ( #78442 ), #10951, .F. ) ;
#55865=EDGE_CURVE ( 'NONE', #16459, #22648, #34394, .T. ) ;
#55867=DIRECTION ( 'NONE',  ( 0.000000000000000000, -1.000000000000000000, 0.000000000000000000 ) ) ;
#55875=ORIENTED_EDGE ( 'NONE', *, *, #46789, .F. ) ;
#55879=LINE ( 'NONE', #86804, #92558 ) ;
#55884=DIRECTION ( 'NONE',  ( 0.000000000000000000, -1.478457507934778393E-16, -1.000000000000000000 ) ) ;
#55888=DIRECTION ( 'NONE',  ( -0.000000000000000000, -1.000000000000000000, 0.000000000000000000 ) ) ;
#55904=VECTOR ( 'NONE', #55061, 1000.000000000000000 ) ;
#55912=CARTESIAN_POINT ( 'NONE',  ( 29.73860345376319003, -1.477225279485574028, 19.84760796525321780 ) ) ;
#55913=FACE_OUTER_BOUND ( 'NONE', #62959, .T. ) ;
#55920=CARTESIAN_POINT ( 'NONE',  ( 31.69157588030356010, 3.540801019308528197, 29.47507166493026176 ) ) ;
#55922=CARTESIAN_POINT ( 'NONE',  ( 282.9764569301858046, -5.965225279485572685, 20.79159422840526616 ) ) ;
#55927=VECTOR ( 'NONE', #57018, 1000.000000000000000 ) ;
#55945=DIRECTION ( 'NONE',  ( 0.000000000000000000, 1.000000000000000000, 0.000000000000000000 ) ) ;
#55951=PLANE ( 'NONE',  #32307 ) ;
#55953=ORIENTED_EDGE ( 'NONE', *, *, #38850, .T. ) ;
#55958=CARTESIAN_POINT ( 'NONE',  ( -11.64875734969026233, 0.3587747205144265483, 31.02402280011862246 ) ) ;
#55976=CIRCLE ( 'NONE', #60827, 1.699999999999996625 ) ;
#55990=CARTESIAN_POINT ( 'NONE',  ( -20.77875734969026311, 3.316774720514426456, 27.45402280011862572 ) ) ;
#56004=EDGE_CURVE ( 'NONE', #76864, #11608, #94457, .T. ) ;
#56028=EDGE_CURVE ( 'NONE', #69852, #97596, #99162, .T. ) ;
#56042=EDGE_LOOP ( 'NONE', ( #2379, #9235, #69752, #71927 ) ) ;
#56043=DIRECTION ( 'NONE',  ( -0.6392559695863496705, -6.845827386180411947E-16, -0.7689940216596069522 ) ) ;
#56054=CARTESIAN_POINT ( 'NONE',  ( 0.000000000000000000, 1.826774720514426464, 6.000000000000000888 ) ) ;
#56067=LINE ( 'NONE', #3289, #23707 ) ;
#56072=LINE ( 'NONE', #87004, #54989 ) ;
#56073=PLANE ( 'NONE',  #58871 ) ;
#56080=LINE ( 'NONE', #10896, #22782 ) ;
#56085=EDGE_CURVE ( 'NONE', #2131, #43884, #18238, .T. ) ;
#56108=CYLINDRICAL_SURFACE ( 'NONE', #63579, 1.325999999999990298 ) ;
#56121=CARTESIAN_POINT ( 'NONE',  ( 31.74473449900405697, 4.976825198871215328, -4.259190951192157293 ) ) ;
#56145=VECTOR ( 'NONE', #51758, 1000.000000000000000 ) ;
#56162=CARTESIAN_POINT ( 'NONE',  ( 30.93860345374796594, -5.965225279485572685, 28.07639619989136293 ) ) ;
#56165=CIRCLE ( 'NONE', #2710, 7.652410033082763796 ) ;
#56169=DIRECTION ( 'NONE',  ( -2.682707457723910108E-15, 0.000000000000000000, -1.000000000000000000 ) ) ;
#56188=ORIENTED_EDGE ( 'NONE', *, *, #40627, .T. ) ;
#56194=CARTESIAN_POINT ( 'NONE',  ( 22.02124265030973760, 3.456774720514426136, 16.20402280011862217 ) ) ;
#56200=CARTESIAN_POINT ( 'NONE',  ( 32.73857899460460175, 1.684774720514424118, -13.20677013500359820 ) ) ;
#56217=DIRECTION ( 'NONE',  ( 0.000000000000000000, 1.000000000000000000, 0.000000000000000000 ) ) ;
#56223=VECTOR ( 'NONE', #89383, 1000.000000000000114 ) ;
#56226=DIRECTION ( 'NONE',  ( -0.000000000000000000, -0.7071067811865513475, 0.7071067811865437980 ) ) ;
#56229=EDGE_CURVE ( 'NONE', #57678, #85295, #71230, .T. ) ;
#56250=DIRECTION ( 'NONE',  ( 0.000000000000000000, -1.000000000000000000, 0.000000000000000000 ) ) ;
#56260=VECTOR ( 'NONE', #63571, 1000.000000000000000 ) ;
#56264=CARTESIAN_POINT ( 'NONE',  ( 15.32643653063177958, 2.682774720514426559, -27.14485409495429380 ) ) ;
#56268=PLANE ( 'NONE',  #37507 ) ;
#56285=CARTESIAN_POINT ( 'NONE',  ( 33.61752870511805469, 3.456547803086276183, -11.38123630260511199 ) ) ;
#56301=CIRCLE ( 'NONE', #1232, 2.040000000000000036 ) ;
#56320=FACE_OUTER_BOUND ( 'NONE', #58315, .T. ) ;
#56326=AXIS2_PLACEMENT_3D ( 'NONE', #85493, #45954, #55565 ) ;
#56335=CARTESIAN_POINT ( 'NONE',  ( 11.03981094302168842, 0.3587747205144256601, -28.06140118199223465 ) ) ;
#56374=CARTESIAN_POINT ( 'NONE',  ( 30.53060340732036337, 5.297812262124996785, 1.539714685317421505 ) ) ;
#56381=CARTESIAN_POINT ( 'NONE',  ( 6.646494591716556322, 3.316774720514426900, -28.33840132637671161 ) ) ;
#56385=LINE ( 'NONE', #87307, #67479 ) ;
#56392=LINE ( 'NONE', #72605, #10691 ) ;
#56398=CARTESIAN_POINT ( 'NONE',  ( 14.02639803017889086, 6.376774720514426065, -25.20535965011783119 ) ) ;
#56399=AXIS2_PLACEMENT_3D ( 'NONE', #67554, #42726, #37087 ) ;
#56415=CARTESIAN_POINT ( 'NONE',  ( 0.000000000000000000, 1.682774720514426114, -1.352392034746782823 ) ) ;
#56420=CARTESIAN_POINT ( 'NONE',  ( 14.43441819135533777, 3.316774720514426900, -28.36222020317639192 ) ) ;
#56423=EDGE_CURVE ( 'NONE', #9985, #15254, #93817, .T. ) ;
#56438=VERTEX_POINT ( 'NONE', #32423 ) ;
#56464=EDGE_LOOP ( 'NONE', ( #10730, #54369, #97275, #12646 ) ) ;
#56469=FACE_OUTER_BOUND ( 'NONE', #47107, .T. ) ;
#56473=FACE_BOUND ( 'NONE', #20868, .T. ) ;
#56493=CARTESIAN_POINT ( 'NONE',  ( 29.73860345376319714, 4.772774720514425972, -4.021250162519585558 ) ) ;
#56497=ORIENTED_EDGE ( 'NONE', *, *, #59124, .F. ) ;
#56507=ORIENTED_EDGE ( 'NONE', *, *, #63892, .T. ) ;
#56519=DIRECTION ( 'NONE',  ( -0.000000000000000000, -1.000000000000000000, -0.000000000000000000 ) ) ;
#56524=VECTOR ( 'NONE', #17349, 1000.000000000000000 ) ;
#56535=LINE ( 'NONE', #9838, #70546 ) ;
#56553=DIRECTION ( 'NONE',  ( 0.7071067811865476838, 0.000000000000000000, -0.7071067811865474617 ) ) ;
#56558=CARTESIAN_POINT ( 'NONE',  ( -28.98875734969026396, -5.965225279485572685, 2.362022800118626531 ) ) ;
#56602=CARTESIAN_POINT ( 'NONE',  ( -28.98875734969026396, 0.3587747205144265483, 10.11402280011862587 ) ) ;
#56612=EDGE_CURVE ( 'NONE', #5380, #48796, #12576, .T. ) ;
#56624=DIRECTION ( 'NONE',  ( -1.000000000000000000, 0.000000000000000000, 0.000000000000000000 ) ) ;
#56627=FACE_OUTER_BOUND ( 'NONE', #52927, .T. ) ;
#56649=CARTESIAN_POINT ( 'NONE',  ( -24.55517127435777525, 0.3587747205143967943, -15.44180958690143157 ) ) ;
#56655=DIRECTION ( 'NONE',  ( 0.000000000000000000, 1.000000000000000000, 0.000000000000000000 ) ) ;
#56687=EDGE_CURVE ( 'NONE', #43471, #14228, #65909, .T. ) ;
#56731=AXIS2_PLACEMENT_3D ( 'NONE', #32390, #56250, #16157 ) ;
#56751=AXIS2_PLACEMENT_3D ( 'NONE', #30960, #85244, #40591 ) ;
#56778=FACE_OUTER_BOUND ( 'NONE', #23436, .T. ) ;
#56781=ORIENTED_EDGE ( 'NONE', *, *, #69201, .T. ) ;
#56790=ORIENTED_EDGE ( 'NONE', *, *, #20668, .T. ) ;
#56810=VERTEX_POINT ( 'NONE', #82589 ) ;
#56814=ORIENTED_EDGE ( 'NONE', *, *, #78039, .F. ) ;
#56817=AXIS2_PLACEMENT_3D ( 'NONE', #96752, #27251, #89147 ) ;
#56822=AXIS2_PLACEMENT_3D ( 'NONE', #11973, #42941, #73875 ) ;
#56844=CARTESIAN_POINT ( 'NONE',  ( 30.53060340732035982, 0.6647747205144264315, 20.86760796525322093 ) ) ;
#56845=LINE ( 'NONE', #74049, #50761 ) ;
#56854=EDGE_LOOP ( 'NONE', ( #32821, #51713, #98427, #37946, #6383, #4969, #15912, #90748 ) ) ;
#56864=ADVANCED_FACE ( 'NONE', ( #46037 ), #29798, .F. ) ;
#56869=DIRECTION ( 'NONE',  ( 1.334402673828313339E-16, -0.000000000000000000, -1.000000000000000000 ) ) ;
#56872=CARTESIAN_POINT ( 'NONE',  ( 30.53060340732036337, 5.329285123471892760, 3.289350009555732868 ) ) ;
#56884=DIRECTION ( 'NONE',  ( 0.000000000000000000, 0.000000000000000000, 1.000000000000000000 ) ) ;
#56887=DIRECTION ( 'NONE',  ( 0.000000000000000000, -1.000000000000000000, 0.000000000000000000 ) ) ;
#56897=AXIS2_PLACEMENT_3D ( 'NONE', #57068, #25597, #89001 ) ;
#56899=CARTESIAN_POINT ( 'NONE',  ( 13.25751441563444999, 6.376774720514426065, -25.10777837594209672 ) ) ;
#56915=EDGE_CURVE ( 'NONE', #17738, #97857, #59260, .T. ) ;
#56922=ORIENTED_EDGE ( 'NONE', *, *, #14594, .T. ) ;
#56927=ORIENTED_EDGE ( 'NONE', *, *, #28440, .F. ) ;
#56965=DIRECTION ( 'NONE',  ( -0.000000000000000000, -0.000000000000000000, -1.000000000000000000 ) ) ;
#56968=DIRECTION ( 'NONE',  ( 0.000000000000000000, -1.000000000000000000, 0.000000000000000000 ) ) ;
#56971=DIRECTION ( 'NONE',  ( 0.000000000000000000, -0.000000000000000000, -1.000000000000000000 ) ) ;
#56976=CARTESIAN_POINT ( 'NONE',  ( 25.40542801349638680, 4.685157528325373910, -10.80549495980642583 ) ) ;
#56980=EDGE_LOOP ( 'NONE', ( #45161, #6592 ) ) ;
#56987=FACE_OUTER_BOUND ( 'NONE', #38736, .T. ) ;
#56994=DIRECTION ( 'NONE',  ( 0.000000000000000000, 0.000000000000000000, -1.000000000000000000 ) ) ;
#56997=ORIENTED_EDGE ( 'NONE', *, *, #16315, .F. ) ;
#57018=DIRECTION ( 'NONE',  ( -0.000000000000000000, -1.000000000000000000, -0.000000000000000000 ) ) ;
#57023=VERTEX_POINT ( 'NONE', #57161 ) ;
#57033=CARTESIAN_POINT ( 'NONE',  ( 31.59111626279633711, 6.376774720514426953, 16.27760796525321751 ) ) ;
#57041=CARTESIAN_POINT ( 'NONE',  ( 14.76093561896379214, -6.475225279485573360, -26.55548769130089681 ) ) ;
#57060=DIRECTION ( 'NONE',  ( 0.000000000000000000, 1.000000000000000000, 0.000000000000000000 ) ) ;
#57067=DIRECTION ( 'NONE',  ( 0.000000000000000000, -1.000000000000000000, 0.000000000000000000 ) ) ;
#57068=CARTESIAN_POINT ( 'NONE',  ( 14.76093561896378148, 3.316774720514426456, -26.55548769130088971 ) ) ;
#57072=FACE_OUTER_BOUND ( 'NONE', #60417, .T. ) ;
#57087=ORIENTED_EDGE ( 'NONE', *, *, #37970, .T. ) ;
#57102=CARTESIAN_POINT ( 'NONE',  ( -25.92875734969025814, 5.356774720514425603, 26.43402280011862615 ) ) ;
#57103=FACE_OUTER_BOUND ( 'NONE', #26811, .T. ) ;
#57107=VECTOR ( 'NONE', #14060, 1000.000000000000000 ) ;
#57108=ORIENTED_EDGE ( 'NONE', *, *, #40335, .T. ) ;
#57113=DIRECTION ( 'NONE',  ( -0.000000000000000000, -1.000000000000000000, -0.000000000000000000 ) ) ;
#57118=FACE_OUTER_BOUND ( 'NONE', #5765, .T. ) ;
#57121=ADVANCED_FACE ( 'NONE', ( #87592 ), #49542, .T. ) ;
#57123=CARTESIAN_POINT ( 'NONE',  ( 26.25551457520356635, 500000.0000000000582, -10.59759736550661913 ) ) ;
#57140=DIRECTION ( 'NONE',  ( -0.7640209514960704107, 0.000000000000000000, 0.6451914333552789538 ) ) ;
#57142=CARTESIAN_POINT ( 'NONE',  ( 5.085443162053245203, 3.316774720514426456, -27.56355752155217331 ) ) ;
#57147=EDGE_CURVE ( 'NONE', #92122, #92240, #95201, .T. ) ;
#57149=EDGE_CURVE ( 'NONE', #59834, #83063, #52912, .T. ) ;
#57150=DIRECTION ( 'NONE',  ( 0.000000000000000000, 0.000000000000000000, 1.000000000000000000 ) ) ;
#57161=CARTESIAN_POINT ( 'NONE',  ( 28.30015606816038698, 1.682774720514426114, -13.13501953239208575 ) ) ;
#57163=ORIENTED_EDGE ( 'NONE', *, *, #52409, .T. ) ;
#57168=ADVANCED_FACE ( 'NONE', ( #98681 ), #17357, .F. ) ;
#57171=ORIENTED_EDGE ( 'NONE', *, *, #8595, .F. ) ;
#57172=CIRCLE ( 'NONE', #39323, 4.300000000000000711 ) ;
#57182=DIRECTION ( 'NONE',  ( 0.000000000000000000, -0.000000000000000000, -1.000000000000000000 ) ) ;
#57184=CARTESIAN_POINT ( 'NONE',  ( 31.74473449900405697, 4.976825198871215328, -4.259190951192157293 ) ) ;
#57187=AXIS2_PLACEMENT_3D ( 'NONE', #64898, #88210, #18678 ) ;
#57196=AXIS2_PLACEMENT_3D ( 'NONE', #11034, #34374, #1428 ) ;
#57223=DIRECTION ( 'NONE',  ( 1.000000000000000000, -0.000000000000000000, -0.000000000000000000 ) ) ;
#57239=EDGE_CURVE ( 'NONE', #52986, #13454, #48077, .T. ) ;
#57244=CARTESIAN_POINT ( 'NONE',  ( -19.80875734969026425, 0.3587747205144265483, 31.02402280011862246 ) ) ;
#57246=EDGE_CURVE ( 'NONE', #396, #86154, #13445, .T. ) ;
#57260=LINE ( 'NONE', #18661, #73539 ) ;
#57263=VECTOR ( 'NONE', #52490, 1000.000000000000000 ) ;
#57269=VECTOR ( 'NONE', #8009, 1000.000000000000000 ) ;
#57272=ORIENTED_EDGE ( 'NONE', *, *, #39819, .T. ) ;
#57274=ADVANCED_FACE ( 'NONE', ( #72198 ), #72698, .F. ) ;
#57279=CYLINDRICAL_SURFACE ( 'NONE', #57187, 1.836000000000000743 ) ;
#57305=EDGE_CURVE ( 'NONE', #52175, #22769, #7574, .T. ) ;
#57318=EDGE_LOOP ( 'NONE', ( #49077, #45538, #47812, #93081 ) ) ;
#57329=VECTOR ( 'NONE', #30898, 1000.000000000000000 ) ;
#57330=ORIENTED_EDGE ( 'NONE', *, *, #52113, .F. ) ;
#57368=DIRECTION ( 'NONE',  ( 0.000000000000000000, 1.000000000000000000, -0.000000000000000000 ) ) ;
#57370=EDGE_CURVE ( 'NONE', #61510, #84489, #42753, .T. ) ;
#57373=ADVANCED_FACE ( 'NONE', ( #80803 ), #81955, .T. ) ;
#57380=CARTESIAN_POINT ( 'NONE',  ( 0.000000000000000000, -6.943225279485572443, -1.149999999999999911 ) ) ;
#57384=ORIENTED_EDGE ( 'NONE', *, *, #9467, .F. ) ;
#57391=CARTESIAN_POINT ( 'NONE',  ( 6.303825520940272042, -5.965225279485572685, -28.39893233836329856 ) ) ;
#57412=CARTESIAN_POINT ( 'NONE',  ( 27.86270917940689174, -5.965225279485572685, 29.49402280011862487 ) ) ;
#57426=VERTEX_POINT ( 'NONE', #45730 ) ;
#57433=CARTESIAN_POINT ( 'NONE',  ( 14.83533542161589480, 3.438288638725202517, -27.37882296607460120 ) ) ;
#57440=ORIENTED_EDGE ( 'NONE', *, *, #1627, .T. ) ;
#57453=ORIENTED_EDGE ( 'NONE', *, *, #83019, .F. ) ;
#57458=LINE ( 'NONE', #81271, #64308 ) ;
#57479=CARTESIAN_POINT ( 'NONE',  ( 25.07255740347941853, 5.130262834649095716, -9.008209484467815997 ) ) ;
#57480=CARTESIAN_POINT ( 'NONE',  ( -20.27875734969026311, 3.456774720514426136, 25.15402280011862146 ) ) ;
#57483=VERTEX_POINT ( 'NONE', #43741 ) ;
#57486=DIRECTION ( 'NONE',  ( 4.089440751051245812E-15, -1.000000000000000000, -1.042451643221144600E-15 ) ) ;
#57490=DIRECTION ( 'NONE',  ( 0.000000000000000000, 0.000000000000000000, -1.000000000000000000 ) ) ;
#57502=VECTOR ( 'NONE', #82635, 1000.000000000000000 ) ;
#57506=DIRECTION ( 'NONE',  ( 0.000000000000000000, -0.000000000000000000, -1.000000000000000000 ) ) ;
#57513=VERTEX_POINT ( 'NONE', #76161 ) ;
#57526=EDGE_CURVE ( 'NONE', #61907, #32410, #38107, .T. ) ;
#57545=ORIENTED_EDGE ( 'NONE', *, *, #98444, .F. ) ;
#57550=CARTESIAN_POINT ( 'NONE',  ( -41.32836283488544638, 4.132774720514426292, 39.26872235229541985 ) ) ;
#57553=AXIS2_PLACEMENT_3D ( 'NONE', #19699, #44051, #20699 ) ;
#57556=CARTESIAN_POINT ( 'NONE',  ( 10.44337217408228291, 4.530443463488840194, -26.67771320976549987 ) ) ;
#57558=CARTESIAN_POINT ( 'NONE',  ( -28.98875734969026396, 0.3587747205144265483, 2.362022800118626531 ) ) ;
#57567=VECTOR ( 'NONE', #90637, 1000.000000000000000 ) ;
#57571=DIRECTION ( 'NONE',  ( 1.000000000000000000, -0.000000000000000000, -0.000000000000000000 ) ) ;
#57572=CARTESIAN_POINT ( 'NONE',  ( -2.768609665556983845, -5.965225279485594001, -29.41086200512614823 ) ) ;
#57578=DIRECTION ( 'NONE',  ( -0.000000000000000000, -1.000000000000000000, 0.000000000000000000 ) ) ;
#57584=VERTEX_POINT ( 'NONE', #66963 ) ;
#57599=DIRECTION ( 'NONE',  ( 0.000000000000000000, 0.000000000000000000, -1.000000000000000000 ) ) ;
#57605=VECTOR ( 'NONE', #6088, 1000.000000000000000 ) ;
#57612=DIRECTION ( 'NONE',  ( 0.000000000000000000, -1.000000000000000000, 0.000000000000000000 ) ) ;
#57618=CARTESIAN_POINT ( 'NONE',  ( 7.227401621481964966, 5.356774720515138810, -27.22638491171618824 ) ) ;
#57622=DIRECTION ( 'NONE',  ( -0.000000000000000000, -1.000000000000000000, -0.000000000000000000 ) ) ;
#57636=CARTESIAN_POINT ( 'NONE',  ( 13.91401389203221406, 0.3587747205144265483, 158.0376437107427137 ) ) ;
#57645=VECTOR ( 'NONE', #46701, 1000.000000000000000 ) ;
#57675=ORIENTED_EDGE ( 'NONE', *, *, #30567, .F. ) ;
#57678=VERTEX_POINT ( 'NONE', #80173 ) ;
#57682=ORIENTED_EDGE ( 'NONE', *, *, #37906, .T. ) ;
#57699=EDGE_CURVE ( 'NONE', #7760, #95350, #17129, .T. ) ;
#57703=DIRECTION ( 'NONE',  ( 0.000000000000000000, 1.000000000000000000, -0.000000000000000000 ) ) ;
#57705=VECTOR ( 'NONE', #97822, 1000.000000000000000 ) ;
#57710=AXIS2_PLACEMENT_3D ( 'NONE', #23740, #47099, #68922 ) ;
#57723=VERTEX_POINT ( 'NONE', #60845 ) ;
#57725=FACE_OUTER_BOUND ( 'NONE', #85890, .T. ) ;
#57728=ADVANCED_FACE ( 'NONE', ( #76036, #29373 ), #60350, .T. ) ;
#57748=DIRECTION ( 'NONE',  ( 0.000000000000000000, -1.000000000000000000, 0.000000000000000000 ) ) ;
#57781=CARTESIAN_POINT ( 'NONE',  ( -24.90875734969025501, 3.316774720514426456, 27.45402280011862572 ) ) ;
#57800=ORIENTED_EDGE ( 'NONE', *, *, #32131, .T. ) ;
#57808=VERTEX_POINT ( 'NONE', #90040 ) ;
#57814=CARTESIAN_POINT ( 'NONE',  ( 32.06540688909007741, -6.475225279485573360, -12.44045471929204716 ) ) ;
#57821=CIRCLE ( 'NONE', #10861, 129.7684398600581517 ) ;
#57827=FACE_OUTER_BOUND ( 'NONE', #88701, .T. ) ;
#57840=CARTESIAN_POINT ( 'NONE',  ( 33.13288845015618023, -5.965225279485572685, -0.1650522222209214185 ) ) ;
#57845=ORIENTED_EDGE ( 'NONE', *, *, #77029, .F. ) ;
#57846=DIRECTION ( 'NONE',  ( -0.000000000000000000, -1.000000000000000000, -0.000000000000000000 ) ) ;
#57848=EDGE_CURVE ( 'NONE', #10813, #18192, #80289, .T. ) ;
#57855=CARTESIAN_POINT ( 'NONE',  ( 30.93860345374796594, -6.475225279485573360, 19.84760796525321780 ) ) ;
#57862=ORIENTED_EDGE ( 'NONE', *, *, #4304, .T. ) ;
#57866=AXIS2_PLACEMENT_3D ( 'NONE', #73686, #4182, #22864 ) ;
#57902=CARTESIAN_POINT ( 'NONE',  ( 31.61406883670153789, 4.508386143373845023, 26.44289287685778334 ) ) ;
#57907=DIRECTION ( 'NONE',  ( -1.000000000000000000, 0.000000000000000000, 0.000000000000000000 ) ) ;
#57913=PLANE ( 'NONE',  #25373 ) ;
#57916=CARTESIAN_POINT ( 'NONE',  ( 14.58759567797699574, 3.520387117721317072, -28.38990266974735732 ) ) ;
#57928=ORIENTED_EDGE ( 'NONE', *, *, #95468, .F. ) ;
#57929=DIRECTION ( 'NONE',  ( 0.000000000000000000, 0.000000000000000000, -1.000000000000000000 ) ) ;
#57930=EDGE_CURVE ( 'NONE', #43884, #2131, #67336, .T. ) ;
#57945=DIRECTION ( 'NONE',  ( 0.000000000000000000, 1.000000000000000000, 0.000000000000000000 ) ) ;
#57952=CIRCLE ( 'NONE', #9318, 3.500000000000000000 ) ;
#57955=LINE ( 'NONE', #72669, #56223 ) ;
#57961=ORIENTED_EDGE ( 'NONE', *, *, #66764, .T. ) ;
#57965=ORIENTED_EDGE ( 'NONE', *, *, #56687, .F. ) ;
#57968=CARTESIAN_POINT ( 'NONE',  ( 0.000000000000000000, 1.682774720514426114, -1.352392034746782823 ) ) ;
#57976=ORIENTED_EDGE ( 'NONE', *, *, #74613, .F. ) ;
#57981=ORIENTED_EDGE ( 'NONE', *, *, #97067, .T. ) ;
#57999=B_SPLINE_CURVE_WITH_KNOTS ( 'NONE', 3,
 ( #48433, #26593, #97588, #41316, #42335, #87485, #73756, #80375, #57556, #19464 ),
 .UNSPECIFIED., .F., .F.,
 ( 4, 2, 2, 2, 4 ),
 ( 0.000000000000000000, 0.08666671201630674060, 0.1733334240326134812, 0.3466668480652273510, 0.6933336961304540358 ),
 .UNSPECIFIED. ) ;
#58026=EDGE_CURVE ( 'NONE', #17009, #60699, #52997, .T. ) ;
#58032=PLANE ( 'NONE',  #20980 ) ;
#58053=FACE_OUTER_BOUND ( 'NONE', #23958, .T. ) ;
#58055=ADVANCED_FACE ( 'NONE', ( #92897 ), #84788, .T. ) ;
#58071=ORIENTED_EDGE ( 'NONE', *, *, #7092, .F. ) ;
#58072=DIRECTION ( 'NONE',  ( 0.000000000000000000, 0.000000000000000000, 1.000000000000000000 ) ) ;
#58074=DIRECTION ( 'NONE',  ( 0.000000000000000000, -1.000000000000000000, 0.000000000000000000 ) ) ;
#58077=CARTESIAN_POINT ( 'NONE',  ( 25.05730599792488533, 1.684774720501991174, -18.59674224247030239 ) ) ;
#58111=CARTESIAN_POINT ( 'NONE',  ( 31.27206728860909024, 4.132774720514318822, -3.930752063305056332 ) ) ;
#58117=VERTEX_POINT ( 'NONE', #48755 ) ;
#58120=CARTESIAN_POINT ( 'NONE',  ( 9.214646252596866205, 5.356774720515496746, -27.04520690447069597 ) ) ;
#58130=CARTESIAN_POINT ( 'NONE',  ( -4.926336369345162502, 0.3587747205143967943, -28.61095484066305161 ) ) ;
#58139=DIRECTION ( 'NONE',  ( -0.000000000000000000, -1.000000000000000000, -0.000000000000000000 ) ) ;
#58141=FACE_OUTER_BOUND ( 'NONE', #88125, .T. ) ;
#58146=VECTOR ( 'NONE', #42195, 1000.000000000000000 ) ;
#58148=DIRECTION ( 'NONE',  ( 0.000000000000000000, 1.000000000000000000, 0.000000000000000000 ) ) ;
#58158=ORIENTED_EDGE ( 'NONE', *, *, #23821, .T. ) ;
#58159=VERTEX_POINT ( 'NONE', #79682 ) ;
#58162=DIRECTION ( 'NONE',  ( -1.000000000000000000, 0.000000000000000000, 0.000000000000000000 ) ) ;
#58172=CARTESIAN_POINT ( 'NONE',  ( -17.97250661212648026, 0.3587747205144057872, -23.43622901028613725 ) ) ;
#58183=CARTESIAN_POINT ( 'NONE',  ( -20.27875734969026311, -6.143225279485574397, 24.00402280011862288 ) ) ;
#58209=CARTESIAN_POINT ( 'NONE',  ( 9.566520649354789185, 3.316774720514426011, -27.03026789950428110 ) ) ;
#58222=B_SPLINE_CURVE_WITH_KNOTS ( 'NONE', 3,
 ( #45639, #37522, #15680, #8069 ),
 .UNSPECIFIED., .F., .F.,
 ( 4, 4 ),
 ( 0.000000000000000000, 1.000000000000000000 ),
 .UNSPECIFIED. ) ;
#58230=CARTESIAN_POINT ( 'NONE',  ( 32.69168087260868560, 4.943943141208723802, -11.74984035242545133 ) ) ;
#58245=EDGE_CURVE ( 'NONE', #35739, #17845, #96418, .T. ) ;
#58247=DIRECTION ( 'NONE',  ( 0.000000000000000000, 0.000000000000000000, 1.000000000000000000 ) ) ;
#58254=ORIENTED_EDGE ( 'NONE', *, *, #28440, .T. ) ;
#58255=CARTESIAN_POINT ( 'NONE',  ( 29.73839433968188573, 4.772784452553388235, -4.021546701937777080 ) ) ;
#58271=DIRECTION ( 'NONE',  ( 1.955152872784845154E-15, -1.000000000000000000, -3.740001113483016365E-15 ) ) ;
#58275=LINE ( 'NONE', #59772, #42854 ) ;
#58281=LINE ( 'NONE', #97817, #17204 ) ;
#58300=ORIENTED_EDGE ( 'NONE', *, *, #63852, .T. ) ;
#58307=DIRECTION ( 'NONE',  ( -0.9994733861282923959, 0.000000000000000000, -0.03244919754393515293 ) ) ;
#58315=EDGE_LOOP ( 'NONE', ( #7180, #94261, #16123, #8336, #89326, #52791, #1932, #42632 ) ) ;
#58322=DIRECTION ( 'NONE',  ( 0.1489078231574191002, 0.000000000000000000, -0.9888510809027407644 ) ) ;
#58323=VECTOR ( 'NONE', #10367, 1000.000000000000000 ) ;
#58337=ORIENTED_EDGE ( 'NONE', *, *, #70205, .T. ) ;
#58340=CIRCLE ( 'NONE', #74545, 251.4258649670780699 ) ;
#58369=PLANE ( 'NONE',  #45802 ) ;
#58382=EDGE_CURVE ( 'NONE', #31584, #37593, #92782, .T. ) ;
#58386=LINE ( 'NONE', #28914, #28631 ) ;
#58397=CARTESIAN_POINT ( 'NONE',  ( 31.62974406627585466, 4.069828902950619387, 27.10097837741100335 ) ) ;
#58407=CARTESIAN_POINT ( 'NONE',  ( 33.96422015159436114, -5.965225279485572685, -7.233236000911337449 ) ) ;
#58408=CARTESIAN_POINT ( 'NONE',  ( 22.81105451610979173, -1.475225279485572916, -18.46691820600746681 ) ) ;
#58411=CARTESIAN_POINT ( 'NONE',  ( 30.53060340732035982, -1.477225279485574028, 19.84760796525321780 ) ) ;
#58412=EDGE_CURVE ( 'NONE', #39929, #9188, #92288, .T. ) ;
#58415=CARTESIAN_POINT ( 'NONE',  ( 15.50761710536933080, 3.593805972274664029, -28.23039328495952915 ) ) ;
#58436=DIRECTION ( 'NONE',  ( 0.000000000000000000, 0.000000000000000000, -1.000000000000000000 ) ) ;
#58446=ORIENTED_EDGE ( 'NONE', *, *, #1575, .T. ) ;
#58453=ORIENTED_EDGE ( 'NONE', *, *, #16946, .T. ) ;
#58457=ORIENTED_EDGE ( 'NONE', *, *, #33555, .T. ) ;
#58471=ORIENTED_EDGE ( 'NONE', *, *, #93792, .F. ) ;
#58479=AXIS2_PLACEMENT_3D ( 'NONE', #9869, #1766, #95609 ) ;
#58480=DIRECTION ( 'NONE',  ( 0.000000000000000000, -0.000000000000000000, 1.000000000000000000 ) ) ;
#58483=CARTESIAN_POINT ( 'NONE',  ( -20.27875734969026311, -4.543225279485573864, 24.00402280011862288 ) ) ;
#58506=ORIENTED_EDGE ( 'NONE', *, *, #49550, .T. ) ;
#58520=ADVANCED_FACE ( 'NONE', ( #2453 ), #9055, .F. ) ;
#58524=CARTESIAN_POINT ( 'NONE',  ( -4.568292318365942073, -5.965225279485572685, 30.06720597538392425 ) ) ;
#58531=CARTESIAN_POINT ( 'NONE',  ( 30.93860345374796594, 0.6647747205144267646, 23.11160796525322070 ) ) ;
#58537=VECTOR ( 'NONE', #48011, 1000.000000000000000 ) ;
#58557=ORIENTED_EDGE ( 'NONE', *, *, #83561, .T. ) ;
#58562=CARTESIAN_POINT ( 'NONE',  ( 15.14080536460164694, 3.622774720514426949, -26.62908960815038384 ) ) ;
#58566=CARTESIAN_POINT ( 'NONE',  ( 31.48454476783385658, 4.132774720514426292, -1.134026763942596494 ) ) ;
#58583=ORIENTED_EDGE ( 'NONE', *, *, #37996, .F. ) ;
#58597=EDGE_CURVE ( 'NONE', #654, #42693, #48132, .T. ) ;
#58610=ADVANCED_FACE ( 'NONE', ( #46007 ), #84550, .F. ) ;
#58628=LINE ( 'NONE', #80460, #61860 ) ;
#58645=EDGE_CURVE ( 'NONE', #95734, #12577, #23644, .T. ) ;
#58683=VERTEX_POINT ( 'NONE', #86054 ) ;
#58715=CARTESIAN_POINT ( 'NONE',  ( 32.85081302853803464, 3.622774720514426949, -13.10817780685209577 ) ) ;
#58720=CARTESIAN_POINT ( 'NONE',  ( 30.57287095715005520, -6.475225279485573360, 25.41160796525322141 ) ) ;
#58726=AXIS2_PLACEMENT_3D ( 'NONE', #46509, #8445, #77438 ) ;
#58727=EDGE_CURVE ( 'NONE', #55726, #69852, #38875, .T. ) ;
#58756=LINE ( 'NONE', #65896, #71641 ) ;
#58762=DIRECTION ( 'NONE',  ( -0.7512896232465786639, 0.000000000000000000, -0.6599726524652470561 ) ) ;
#58763=AXIS2_PLACEMENT_3D ( 'NONE', #54951, #92988, #70165 ) ;
#58764=B_SPLINE_CURVE_WITH_KNOTS ( 'NONE', 3,
 ( #3393, #94211, #71394, #17596, #65305, #26211, #40443, #95722, #2891, #57184 ),
 .UNSPECIFIED., .F., .F.,
 ( 4, 2, 2, 2, 4 ),
 ( -1.423960876792978737E-05, 0.0005136504108877040049, 0.001041540430543337831, 0.001569430450198971549, 0.002097320469854605483 ),
 .UNSPECIFIED. ) ;
#58788=ORIENTED_EDGE ( 'NONE', *, *, #60229, .F. ) ;
#58794=VECTOR ( 'NONE', #53699, 1000.000000000000000 ) ;
#58826=PLANE ( 'NONE',  #63740 ) ;
#58827=ORIENTED_EDGE ( 'NONE', *, *, #23308, .F. ) ;
#58831=DIRECTION ( 'NONE',  ( 1.955152872784845154E-15, -1.000000000000000000, -3.740001113483016365E-15 ) ) ;
#58834=DIRECTION ( 'NONE',  ( -2.135527794058834642E-14, 0.000000000000000000, -1.000000000000000000 ) ) ;
#58837=DIRECTION ( 'NONE',  ( -1.000000000000000000, 0.000000000000000000, -7.994117400814786717E-16 ) ) ;
#58839=DIRECTION ( 'NONE',  ( 0.000000000000000000, 0.000000000000000000, -1.000000000000000000 ) ) ;
#58848=DIRECTION ( 'NONE',  ( 0.000000000000000000, -1.000000000000000000, 0.000000000000000000 ) ) ;
#58855=DIRECTION ( 'NONE',  ( 0.000000000000000000, 0.000000000000000000, -1.000000000000000000 ) ) ;
#58858=EDGE_CURVE ( 'NONE', #7917, #51194, #89049, .T. ) ;
#58869=CARTESIAN_POINT ( 'NONE',  ( -11.64875734969026233, -5.965225279485572685, 31.02402280011862246 ) ) ;
#58871=AXIS2_PLACEMENT_3D ( 'NONE', #95122, #10888, #25611 ) ;
#58880=ORIENTED_EDGE ( 'NONE', *, *, #12883, .T. ) ;
#58894=VECTOR ( 'NONE', #91197, 1000.000000000000000 ) ;
#58897=CARTESIAN_POINT ( 'NONE',  ( 20.13489193910601216, 1.682774720514426114, -22.92085183005151450 ) ) ;
#58906=VECTOR ( 'NONE', #24010, 1000.000000000000000 ) ;
#58907=VERTEX_POINT ( 'NONE', #88067 ) ;
#58909=DIRECTION ( 'NONE',  ( -0.000000000000000000, -1.000000000000000000, 0.000000000000000000 ) ) ;
#58928=CARTESIAN_POINT ( 'NONE',  ( -27.25988310792305214, -5.965225279485572685, 30.32664379231667695 ) ) ;
#58933=ORIENTED_EDGE ( 'NONE', *, *, #81386, .T. ) ;
#58945=DIRECTION ( 'NONE',  ( -0.000000000000000000, 0.000000000000000000, 1.000000000000000000 ) ) ;
#58950=ORIENTED_EDGE ( 'NONE', *, *, #96456, .T. ) ;
#58961=CARTESIAN_POINT ( 'NONE',  ( 22.81105451610979173, -1.475225279485572916, -18.46691820600746681 ) ) ;
#58970=ORIENTED_EDGE ( 'NONE', *, *, #65563, .F. ) ;
#59019=VECTOR ( 'NONE', #91972, 1000.000000000000000 ) ;
#59032=CARTESIAN_POINT ( 'NONE',  ( 15.14080536460164517, 5.152774720514427642, -26.62908960815038384 ) ) ;
#59045=FACE_OUTER_BOUND ( 'NONE', #91266, .T. ) ;
#59053=ORIENTED_EDGE ( 'NONE', *, *, #56612, .T. ) ;
#59058=EDGE_CURVE ( 'NONE', #50681, #60699, #64014, .T. ) ;
#59062=CARTESIAN_POINT ( 'NONE',  ( -28.98875734969026041, -5.965225279485572685, 25.61802280011862720 ) ) ;
#59063=DIRECTION ( 'NONE',  ( -1.000000000000000000, 0.000000000000000000, -7.994117400814786717E-16 ) ) ;
#59066=EDGE_CURVE ( 'NONE', #79629, #82392, #48266, .T. ) ;
#59070=CARTESIAN_POINT ( 'NONE',  ( 27.53860345374784657, 4.772774720514425972, -8.321925749325748356 ) ) ;
#59090=ORIENTED_EDGE ( 'NONE', *, *, #47190, .F. ) ;
#59098=EDGE_CURVE ( 'NONE', #63837, #91326, #56392, .T. ) ;
#59110=EDGE_LOOP ( 'NONE', ( #76989, #5745, #58453, #66060 ) ) ;
#59112=CARTESIAN_POINT ( 'NONE',  ( 8.476323908314187250, 3.316774720514010788, -27.09030197646909599 ) ) ;
#59117=DIRECTION ( 'NONE',  ( -0.000000000000000000, -1.000000000000000000, -0.000000000000000000 ) ) ;
#59124=EDGE_CURVE ( 'NONE', #23703, #87143, #2598, .T. ) ;
#59135=DIRECTION ( 'NONE',  ( 1.000000000000000000, 0.000000000000000000, 0.000000000000000000 ) ) ;
#59139=CARTESIAN_POINT ( 'NONE',  ( 31.79364159983995464, 6.376774720514426953, -11.59305536555894278 ) ) ;
#59140=CARTESIAN_POINT ( 'NONE',  ( -22.05275734969026047, 0.3587747205144262708, 31.02402280011862246 ) ) ;
#59141=LINE ( 'NONE', #81479, #54022 ) ;
#59149=CARTESIAN_POINT ( 'NONE',  ( 30.58729439590573307, 4.540774720514427543, 26.14186284044631492 ) ) ;
#59151=AXIS2_PLACEMENT_3D ( 'NONE', #3777, #18981, #41845 ) ;
#59168=ORIENTED_EDGE ( 'NONE', *, *, #28977, .F. ) ;
#59173=EDGE_CURVE ( 'NONE', #80239, #75450, #10700, .T. ) ;
#59178=CARTESIAN_POINT ( 'NONE',  ( 32.66876533700882845, -6.475225279485573360, -12.58926540598385557 ) ) ;
#59183=DIRECTION ( 'NONE',  ( 0.000000000000000000, 0.000000000000000000, 1.000000000000000000 ) ) ;
#59189=LINE ( 'NONE', #91614, #53327 ) ;
#59204=CARTESIAN_POINT ( 'NONE',  ( 30.93860345374796594, 0.6647747205144264315, 19.84760796525321780 ) ) ;
#59213=EDGE_LOOP ( 'NONE', ( #54922, #100102, #53834, #75532 ) ) ;
#59221=AXIS2_PLACEMENT_3D ( 'NONE', #98111, #20988, #83390 ) ;
#59223=CARTESIAN_POINT ( 'NONE',  ( -2.704906987277317931, 6.376774720514425177, -28.92935364444904778 ) ) ;
#59238=CYLINDRICAL_SURFACE ( 'NONE', #14261, 2.249999999999998668 ) ;
#59256=CARTESIAN_POINT ( 'NONE',  ( 12.16765770914787304, -5.965225279485572685, -27.57618308014988173 ) ) ;
#59260=LINE ( 'NONE', #78960, #83693 ) ;
#59263=FACE_OUTER_BOUND ( 'NONE', #51834, .T. ) ;
#59276=FACE_OUTER_BOUND ( 'NONE', #29202, .T. ) ;
#59277=VECTOR ( 'NONE', #11363, 1000.000000000000114 ) ;
#59278=DIRECTION ( 'NONE',  ( 0.000000000000000000, 0.000000000000000000, 1.000000000000000000 ) ) ;
#59281=ORIENTED_EDGE ( 'NONE', *, *, #23176, .T. ) ;
#59295=ORIENTED_EDGE ( 'NONE', *, *, #47078, .T. ) ;
#59314=ORIENTED_EDGE ( 'NONE', *, *, #29263, .T. ) ;
#59325=VERTEX_POINT ( 'NONE', #28527 ) ;
#59332=LINE ( 'NONE', #12648, #23847 ) ;
#59334=CARTESIAN_POINT ( 'NONE',  ( 27.53860345374771867, 5.356774720514425603, -9.482392034746240483 ) ) ;
#59335=CARTESIAN_POINT ( 'NONE',  ( 9.422519371942208011, 3.316774720514425567, -27.03574706870085720 ) ) ;
#59382=LINE ( 'NONE', #42179, #76673 ) ;
#59383=CARTESIAN_POINT ( 'NONE',  ( 31.60706529141452137, 4.540774720514427543, 26.12024523944105070 ) ) ;
#59393=DIRECTION ( 'NONE',  ( 0.7512896232465891000, 0.000000000000000000, 0.6599726524652351767 ) ) ;
#59406=AXIS2_PLACEMENT_3D ( 'NONE', #67000, #96933, #27427 ) ;
#59407=CARTESIAN_POINT ( 'NONE',  ( -29.49875734969026198, -5.965225279485572685, 10.11402280011862587 ) ) ;
#59411=EDGE_CURVE ( 'NONE', #33824, #628, #30154, .T. ) ;
#59443=CARTESIAN_POINT ( 'NONE',  ( 32.76111974776238611, 3.316774720514426900, -3.850861272813261849 ) ) ;
#59458=EDGE_LOOP ( 'NONE', ( #51533, #38292, #52451, #98723 ) ) ;
#59473=EDGE_CURVE ( 'NONE', #50385, #22003, #50387, .T. ) ;
#59499=CIRCLE ( 'NONE', #64158, 1.149999999999999911 ) ;
#59506=DIRECTION ( 'NONE',  ( 0.000000000000000000, -1.000000000000000000, 0.000000000000000000 ) ) ;
#59514=EDGE_CURVE ( 'NONE', #24841, #4424, #25310, .T. ) ;
#59525=ADVANCED_FACE ( 'NONE', ( #60991 ), #37142, .F. ) ;
#59530=ORIENTED_EDGE ( 'NONE', *, *, #57149, .F. ) ;
#59546=DIRECTION ( 'NONE',  ( -0.000000000000000000, -1.000000000000000000, -0.000000000000000000 ) ) ;
#59575=CIRCLE ( 'NONE', #54724, 1.325999999999969647 ) ;
#59576=ORIENTED_EDGE ( 'NONE', *, *, #65273, .F. ) ;
#59602=ORIENTED_EDGE ( 'NONE', *, *, #82074, .T. ) ;
#59608=CARTESIAN_POINT ( 'NONE',  ( 7.491841679052118508, 5.356774720514426491, -25.13395656343690021 ) ) ;
#59610=CARTESIAN_POINT ( 'NONE',  ( -13.89275734969026388, -5.965225279485572685, 31.02402280011862246 ) ) ;
#59636=EDGE_CURVE ( 'NONE', #95120, #63086, #82152, .T. ) ;
#59646=FACE_OUTER_BOUND ( 'NONE', #75619, .T. ) ;
#59648=CARTESIAN_POINT ( 'NONE',  ( 30.61866831821571111, 5.272393720821680674, 0.8164977272573440414 ) ) ;
#59653=CARTESIAN_POINT ( 'NONE',  ( 29.71903944837828604, 4.668615314384465087, 27.69752233256919993 ) ) ;
#59669=ORIENTED_EDGE ( 'NONE', *, *, #19452, .F. ) ;
#59675=ORIENTED_EDGE ( 'NONE', *, *, #84833, .F. ) ;
#59678=ORIENTED_EDGE ( 'NONE', *, *, #28249, .T. ) ;
#59682=FACE_OUTER_BOUND ( 'NONE', #31788, .T. ) ;
#59700=EDGE_LOOP ( 'NONE', ( #57976, #64714, #58827, #76621, #75961, #33321 ) ) ;
#59707=DIRECTION ( 'NONE',  ( -0.000000000000000000, -0.000000000000000000, 1.000000000000000000 ) ) ;
#59711=ORIENTED_EDGE ( 'NONE', *, *, #77312, .T. ) ;
#59721=DIRECTION ( 'NONE',  ( 0.000000000000000000, 0.000000000000000000, 1.000000000000000000 ) ) ;
#59728=DIRECTION ( 'NONE',  ( 0.000000000000000000, 1.000000000000000000, 0.000000000000000000 ) ) ;
#59745=CARTESIAN_POINT ( 'NONE',  ( 31.31283134548411340, 4.772774720514425972, -10.20862453625735533 ) ) ;
#59763=CARTESIAN_POINT ( 'NONE',  ( 13.74975846015576586, -6.475225279485573360, -27.72022515045486557 ) ) ;
#59764=CARTESIAN_POINT ( 'NONE',  ( 26.73860345374794889, 5.162006989575464999, -6.453654992509125776 ) ) ;
#59770=ORIENTED_EDGE ( 'NONE', *, *, #22393, .F. ) ;
#59772=CARTESIAN_POINT ( 'NONE',  ( 19.75748517575715368, 0.3587747205144265483, 28.87153971905864580 ) ) ;
#59778=DIRECTION ( 'NONE',  ( 1.000000000000000000, -0.000000000000000000, -0.000000000000000000 ) ) ;
#59785=VECTOR ( 'NONE', #74966, 1000.000000000000114 ) ;
#59797=VECTOR ( 'NONE', #67885, 1000.000000000000000 ) ;
#59821=ORIENTED_EDGE ( 'NONE', *, *, #29719, .T. ) ;
#59834=VERTEX_POINT ( 'NONE', #15134 ) ;
#59838=LINE ( 'NONE', #91272, #55383 ) ;
#59841=LINE ( 'NONE', #27879, #7700 ) ;
#59842=AXIS2_PLACEMENT_3D ( 'NONE', #40686, #76353, #22556 ) ;
#59870=DIRECTION ( 'NONE',  ( -0.8264557562326033668, -6.845827386180409975E-16, -0.5630016722799281448 ) ) ;
#59877=LINE ( 'NONE', #75070, #56145 ) ;
#59888=CARTESIAN_POINT ( 'NONE',  ( 6.184520403203634942, 6.376774720514426953, -25.32021290018218451 ) ) ;
#59905=CYLINDRICAL_SURFACE ( 'NONE', #62333, 1.149999999999998135 ) ;
#59906=DIRECTION ( 'NONE',  ( 0.000000000000000000, 0.000000000000000000, -1.000000000000000000 ) ) ;
#59909=FACE_OUTER_BOUND ( 'NONE', #62413, .T. ) ;
#59911=ORIENTED_EDGE ( 'NONE', *, *, #63607, .F. ) ;
#59931=VECTOR ( 'NONE', #77762, 1000.000000000000000 ) ;
#59953=ORIENTED_EDGE ( 'NONE', *, *, #99252, .F. ) ;
#59959=ORIENTED_EDGE ( 'NONE', *, *, #83202, .F. ) ;
#59985=CIRCLE ( 'NONE', #85897, 27.94799999999999685 ) ;
#59986=EDGE_CURVE ( 'NONE', #57023, #45709, #56067, .T. ) ;
#60001=EDGE_CURVE ( 'NONE', #41039, #82023, #80434, .T. ) ;
#60006=AXIS2_PLACEMENT_3D ( 'NONE', #86608, #32323, #9984 ) ;
#60019=DIRECTION ( 'NONE',  ( 0.000000000000000000, 1.000000000000000000, -0.000000000000000000 ) ) ;
#60020=LINE ( 'NONE', #68122, #97217 ) ;
#60033=CARTESIAN_POINT ( 'NONE',  ( 22.33191539159815164, 4.132774720514426292, -16.26852658953823649 ) ) ;
#60037=EDGE_CURVE ( 'NONE', #56810, #33445, #64193, .T. ) ;
#60038=CARTESIAN_POINT ( 'NONE',  ( -4.993225604111834137, 0.3587747205143964613, -29.11654937215279304 ) ) ;
#60049=CARTESIAN_POINT ( 'NONE',  ( 31.44923352942285177, 5.094381739198088788, -4.378347922178638107 ) ) ;
#60062=FACE_OUTER_BOUND ( 'NONE', #28855, .T. ) ;
#60078=VECTOR ( 'NONE', #66859, 1000.000000000000000 ) ;
#60089=CARTESIAN_POINT ( 'NONE',  ( 19.75748517575715368, 0.3587747205144265483, 28.87153971905864580 ) ) ;
#60095=DIRECTION ( 'NONE',  ( -0.000000000000000000, -1.000000000000000000, 0.000000000000000000 ) ) ;
#60096=ORIENTED_EDGE ( 'NONE', *, *, #91518, .F. ) ;
#60101=ORIENTED_EDGE ( 'NONE', *, *, #4660, .T. ) ;
#60128=EDGE_CURVE ( 'NONE', #45825, #86005, #28105, .T. ) ;
#60131=DIRECTION ( 'NONE',  ( -0.000000000000000000, -1.000000000000000000, -0.000000000000000000 ) ) ;
#60145=EDGE_CURVE ( 'NONE', #10246, #50276, #42843, .T. ) ;
#60146=AXIS2_PLACEMENT_3D ( 'NONE', #64762, #3839, #50018 ) ;
#60152=CARTESIAN_POINT ( 'NONE',  ( 31.31121903262429029, 5.174141622015902442, 0.9154248472334550746 ) ) ;
#60157=CARTESIAN_POINT ( 'NONE',  ( 29.70220533163293908, 3.584876737299458771, 28.20564067568759015 ) ) ;
#60182=ORIENTED_EDGE ( 'NONE', *, *, #21671, .T. ) ;
#60197=AXIS2_PLACEMENT_3D ( 'NONE', #51019, #66262, #88082 ) ;
#60198=ORIENTED_EDGE ( 'NONE', *, *, #47736, .T. ) ;
#60202=CARTESIAN_POINT ( 'NONE',  ( 14.43441819135929194, 3.316774720514426456, -28.36222020317710957 ) ) ;
#60203=ORIENTED_EDGE ( 'NONE', *, *, #37889, .F. ) ;
#60217=ORIENTED_EDGE ( 'NONE', *, *, #56229, .T. ) ;
#60220=ORIENTED_EDGE ( 'NONE', *, *, #41109, .F. ) ;
#60222=ADVANCED_FACE ( 'NONE', ( #85880 ), #30587, .T. ) ;
#60229=EDGE_CURVE ( 'NONE', #44309, #32299, #61056, .T. ) ;
#60248=CARTESIAN_POINT ( 'NONE',  ( 22.02124265030973760, -6.143225279485574397, 16.20402280011862217 ) ) ;
#60251=DIRECTION ( 'NONE',  ( -0.000000000000000000, -1.000000000000000000, -0.000000000000000000 ) ) ;
#60262=ADVANCED_FACE ( 'NONE', ( #47325 ), #76252, .F. ) ;
#60263=ADVANCED_FACE ( 'NONE', ( #62052 ), #1149, .F. ) ;
#60266=CARTESIAN_POINT ( 'NONE',  ( 5.184553252003285984, -5.965225279485572685, -28.06387035751381731 ) ) ;
#60275=CARTESIAN_POINT ( 'NONE',  ( 20.13489193910630703, 2.682774720514426559, -22.92085183005112370 ) ) ;
#60278=CARTESIAN_POINT ( 'NONE',  ( 32.15269211224249091, 6.376774720514427841, 3.401810532325274750 ) ) ;
#60296=ORIENTED_EDGE ( 'NONE', *, *, #20454, .F. ) ;
#60312=PLANE ( 'NONE',  #51659 ) ;
#60319=EDGE_CURVE ( 'NONE', #96596, #12582, #14775, .T. ) ;
#60341=ORIENTED_EDGE ( 'NONE', *, *, #35638, .F. ) ;
#60343=AXIS2_PLACEMENT_3D ( 'NONE', #39147, #61998, #92926 ) ;
#60346=CARTESIAN_POINT ( 'NONE',  ( 5.356969261897235768, 0.3587747205143965168, -28.55262118024313978 ) ) ;
#60350=PLANE ( 'NONE',  #21948 ) ;
#60371=DIRECTION ( 'NONE',  ( 0.000000000000000000, -1.000000000000000000, 0.000000000000000000 ) ) ;
#60372=DIRECTION ( 'NONE',  ( 0.000000000000000000, 0.000000000000000000, -1.000000000000000000 ) ) ;
#60381=CARTESIAN_POINT ( 'NONE',  ( -19.80875734969026425, 0.3587747205144265483, 31.02402280011862246 ) ) ;
#60401=CARTESIAN_POINT ( 'NONE',  ( 27.53860345374808105, 5.356774720514427379, 1.647607965253217399 ) ) ;
#60409=VECTOR ( 'NONE', #38386, 1000.000000000000114 ) ;
#60415=ORIENTED_EDGE ( 'NONE', *, *, #95490, .F. ) ;
#60417=EDGE_LOOP ( 'NONE', ( #73416, #11734, #20820, #88154 ) ) ;
#60428=VERTEX_POINT ( 'NONE', #41217 ) ;
#60467=DIRECTION ( 'NONE',  ( -0.000000000000000000, -1.000000000000000000, -0.000000000000000000 ) ) ;
#60485=CARTESIAN_POINT ( 'NONE',  ( 25.61870917940689196, 6.376774720514426953, 28.79814474876424768 ) ) ;
#60499=ORIENTED_EDGE ( 'NONE', *, *, #39596, .F. ) ;
#60510=CARTESIAN_POINT ( 'NONE',  ( 22.02124265030973760, -6.143225279485574397, 19.55402280011862004 ) ) ;
#60530=FACE_OUTER_BOUND ( 'NONE', #85232, .T. ) ;
#60531=ORIENTED_EDGE ( 'NONE', *, *, #4542, .F. ) ;
#60534=DIRECTION ( 'NONE',  ( 0.000000000000000000, 0.000000000000000000, 1.000000000000000000 ) ) ;
#60562=VERTEX_POINT ( 'NONE', #15625 ) ;
#60573=EDGE_CURVE ( 'NONE', #53725, #13237, #86144, .T. ) ;
#60577=ORIENTED_EDGE ( 'NONE', *, *, #4476, .F. ) ;
#60592=ORIENTED_EDGE ( 'NONE', *, *, #63432, .T. ) ;
#60594=DIRECTION ( 'NONE',  ( 0.6559908753439240847, -0.4874460344622444929, 0.5762571777883070956 ) ) ;
#60595=CARTESIAN_POINT ( 'NONE',  ( -11.64875734969026233, -5.965225279485572685, 31.02402280011862246 ) ) ;
#60619=VECTOR ( 'NONE', #69266, 1000.000000000000000 ) ;
#60641=FACE_OUTER_BOUND ( 'NONE', #5595, .T. ) ;
#60643=FACE_OUTER_BOUND ( 'NONE', #24354, .T. ) ;
#60653=CARTESIAN_POINT ( 'NONE',  ( 2.449489742783178770, 4.293056017849825601, 2.499999999999999556 ) ) ;
#60680=ADVANCED_FACE ( 'NONE', ( #16126 ), #33497, .T. ) ;
#60699=VERTEX_POINT ( 'NONE', #26749 ) ;
#60725=FACE_OUTER_BOUND ( 'NONE', #49688, .T. ) ;
#60760=CARTESIAN_POINT ( 'NONE',  ( 9.843544857143434967, -5.965225279485572685, -27.49819965379373343 ) ) ;
#60774=ADVANCED_FACE ( 'NONE', ( #18625 ), #79532, .F. ) ;
#60775=B_SPLINE_CURVE_WITH_KNOTS ( 'NONE', 3,
 ( #22157, #78447, #55140, #24168 ),
 .UNSPECIFIED., .F., .F.,
 ( 4, 4 ),
 ( 8.673617379884035472E-19, 0.0002632372126714214219 ),
 .UNSPECIFIED. ) ;
#60784=CIRCLE ( 'NONE', #33245, 1.836000000000000743 ) ;
#60796=ORIENTED_EDGE ( 'NONE', *, *, #52088, .F. ) ;
#60812=CARTESIAN_POINT ( 'NONE',  ( 14.56569730433581533, 3.366897624368340391, -28.38594530802162197 ) ) ;
#60818=ORIENTED_EDGE ( 'NONE', *, *, #32985, .F. ) ;
#60826=EDGE_CURVE ( 'NONE', #46180, #81702, #48784, .T. ) ;
#60827=AXIS2_PLACEMENT_3D ( 'NONE', #65833, #89150, #81542 ) ;
#60844=LINE ( 'NONE', #92266, #31971 ) ;
#60845=CARTESIAN_POINT ( 'NONE',  ( 22.02124265030973760, -4.543225279485573864, 18.45402280011862217 ) ) ;
#60854=CARTESIAN_POINT ( 'NONE',  ( 30.53060340732036337, 5.329285123471892760, 3.289350009555732868 ) ) ;
#60861=CARTESIAN_POINT ( 'NONE',  ( 10.46399479596398052, 3.316774720514422903, -27.03001098546561209 ) ) ;
#60864=ORIENTED_EDGE ( 'NONE', *, *, #75467, .T. ) ;
#60890=VECTOR ( 'NONE', #30496, 1000.000000000000000 ) ;
#60894=CIRCLE ( 'NONE', #21955, 6.000000000000000888 ) ;
#60895=CARTESIAN_POINT ( 'NONE',  ( -29.49875734969025842, 0.3587747205144265483, 17.86602280011862476 ) ) ;
#60897=DIRECTION ( 'NONE',  ( 0.5630016722799281448, -5.365801633547219206E-16, -0.8264557562326033668 ) ) ;
#60906=CARTESIAN_POINT ( 'NONE',  ( 30.55775998287478856, -1.765878758506237434, 24.49934028559106736 ) ) ;
#60909=ORIENTED_EDGE ( 'NONE', *, *, #58382, .T. ) ;
#60928=ORIENTED_EDGE ( 'NONE', *, *, #51844, .T. ) ;
#60931=EDGE_LOOP ( 'NONE', ( #9782, #84647, #33838, #29056 ) ) ;
#60937=DIRECTION ( 'NONE',  ( 8.334928612639484546E-17, 1.000000000000000000, 7.321843366904296032E-17 ) ) ;
#60940=VECTOR ( 'NONE', #43903, 1000.000000000000000 ) ;
#60941=EDGE_CURVE ( 'NONE', #94742, #82156, #28243, .T. ) ;
#60944=DIRECTION ( 'NONE',  ( 0.000000000000000000, 0.000000000000000000, -1.000000000000000000 ) ) ;
#60950=VERTEX_POINT ( 'NONE', #47968 ) ;
#60963=LINE ( 'NONE', #23874, #85906 ) ;
#60987=CARTESIAN_POINT ( 'NONE',  ( 16.26279755680690542, 1.684774720514426560, -27.67997040356620531 ) ) ;
#60990=CARTESIAN_POINT ( 'NONE',  ( 9.196673285530609476, 6.376774720514424288, -25.00509208784493964 ) ) ;
#60991=FACE_OUTER_BOUND ( 'NONE', #77773, .T. ) ;
#61013=DIRECTION ( 'NONE',  ( 0.000000000000000000, 0.000000000000000000, -1.000000000000000000 ) ) ;
#61015=CARTESIAN_POINT ( 'NONE',  ( 25.61870917940689552, -5.965225279485572685, 28.79814474876421926 ) ) ;
#61025=CARTESIAN_POINT ( 'NONE',  ( 21.48823513768370574, 4.361976414099077992, -16.63192637262848450 ) ) ;
#61040=ORIENTED_EDGE ( 'NONE', *, *, #16430, .F. ) ;
#61056=LINE ( 'NONE', #22951, #18855 ) ;
#61069=ORIENTED_EDGE ( 'NONE', *, *, #25140, .T. ) ;
#61085=DIRECTION ( 'NONE',  ( 0.000000000000000000, -0.000000000000000000, -1.000000000000000000 ) ) ;
#61091=LINE ( 'NONE', #45857, #85376 ) ;
#61093=DIRECTION ( 'NONE',  ( 0.7071067811865476838, 0.000000000000000000, -0.7071067811865474617 ) ) ;
#61096=CIRCLE ( 'NONE', #1113, 1.325999999999943446 ) ;
#61116=CARTESIAN_POINT ( 'NONE',  ( 32.98733314340959311, 0.3587747205144265483, 2.074222136288530027 ) ) ;
#61136=CIRCLE ( 'NONE', #51415, 0.8160000000000000586 ) ;
#61149=ORIENTED_EDGE ( 'NONE', *, *, #32860, .F. ) ;
#61172=CIRCLE ( 'NONE', #12551, 251.4258649670780699 ) ;
#61181=VECTOR ( 'NONE', #32375, 1000.000000000000114 ) ;
#61220=VERTEX_POINT ( 'NONE', #21981 ) ;
#61222=CARTESIAN_POINT ( 'NONE',  ( 31.14267748017797288, 4.481735162546534923, -3.047060235321841226 ) ) ;
#61234=DIRECTION ( 'NONE',  ( 0.000000000000000000, -1.000000000000000000, 0.000000000000000000 ) ) ;
#61235=VECTOR ( 'NONE', #74573, 1000.000000000000000 ) ;
#61273=CARTESIAN_POINT ( 'NONE',  ( 14.76093561896379214, -5.965225279485572685, -26.55548769130089681 ) ) ;
#61289=CARTESIAN_POINT ( 'NONE',  ( 32.45853543194704116, -5.965225279485572685, 9.169203677920338080 ) ) ;
#61290=DIRECTION ( 'NONE',  ( 0.000000000000000000, 0.000000000000000000, 1.000000000000000000 ) ) ;
#61308=CARTESIAN_POINT ( 'NONE',  ( 27.53860345374808105, -1.477225279485574028, -6.982392034746242260 ) ) ;
#61312=FACE_OUTER_BOUND ( 'NONE', #73909, .T. ) ;
#61343=DIRECTION ( 'NONE',  ( -0.000000000000000000, -1.000000000000000000, -0.000000000000000000 ) ) ;
#61378=CARTESIAN_POINT ( 'NONE',  ( -4.686006777320708139, -5.965225279485572685, 29.60911411231905888 ) ) ;
#61399=DIRECTION ( 'NONE',  ( 0.000000000000000000, 0.000000000000000000, -1.000000000000000000 ) ) ;
#61406=PLANE ( 'NONE',  #20584 ) ;
#61409=DIRECTION ( 'NONE',  ( -0.000000000000000000, -1.000000000000000000, -0.000000000000000000 ) ) ;
#61421=ORIENTED_EDGE ( 'NONE', *, *, #23176, .F. ) ;
#61432=DIRECTION ( 'NONE',  ( 0.000000000000000000, -1.000000000000000000, 0.000000000000000000 ) ) ;
#61434=ORIENTED_EDGE ( 'NONE', *, *, #65989, .F. ) ;
#61450=ORIENTED_EDGE ( 'NONE', *, *, #28611, .F. ) ;
#61477=DIRECTION ( 'NONE',  ( 0.000000000000000000, 0.000000000000000000, -1.000000000000000000 ) ) ;
#61481=CARTESIAN_POINT ( 'NONE',  ( -26.91814428177455909, -5.965225279485572685, 29.98490496616818746 ) ) ;
#61504=CARTESIAN_POINT ( 'NONE',  ( 7.347880794884120722E-16, 5.356774720514425603, -6.000000000000000888 ) ) ;
#61510=VERTEX_POINT ( 'NONE', #52339 ) ;
#61511=AXIS2_PLACEMENT_3D ( 'NONE', #44836, #13866, #20481 ) ;
#61523=AXIS2_PLACEMENT_3D ( 'NONE', #100218, #7893, #15999 ) ;
#61547=DIRECTION ( 'NONE',  ( -0.9685340172660600322, 0.000000000000000000, 0.2488812114211667037 ) ) ;
#61551=DIRECTION ( 'NONE',  ( -4.448048651795319837E-16, 1.000000000000000000, -7.118365844322522408E-16 ) ) ;
#61556=VERTEX_POINT ( 'NONE', #19872 ) ;
#61574=EDGE_LOOP ( 'NONE', ( #8359, #26307 ) ) ;
#61587=CARTESIAN_POINT ( 'NONE',  ( 25.73006673792228938, 5.175315920840755091, -7.739742029708382987 ) ) ;
#61601=LINE ( 'NONE', #94022, #77363 ) ;
#61611=EDGE_CURVE ( 'NONE', #31632, #76406, #81786, .T. ) ;
#61616=CARTESIAN_POINT ( 'NONE',  ( 22.81105451610979173, -1.477225279485574028, -18.46691820600746681 ) ) ;
#61645=DIRECTION ( 'NONE',  ( 0.000000000000000000, 0.000000000000000000, 1.000000000000000000 ) ) ;
#61654=VERTEX_POINT ( 'NONE', #77651 ) ;
#61683=CARTESIAN_POINT ( 'NONE',  ( -2.872281323269014752, -1.473225279485573358, 1.999999999999999556 ) ) ;
#61685=CARTESIAN_POINT ( 'NONE',  ( 14.43441819135929194, 3.316774720514426456, -28.36222020317710957 ) ) ;
#61696=PLANE ( 'NONE',  #81111 ) ;
#61719=AXIS2_PLACEMENT_3D ( 'NONE', #38210, #85891, #54448 ) ;
#61731=CARTESIAN_POINT ( 'NONE',  ( 31.84105487026623393, 5.152774720514427642, -11.95870468328481806 ) ) ;
#61734=AXIS2_PLACEMENT_3D ( 'NONE', #82422, #90536, #21018 ) ;
#61740=CARTESIAN_POINT ( 'NONE',  ( 15.58962545129234556, 1.684774720514426560, -26.91365498785467736 ) ) ;
#61767=EDGE_CURVE ( 'NONE', #16991, #39655, #27388, .T. ) ;
#61771=CARTESIAN_POINT ( 'NONE',  ( 0.000000000000000000, 1.682774720514426114, 0.000000000000000000 ) ) ;
#61772=EDGE_CURVE ( 'NONE', #51486, #92435, #59841, .T. ) ;
#61774=CARTESIAN_POINT ( 'NONE',  ( 32.76524810979199742, 3.299944812882172229, -3.892744026461423701 ) ) ;
#61794=ORIENTED_EDGE ( 'NONE', *, *, #88594, .T. ) ;
#61796=ORIENTED_EDGE ( 'NONE', *, *, #8785, .F. ) ;
#61797=EDGE_LOOP ( 'NONE', ( #79289, #97314, #63301, #100126, #17477, #41716, #69202, #86766, #15472, #42964, #96327, #78883, #59295, #50884, #43369, #16318, #21820, #22549, #58337, #45586, #70552, #68250, #68695, #56790, #83745 ) ) ;
#61815=ORIENTED_EDGE ( 'NONE', *, *, #21035, .F. ) ;
#61829=CARTESIAN_POINT ( 'NONE',  ( 30.09341516180546350, 1.682774720514426114, -11.39311774897855756 ) ) ;
#61833=ORIENTED_EDGE ( 'NONE', *, *, #29742, .F. ) ;
#61838=CARTESIAN_POINT ( 'NONE',  ( -0.02075734969026423599, 6.376774720514426953, -0.08597719988137648983 ) ) ;
#61860=VECTOR ( 'NONE', #89076, 1000.000000000000227 ) ;
#61869=FACE_OUTER_BOUND ( 'NONE', #18526, .T. ) ;
#61885=EDGE_CURVE ( 'NONE', #18367, #94148, #12145, .T. ) ;
#61905=LINE ( 'NONE', #38050, #7324 ) ;
#61906=FACE_OUTER_BOUND ( 'NONE', #13119, .T. ) ;
#61907=VERTEX_POINT ( 'NONE', #57855 ) ;
#61909=EDGE_LOOP ( 'NONE', ( #97267, #19239, #14598, #69824 ) ) ;
#61928=CARTESIAN_POINT ( 'NONE',  ( -0.02075734969026423599, -5.965225279485572685, -0.08597719988137648983 ) ) ;
#61929=VERTEX_POINT ( 'NONE', #44110 ) ;
#61931=EDGE_CURVE ( 'NONE', #15218, #55557, #59332, .T. ) ;
#61946=ORIENTED_EDGE ( 'NONE', *, *, #44602, .T. ) ;
#61952=ORIENTED_EDGE ( 'NONE', *, *, #98102, .F. ) ;
#61977=EDGE_LOOP ( 'NONE', ( #70122, #75187 ) ) ;
#61989=CARTESIAN_POINT ( 'NONE',  ( 8.655157120194559184, 6.376774720514430506, -28.10018424674326099 ) ) ;
#61998=DIRECTION ( 'NONE',  ( -0.000000000000000000, 1.000000000000000000, -0.000000000000000000 ) ) ;
#62003=ORIENTED_EDGE ( 'NONE', *, *, #52294, .T. ) ;
#62004=CIRCLE ( 'NONE', #73383, 2.499999999999998668 ) ;
#62012=EDGE_CURVE ( 'NONE', #95021, #73142, #53064, .T. ) ;
#62014=AXIS2_PLACEMENT_3D ( 'NONE', #96811, #95808, #11565 ) ;
#62025=ORIENTED_EDGE ( 'NONE', *, *, #77124, .F. ) ;
#62029=EDGE_CURVE ( 'NONE', #7917, #76864, #54230, .T. ) ;
#62033=AXIS2_PLACEMENT_3D ( 'NONE', #54611, #16526, #316 ) ;
#62037=ORIENTED_EDGE ( 'NONE', *, *, #82410, .T. ) ;
#62043=CARTESIAN_POINT ( 'NONE',  ( 19.75748517575715368, 0.3587747205144265483, 28.87153971905864580 ) ) ;
#62052=FACE_OUTER_BOUND ( 'NONE', #28095, .T. ) ;
#62055=CARTESIAN_POINT ( 'NONE',  ( 32.33217928425140997, 6.376774720514426953, -12.20610769812822483 ) ) ;
#62056=VERTEX_POINT ( 'NONE', #29873 ) ;
#62066=DIRECTION ( 'NONE',  ( 0.000000000000000000, 0.000000000000000000, 1.000000000000000000 ) ) ;
#62068=EDGE_CURVE ( 'NONE', #76713, #35613, #60844, .T. ) ;
#62069=ORIENTED_EDGE ( 'NONE', *, *, #68327, .F. ) ;
#62082=ORIENTED_EDGE ( 'NONE', *, *, #48921, .F. ) ;
#62086=EDGE_CURVE ( 'NONE', #99683, #51818, #43359, .T. ) ;
#62090=CARTESIAN_POINT ( 'NONE',  ( -19.77875734969026311, -6.143225279485574397, 29.49402280011862487 ) ) ;
#62095=CARTESIAN_POINT ( 'NONE',  ( -12.64432969575899968, 0.3587747205143967943, -26.13179214487285407 ) ) ;
#62106=DIRECTION ( 'NONE',  ( 0.000000000000000000, 1.000000000000000000, 0.000000000000000000 ) ) ;
#62134=CARTESIAN_POINT ( 'NONE',  ( 5.271800844963591359, 3.316774720514426456, -28.56638892015329034 ) ) ;
#62137=EDGE_LOOP ( 'NONE', ( #31761, #59911, #93139, #94147, #34589 ) ) ;
#62145=EDGE_CURVE ( 'NONE', #98626, #82004, #50989, .T. ) ;
#62170=VECTOR ( 'NONE', #94409, 1000.000000000000000 ) ;
#62177=ORIENTED_EDGE ( 'NONE', *, *, #82188, .T. ) ;
#62182=CARTESIAN_POINT ( 'NONE',  ( 27.53860345374808105, 1.682774720514426114, -1.352392034746782823 ) ) ;
#62206=PLANE ( 'NONE',  #44003 ) ;
#62208=AXIS2_PLACEMENT_3D ( 'NONE', #40567, #71519, #19700 ) ;
#62215=CARTESIAN_POINT ( 'NONE',  ( 30.53060340732036337, 5.297812262124996785, 1.539714685317421505 ) ) ;
#62219=ORIENTED_EDGE ( 'NONE', *, *, #8636, .F. ) ;
#62260=AXIS2_PLACEMENT_3D ( 'NONE', #24423, #88337, #74110 ) ;
#62271=DIRECTION ( 'NONE',  ( 0.7512896232465892110, -0.000000000000000000, 0.6599726524652351767 ) ) ;
#62301=EDGE_LOOP ( 'NONE', ( #7807, #89620, #46364, #50576 ) ) ;
#62323=CARTESIAN_POINT ( 'NONE',  ( 32.76111974776238611, 3.316774720514426900, -3.850861272813261849 ) ) ;
#62333=AXIS2_PLACEMENT_3D ( 'NONE', #98940, #4616, #82718 ) ;
#62347=CARTESIAN_POINT ( 'NONE',  ( 5.271800844830267785, -5.965225279485592225, -28.56638892017480913 ) ) ;
#62379=VERTEX_POINT ( 'NONE', #52477 ) ;
#62389=ORIENTED_EDGE ( 'NONE', *, *, #27192, .T. ) ;
#62397=CARTESIAN_POINT ( 'NONE',  ( 32.16024265030974050, 0.3587747205144265483, 16.27760796525321751 ) ) ;
#62412=CIRCLE ( 'NONE', #76943, 0.8160000000000007248 ) ;
#62413=EDGE_LOOP ( 'NONE', ( #19235, #3017, #36728, #3027 ) ) ;
#62414=CARTESIAN_POINT ( 'NONE',  ( -10.59832330691884117, 0.3587747205144061757, -27.05373799718300987 ) ) ;
#62415=VECTOR ( 'NONE', #59546, 1000.000000000000000 ) ;
#62439=EDGE_CURVE ( 'NONE', #93762, #73142, #99619, .T. ) ;
#62442=VECTOR ( 'NONE', #56519, 1000.000000000000000 ) ;
#62445=ADVANCED_FACE ( 'NONE', ( #92022 ), #90527, .F. ) ;
#62472=VECTOR ( 'NONE', #39806, 1000.000000000000000 ) ;
#62522=ORIENTED_EDGE ( 'NONE', *, *, #48287, .T. ) ;
#62540=VECTOR ( 'NONE', #9425, 1000.000000000000000 ) ;
#62553=VECTOR ( 'NONE', #62271, 1000.000000000000227 ) ;
#62556=EDGE_CURVE ( 'NONE', #29304, #39840, #61601, .T. ) ;
#62562=PLANE ( 'NONE',  #58763 ) ;
#62563=VERTEX_POINT ( 'NONE', #38730 ) ;
#62573=DIRECTION ( 'NONE',  ( 0.000000000000000000, 0.000000000000000000, 1.000000000000000000 ) ) ;
#62580=AXIS2_PLACEMENT_3D ( 'NONE', #78563, #33403, #87196 ) ;
#62620=PLANE ( 'NONE',  #51549 ) ;
#62621=CIRCLE ( 'NONE', #78811, 252.4458649670781085 ) ;
#62634=FACE_OUTER_BOUND ( 'NONE', #90733, .T. ) ;
#62637=EDGE_CURVE ( 'NONE', #26765, #81702, #83597, .T. ) ;
#62650=VECTOR ( 'NONE', #22705, 1000.000000000000000 ) ;
#62662=DIRECTION ( 'NONE',  ( -0.000000000000000000, 1.000000000000000000, -0.000000000000000000 ) ) ;
#62679=ORIENTED_EDGE ( 'NONE', *, *, #52235, .T. ) ;
#62681=CARTESIAN_POINT ( 'NONE',  ( -4.686006777320704586, 6.376774720514426953, 29.60911411231905888 ) ) ;
#62684=AXIS2_PLACEMENT_3D ( 'NONE', #75432, #99757, #6438 ) ;
#62685=LINE ( 'NONE', #62182, #15704 ) ;
#62700=AXIS2_PLACEMENT_3D ( 'NONE', #18013, #40848, #70809 ) ;
#62717=ORIENTED_EDGE ( 'NONE', *, *, #83651, .F. ) ;
#62734=CARTESIAN_POINT ( 'NONE',  ( 32.84232313084847732, 4.840274619473232676, -11.71291885348859196 ) ) ;
#62758=EDGE_CURVE ( 'NONE', #1553, #48376, #48279, .T. ) ;
#62775=ORIENTED_EDGE ( 'NONE', *, *, #50981, .T. ) ;
#62779=PLANE ( 'NONE',  #30503 ) ;
#62785=VERTEX_POINT ( 'NONE', #83288 ) ;
#62815=CARTESIAN_POINT ( 'NONE',  ( 9.315600972258339496, 6.376774720514426953, 28.35070303307545458 ) ) ;
#62819=ORIENTED_EDGE ( 'NONE', *, *, #14530, .T. ) ;
#62823=AXIS2_PLACEMENT_3D ( 'NONE', #38744, #83928, #39746 ) ;
#62842=PLANE ( 'NONE',  #97650 ) ;
#62856=DIRECTION ( 'NONE',  ( 0.7689940216596069522, -5.365801633547218220E-16, -0.6392559695863496705 ) ) ;
#62884=CARTESIAN_POINT ( 'NONE',  ( 29.93983266611829563, 5.350981799920698556, 19.84760796525321780 ) ) ;
#62885=CARTESIAN_POINT ( 'NONE',  ( 13.91401389203221406, -6.475225279485573360, 158.0376437107427137 ) ) ;
#62896=VERTEX_POINT ( 'NONE', #54356 ) ;
#62905=PLANE ( 'NONE',  #78679 ) ;
#62916=CIRCLE ( 'NONE', #56399, 22.69500000000000384 ) ;
#62932=ORIENTED_EDGE ( 'NONE', *, *, #13604, .F. ) ;
#62943=CARTESIAN_POINT ( 'NONE',  ( 10.86264264036872440, 0.3587747205144257157, -28.05717073575603138 ) ) ;
#62959=EDGE_LOOP ( 'NONE', ( #92219, #88055, #85504, #15596 ) ) ;
#62972=DIRECTION ( 'NONE',  ( -0.4009304992412300317, -6.845827386180410961E-16, -0.9161084732596779245 ) ) ;
#62993=VECTOR ( 'NONE', #25186, 1000.000000000000000 ) ;
#63005=CARTESIAN_POINT ( 'NONE',  ( 9.818046095193736278, 3.316774720514088504, -28.04791984001701621 ) ) ;
#63007=ORIENTED_EDGE ( 'NONE', *, *, #92731, .F. ) ;
#63012=CARTESIAN_POINT ( 'NONE',  ( 3.252401863874215593, 0.3587747205143964613, -29.35688408629929214 ) ) ;
#63023=LINE ( 'NONE', #55912, #93763 ) ;
#63053=ORIENTED_EDGE ( 'NONE', *, *, #81947, .T. ) ;
#63086=VERTEX_POINT ( 'NONE', #2572 ) ;
#63105=CARTESIAN_POINT ( 'NONE',  ( -41.32836283488544638, 2.682774720514426559, 39.26872235229541985 ) ) ;
#63107=EDGE_LOOP ( 'NONE', ( #86435, #2838, #25219, #11343 ) ) ;
#63113=FACE_OUTER_BOUND ( 'NONE', #69645, .T. ) ;
#63149=CARTESIAN_POINT ( 'NONE',  ( -29.49875734969025842, 0.3587747205144265483, 17.86602280011862476 ) ) ;
#63177=CARTESIAN_POINT ( 'NONE',  ( 282.9764569301858046, -5.965225279485572685, 20.79159422840526616 ) ) ;
#63208=VERTEX_POINT ( 'NONE', #82676 ) ;
#63227=DIRECTION ( 'NONE',  ( -0.000000000000000000, -1.000000000000000000, -0.000000000000000000 ) ) ;
#63230=DIRECTION ( 'NONE',  ( 0.000000000000000000, -0.000000000000000000, -1.000000000000000000 ) ) ;
#63238=LINE ( 'NONE', #40391, #99875 ) ;
#63244=CARTESIAN_POINT ( 'NONE',  ( 11.62916340711181284, -5.965225279485572685, 28.75961759920349792 ) ) ;
#63254=CIRCLE ( 'NONE', #94013, 130.2784398600581710 ) ;
#63256=CYLINDRICAL_SURFACE ( 'NONE', #5882, 2.040000000000000036 ) ;
#63260=AXIS2_PLACEMENT_3D ( 'NONE', #12149, #35510, #66485 ) ;
#63270=AXIS2_PLACEMENT_3D ( 'NONE', #31898, #85684, #16164 ) ;
#63281=FACE_OUTER_BOUND ( 'NONE', #797, .T. ) ;
#63297=DIRECTION ( 'NONE',  ( 0.000000000000000000, 0.000000000000000000, -1.000000000000000000 ) ) ;
#63301=ORIENTED_EDGE ( 'NONE', *, *, #100223, .T. ) ;
#63302=ORIENTED_EDGE ( 'NONE', *, *, #58727, .T. ) ;
#63303=ORIENTED_EDGE ( 'NONE', *, *, #46204, .F. ) ;
#63304=EDGE_LOOP ( 'NONE', ( #57981, #95307, #41446, #41450, #79128 ) ) ;
#63348=LINE ( 'NONE', #46105, #47336 ) ;
#63362=CARTESIAN_POINT ( 'NONE',  ( -6.741682653110981249, 0.3587747205144265483, 30.62569541381301619 ) ) ;
#63366=CYLINDRICAL_SURFACE ( 'NONE', #91649, 1.149999999999999911 ) ;
#63376=EDGE_CURVE ( 'NONE', #85295, #89124, #25275, .T. ) ;
#63388=LINE ( 'NONE', #9073, #49652 ) ;
#63403=PLANE ( 'NONE',  #66260 ) ;
#63406=B_SPLINE_CURVE_WITH_KNOTS ( 'NONE', 3,
 ( #13635, #60346, #21247, #21743 ),
 .UNSPECIFIED., .F., .F.,
 ( 4, 4 ),
 ( 0.6459941988912109023, 0.6543842573219610381 ),
 .UNSPECIFIED. ) ;
#63410=ORIENTED_EDGE ( 'NONE', *, *, #14237, .T. ) ;
#63421=EDGE_CURVE ( 'NONE', #871, #92857, #40520, .T. ) ;
#63431=LINE ( 'NONE', #94348, #36889 ) ;
#63432=EDGE_CURVE ( 'NONE', #31584, #22977, #9552, .T. ) ;
#63435=ORIENTED_EDGE ( 'NONE', *, *, #40335, .F. ) ;
#63436=VERTEX_POINT ( 'NONE', #1456 ) ;
#63447=DIRECTION ( 'NONE',  ( 0.000000000000000000, 0.000000000000000000, 1.000000000000000000 ) ) ;
#63457=EDGE_CURVE ( 'NONE', #50697, #15254, #94787, .T. ) ;
#63481=VECTOR ( 'NONE', #95813, 1000.000000000000000 ) ;
#63490=DIRECTION ( 'NONE',  ( 0.000000000000000000, -1.000000000000000000, 0.000000000000000000 ) ) ;
#63492=CARTESIAN_POINT ( 'NONE',  ( 33.61456970919604714, -5.965225279485572685, -11.35828564741647462 ) ) ;
#63500=ORIENTED_EDGE ( 'NONE', *, *, #36502, .T. ) ;
#63505=DIRECTION ( 'NONE',  ( -0.000000000000000000, 1.000000000000000000, -0.000000000000000000 ) ) ;
#63513=CARTESIAN_POINT ( 'NONE',  ( -19.80875734969026425, 0.3587747205144265483, 30.51402280011862089 ) ) ;
#63524=DIRECTION ( 'NONE',  ( -0.9994733861282923959, -0.000000000000000000, -0.03244919754393515293 ) ) ;
#63531=VERTEX_POINT ( 'NONE', #92603 ) ;
#63556=DIRECTION ( 'NONE',  ( -6.267148949376405333E-16, -1.000000000000000000, 5.583826031377241668E-16 ) ) ;
#63567=CARTESIAN_POINT ( 'NONE',  ( -13.89275734969026388, 0.3587747205144262708, 31.02402280011862246 ) ) ;
#63571=DIRECTION ( 'NONE',  ( -0.000000000000000000, -1.000000000000000000, 0.000000000000000000 ) ) ;
#63573=DIRECTION ( 'NONE',  ( -0.000000000000000000, -1.000000000000000000, 0.000000000000000000 ) ) ;
#63579=AXIS2_PLACEMENT_3D ( 'NONE', #79922, #57113, #48494 ) ;
#63607=EDGE_CURVE ( 'NONE', #19596, #35854, #13247, .T. ) ;
#63611=FACE_OUTER_BOUND ( 'NONE', #68108, .T. ) ;
#63663=CARTESIAN_POINT ( 'NONE',  ( -10.21560369921944833, 5.622950887248190810, 29.47514638292475553 ) ) ;
#63666=AXIS2_PLACEMENT_3D ( 'NONE', #35785, #57140, #26675 ) ;
#63674=CARTESIAN_POINT ( 'NONE',  ( -19.69812919673063689, -5.965225279485592225, -22.00173861453435720 ) ) ;
#63679=ORIENTED_EDGE ( 'NONE', *, *, #53856, .T. ) ;
#63699=LINE ( 'NONE', #69790, #77569 ) ;
#63703=ORIENTED_EDGE ( 'NONE', *, *, #10083, .F. ) ;
#63705=EDGE_LOOP ( 'NONE', ( #77860, #29954, #10983 ) ) ;
#63706=ORIENTED_EDGE ( 'NONE', *, *, #11451, .F. ) ;
#63720=ORIENTED_EDGE ( 'NONE', *, *, #20454, .T. ) ;
#63735=CARTESIAN_POINT ( 'NONE',  ( -0.02075734969026423599, -5.965225279485572685, -0.08597719988137648983 ) ) ;
#63740=AXIS2_PLACEMENT_3D ( 'NONE', #57840, #89271, #82154 ) ;
#63763=FACE_OUTER_BOUND ( 'NONE', #33953, .T. ) ;
#63774=CARTESIAN_POINT ( 'NONE',  ( 14.43441820105630136, 3.540887625665272598, -28.36222020492957796 ) ) ;
#63793=CARTESIAN_POINT ( 'NONE',  ( -41.32836283488544638, 5.356774720514427379, 39.26872235229541985 ) ) ;
#63810=ORIENTED_EDGE ( 'NONE', *, *, #30203, .T. ) ;
#63816=EDGE_CURVE ( 'NONE', #69079, #44339, #28056, .T. ) ;
#63821=CARTESIAN_POINT ( 'NONE',  ( -24.90875734969025501, -5.965225279485572685, 30.00402280011862288 ) ) ;
#63833=CARTESIAN_POINT ( 'NONE',  ( 29.70220533433691301, 3.316774720514426456, 28.20564067601639735 ) ) ;
#63835=DIRECTION ( 'NONE',  ( 0.000000000000000000, -1.000000000000000000, 0.000000000000000000 ) ) ;
#63837=VERTEX_POINT ( 'NONE', #95194 ) ;
#63850=DIRECTION ( 'NONE',  ( -0.000000000000000000, -1.000000000000000000, -0.000000000000000000 ) ) ;
#63852=EDGE_CURVE ( 'NONE', #29304, #92190, #14280, .T. ) ;
#63892=EDGE_CURVE ( 'NONE', #57483, #88037, #25172, .T. ) ;
#63895=EDGE_CURVE ( 'NONE', #78402, #24307, #35670, .T. ) ;
#63906=CARTESIAN_POINT ( 'NONE',  ( 33.63305001869471056, 3.481148584080995700, -11.52139411009015291 ) ) ;
#63907=CARTESIAN_POINT ( 'NONE',  ( 30.57170936966216601, -5.053692695095620913, 25.34935773471745790 ) ) ;
#63916=VERTEX_POINT ( 'NONE', #48537 ) ;
#63925=DIRECTION ( 'NONE',  ( -0.000000000000000000, -1.000000000000000000, -0.000000000000000000 ) ) ;
#63939=LINE ( 'NONE', #45309, #9283 ) ;
#63962=CARTESIAN_POINT ( 'NONE',  ( 15.29947330337540556, 3.405372460181236960, -27.16854002387011491 ) ) ;
#63971=CARTESIAN_POINT ( 'NONE',  ( -0.02075734969026145696, 5.866774720514426278, -22.78097719988138081 ) ) ;
#63986=DIRECTION ( 'NONE',  ( 1.000000000000000000, -0.000000000000000000, 0.000000000000000000 ) ) ;
#64014=LINE ( 'NONE', #93035, #18790 ) ;
#64025=DIRECTION ( 'NONE',  ( -0.000000000000000000, -1.000000000000000000, -0.000000000000000000 ) ) ;
#64043=CARTESIAN_POINT ( 'NONE',  ( -20.77875734969026311, -6.143225279485574397, 27.31649921512899937 ) ) ;
#64064=VERTEX_POINT ( 'NONE', #99039 ) ;
#64072=ORIENTED_EDGE ( 'NONE', *, *, #81154, .T. ) ;
#64073=LINE ( 'NONE', #63567, #98509 ) ;
#64088=EDGE_LOOP ( 'NONE', ( #1581, #94517, #4411, #49568 ) ) ;
#64097=LINE ( 'NONE', #73192, #2 ) ;
#64100=AXIS2_PLACEMENT_3D ( 'NONE', #67821, #28744, #22597 ) ;
#64113=VERTEX_POINT ( 'NONE', #14803 ) ;
#64119=DIRECTION ( 'NONE',  ( -2.464095846557964090E-17, -1.000000000000000000, 0.000000000000000000 ) ) ;
#64135=CARTESIAN_POINT ( 'NONE',  ( 30.93860345374796594, 6.376774720514426953, 28.83647319851474933 ) ) ;
#64158=AXIS2_PLACEMENT_3D ( 'NONE', #83901, #21486, #67204 ) ;
#64166=DIRECTION ( 'NONE',  ( -0.000000000000000000, 1.000000000000000000, -0.000000000000000000 ) ) ;
#64177=CARTESIAN_POINT ( 'NONE',  ( 14.76093561896379214, -6.475225279485574248, -26.55548769130089681 ) ) ;
#64192=CYLINDRICAL_SURFACE ( 'NONE', #46676, 1.150000000000003464 ) ;
#64193=LINE ( 'NONE', #57572, #73992 ) ;
#64199=FACE_OUTER_BOUND ( 'NONE', #47431, .T. ) ;
#64223=DIRECTION ( 'NONE',  ( -0.000000000000000000, 1.000000000000000000, -0.000000000000000000 ) ) ;
#64240=EDGE_CURVE ( 'NONE', #86154, #74525, #32546, .T. ) ;
#64242=CARTESIAN_POINT ( 'NONE',  ( -53.01255352321339842, 5.356774720514425603, 35.59556822165056644 ) ) ;
#64249=VERTEX_POINT ( 'NONE', #16818 ) ;
#64253=DIRECTION ( 'NONE',  ( -0.9952638024365005887, -0.000000000000000000, -0.09721092304694052555 ) ) ;
#64268=CARTESIAN_POINT ( 'NONE',  ( -65.05438548721848235, 3.316774720514426456, 27.45402280011862572 ) ) ;
#64303=ORIENTED_EDGE ( 'NONE', *, *, #16101, .T. ) ;
#64304=DIRECTION ( 'NONE',  ( -0.000000000000000000, -1.000000000000000000, -0.000000000000000000 ) ) ;
#64308=VECTOR ( 'NONE', #66077, 1000.000000000000000 ) ;
#64313=ORIENTED_EDGE ( 'NONE', *, *, #79555, .F. ) ;
#64320=ADVANCED_FACE ( 'NONE', ( #88343 ), #96948, .T. ) ;
#64328=ORIENTED_EDGE ( 'NONE', *, *, #28018, .F. ) ;
#64352=VECTOR ( 'NONE', #75791, 1000.000000000000000 ) ;
#64364=EDGE_CURVE ( 'NONE', #32410, #65068, #36045, .T. ) ;
#64373=ADVANCED_FACE ( 'NONE', ( #11214 ), #95947, .F. ) ;
#64388=VECTOR ( 'NONE', #89898, 1000.000000000000000 ) ;
#64391=ORIENTED_EDGE ( 'NONE', *, *, #59098, .F. ) ;
#64392=EDGE_CURVE ( 'NONE', #42928, #44309, #26448, .T. ) ;
#64403=DIRECTION ( 'NONE',  ( 0.000000000000000000, -1.478457507934778393E-16, -1.000000000000000000 ) ) ;
#64407=LINE ( 'NONE', #10087, #16902 ) ;
#64412=ORIENTED_EDGE ( 'NONE', *, *, #7932, .F. ) ;
#64415=ADVANCED_FACE ( 'NONE', ( #42187 ), #43666, .T. ) ;
#64419=B_SPLINE_SURFACE_WITH_KNOTS ( 'NONE', 3, 1, ( 
 ( #6041, #21253 ),
 ( #35509, #82169 ),
 ( #52227, #35992 ),
 ( #83157, #20257 ),
 ( #97878, #13142 ),
 ( #5045, #44114 ),
 ( #59335, #84157 ),
 ( #66966, #90284 ),
 ( #20755, #43616 ),
 ( #99381, #36992 ),
 ( #51225, #74557 ),
 ( #74067, #67453 ),
 ( #22247, #14142 ),
 ( #13641, #53229 ) ),
 .UNSPECIFIED., .F., .F., .F.,
 ( 4, 2, 2, 2, 2, 2, 4 ),
 ( 2, 2 ),
 ( 0.000000000000000000, 0.2499999999999996114, 0.3749999999999996669, 0.4999999999999997780, 0.6249999999999998890, 0.7499999999999998890, 1.000000000000000000 ),
 ( 0.000000000000000000, 1.000000000000000000 ),
 .UNSPECIFIED. ) ;
#64420=CARTESIAN_POINT ( 'NONE',  ( 33.23241444531825550, 3.542570809989110447, -12.77295888271925328 ) ) ;
#64426=ADVANCED_FACE ( 'NONE', ( #73124 ), #96448, .F. ) ;
#64430=ORIENTED_EDGE ( 'NONE', *, *, #15243, .F. ) ;
#64431=PRODUCT_DEFINITION_SHAPE ( 'NONE', 'NONE',  #10919 ) ;
#64434=ORIENTED_EDGE ( 'NONE', *, *, #84192, .T. ) ;
#64450=AXIS2_PLACEMENT_3D ( 'NONE', #41583, #5005, #89245 ) ;
#64457=ORIENTED_EDGE ( 'NONE', *, *, #57699, .T. ) ;
#64465=EDGE_CURVE ( 'NONE', #57808, #14974, #12198, .T. ) ;
#64473=ORIENTED_EDGE ( 'NONE', *, *, #28695, .F. ) ;
#64493=DIRECTION ( 'NONE',  ( -0.000000000000000000, -1.000000000000000000, -0.000000000000000000 ) ) ;
#64500=LINE ( 'NONE', #49761, #52461 ) ;
#64509=PLANE ( 'NONE',  #40656 ) ;
#64527=DIRECTION ( 'NONE',  ( -0.000000000000000000, 1.000000000000000000, -0.000000000000000000 ) ) ;
#64534=DIRECTION ( 'NONE',  ( 1.000000000000000000, 4.088963247170718308E-15, 0.000000000000000000 ) ) ;
#64537=EDGE_LOOP ( 'NONE', ( #28766, #44332, #49121, #59675 ) ) ;
#64538=ADVANCED_FACE ( 'NONE', ( #20806 ), #75097, .F. ) ;
#64540=CARTESIAN_POINT ( 'NONE',  ( -24.57525087998973845, -5.965225279485572685, -15.45548830044932309 ) ) ;
#64548=VERTEX_POINT ( 'NONE', #90830 ) ;
#64549=CARTESIAN_POINT ( 'NONE',  ( 29.64448763235240136, 5.625929005037784592, 28.17618604274316851 ) ) ;
#64552=DIRECTION ( 'NONE',  ( -0.000000000000000000, 1.000000000000000000, -0.000000000000000000 ) ) ;
#64559=VERTEX_POINT ( 'NONE', #91822 ) ;
#64574=EDGE_CURVE ( 'NONE', #37842, #58683, #76586, .T. ) ;
#64579=VECTOR ( 'NONE', #99525, 1000.000000000000000 ) ;
#64582=DIRECTION ( 'NONE',  ( 1.000000000000000000, -0.000000000000000000, -0.000000000000000000 ) ) ;
#64585=CARTESIAN_POINT ( 'NONE',  ( 29.67488939790761648, 5.972177877498852538, 27.69255262365155801 ) ) ;
#64587=EDGE_CURVE ( 'NONE', #50385, #92857, #66183, .T. ) ;
#64600=CARTESIAN_POINT ( 'NONE',  ( 28.87399897812681004, 4.772774720514425972, -12.57761096169975445 ) ) ;
#64602=CARTESIAN_POINT ( 'NONE',  ( 3.509873074917118085, -5.965225279485572685, 29.15869884040363758 ) ) ;
#64604=CARTESIAN_POINT ( 'NONE',  ( 25.26411791610096813, 5.170221718577081127, -8.437879337975932259 ) ) ;
#64634=ADVANCED_FACE ( 'NONE', ( #22792 ), #63403, .T. ) ;
#64645=VECTOR ( 'NONE', #11364, 1000.000000000000000 ) ;
#64655=CARTESIAN_POINT ( 'NONE',  ( 32.53346577320684219, 2.682774720514426559, -11.93731717363806766 ) ) ;
#64661=DIRECTION ( 'NONE',  ( -0.2488812114211667037, -0.000000000000000000, -0.9685340172660599212 ) ) ;
#64664=CARTESIAN_POINT ( 'NONE',  ( -29.49875734969025842, -5.965225279485572685, 23.37402280011862743 ) ) ;
#64683=LINE ( 'NONE', #47932, #64645 ) ;
#64689=ORIENTED_EDGE ( 'NONE', *, *, #13716, .F. ) ;
#64710=EDGE_LOOP ( 'NONE', ( #24464, #33724, #88046, #14100 ) ) ;
#64714=ORIENTED_EDGE ( 'NONE', *, *, #3842, .F. ) ;
#64721=AXIS2_PLACEMENT_3D ( 'NONE', #45620, #51733, #91772 ) ;
#64762=CARTESIAN_POINT ( 'NONE',  ( -20.27875734969026311, -4.543225279485573864, 24.00402280011862288 ) ) ;
#64769=CARTESIAN_POINT ( 'NONE',  ( 9.402885806365684829, 0.3587747205144265483, 29.04108526060719342 ) ) ;
#64770=DIRECTION ( 'NONE',  ( 0.03244919754393515293, 0.000000000000000000, -0.9994733861282923959 ) ) ;
#64783=LINE ( 'NONE', #39906, #26306 ) ;
#64791=AXIS2_PLACEMENT_3D ( 'NONE', #58183, #81516, #51066 ) ;
#64805=CARTESIAN_POINT ( 'NONE',  ( -25.92875734969025814, 3.316774720514426456, 0.7300228001186309656 ) ) ;
#64808=AXIS2_PLACEMENT_3D ( 'NONE', #93497, #87398, #47343 ) ;
#64832=CARTESIAN_POINT ( 'NONE',  ( -29.49875734969025842, 0.3587747205144265483, 17.86602280011862476 ) ) ;
#64859=AXIS2_PLACEMENT_3D ( 'NONE', #32199, #49956, #55559 ) ;
#64875=CIRCLE ( 'NONE', #3297, 2.040000000000001368 ) ;
#64889=DIRECTION ( 'NONE',  ( 0.000000000000000000, -1.000000000000000000, 1.478457507934778393E-16 ) ) ;
#64898=CARTESIAN_POINT ( 'NONE',  ( 14.76093561896379214, 3.316774720514426456, -26.55548769130089681 ) ) ;
#64904=LINE ( 'NONE', #33924, #63481 ) ;
#64908=DIRECTION ( 'NONE',  ( 0.9822594791677485837, 0.000000000000000000, -0.1875268396392986980 ) ) ;
#64927=CARTESIAN_POINT ( 'NONE',  ( 22.81105451610979173, -1.477225279485574028, -18.46691820600746681 ) ) ;
#64950=VECTOR ( 'NONE', #87686, 1000.000000000000000 ) ;
#64971=ORIENTED_EDGE ( 'NONE', *, *, #44281, .T. ) ;
#64973=EDGE_LOOP ( 'NONE', ( #99837, #60531, #17417, #27430, #88934, #5131, #67171 ) ) ;
#64990=DIRECTION ( 'NONE',  ( 0.000000000000000000, -1.000000000000000000, 0.000000000000000000 ) ) ;
#64998=CARTESIAN_POINT ( 'NONE',  ( -19.80875734969026425, 0.3587747205144265483, 31.02402280011862246 ) ) ;
#65043=CARTESIAN_POINT ( 'NONE',  ( 15.63775912259742995, 4.567193422986040474, -28.22903731538627525 ) ) ;
#65049=CARTESIAN_POINT ( 'NONE',  ( 31.62080439023052492, 4.380055315099236957, 26.73348078282562668 ) ) ;
#65054=CARTESIAN_POINT ( 'NONE',  ( 15.03820766250734309, 3.514597374712530531, -27.31689629941529773 ) ) ;
#65067=ORIENTED_EDGE ( 'NONE', *, *, #70272, .T. ) ;
#65068=VERTEX_POINT ( 'NONE', #22675 ) ;
#65083=CARTESIAN_POINT ( 'NONE',  ( 29.74616903497430442, 6.356993644837154456, 26.56043482791313082 ) ) ;
#65128=VECTOR ( 'NONE', #39893, 1000.000000000000000 ) ;
#65147=EDGE_CURVE ( 'NONE', #35959, #97546, #13570, .T. ) ;
#65166=EDGE_CURVE ( 'NONE', #57723, #91984, #24187, .T. ) ;
#65203=EDGE_CURVE ( 'NONE', #41305, #16459, #46537, .T. ) ;
#65206=AXIS2_PLACEMENT_3D ( 'NONE', #24163, #86067, #47517 ) ;
#65212=VERTEX_POINT ( 'NONE', #77463 ) ;
#65229=ORIENTED_EDGE ( 'NONE', *, *, #29742, .T. ) ;
#65270=CARTESIAN_POINT ( 'NONE',  ( -41.32836283488544638, 5.152774720514427642, 39.26872235229541985 ) ) ;
#65273=EDGE_CURVE ( 'NONE', #74181, #20569, #73867, .T. ) ;
#65281=CARTESIAN_POINT ( 'NONE',  ( 15.30669617938070459, 3.316774720514427344, -28.51986056384665957 ) ) ;
#65298=DIRECTION ( 'NONE',  ( -0.7689940216596065081, 0.000000000000000000, 0.6392559695863502256 ) ) ;
#65302=ORIENTED_EDGE ( 'NONE', *, *, #94197, .F. ) ;
#65305=CARTESIAN_POINT ( 'NONE',  ( 32.58581522646812090, 4.151341569991283897, -4.025368652865530805 ) ) ;
#65322=DIRECTION ( 'NONE',  ( 0.000000000000000000, -0.000000000000000000, -1.000000000000000000 ) ) ;
#65333=ORIENTED_EDGE ( 'NONE', *, *, #97653, .F. ) ;
#65337=CARTESIAN_POINT ( 'NONE',  ( 30.09341516180546350, 4.772774720514425972, -11.39311774897855756 ) ) ;
#65355=CIRCLE ( 'NONE', #28084, 28.96799999999999642 ) ;
#65356=ORIENTED_EDGE ( 'NONE', *, *, #60128, .F. ) ;
#65385=VECTOR ( 'NONE', #84416, 1000.000000000000000 ) ;
#65391=CARTESIAN_POINT ( 'NONE',  ( 29.73828978136054602, 4.772774720514425972, -4.021765098496561386 ) ) ;
#65398=DIRECTION ( 'NONE',  ( 0.000000000000000000, -1.000000000000000000, 0.000000000000000000 ) ) ;
#65425=CARTESIAN_POINT ( 'NONE',  ( -10.21384395349174490, 6.376774720514426953, 29.49402280011861777 ) ) ;
#65428=VERTEX_POINT ( 'NONE', #93069 ) ;
#65430=ORIENTED_EDGE ( 'NONE', *, *, #5837, .F. ) ;
#65434=DIRECTION ( 'NONE',  ( 0.000000000000000000, 1.000000000000000000, 0.000000000000000000 ) ) ;
#65436=VERTEX_POINT ( 'NONE', #78836 ) ;
#65442=EDGE_LOOP ( 'NONE', ( #98988, #98012, #24315 ) ) ;
#65473=CARTESIAN_POINT ( 'NONE',  ( -41.32836283488544638, 2.682774720514426559, 39.26872235229541985 ) ) ;
#65488=AXIS2_PLACEMENT_3D ( 'NONE', #68907, #53197, #46082 ) ;
#65506=CARTESIAN_POINT ( 'NONE',  ( 8.573524122111766843, -5.965225279485574461, -28.10203366675327175 ) ) ;
#65525=DIRECTION ( 'NONE',  ( 0.000000000000000000, 0.000000000000000000, 1.000000000000000000 ) ) ;
#65531=DIRECTION ( 'NONE',  ( 0.000000000000000000, -0.000000000000000000, 1.000000000000000000 ) ) ;
#65540=CARTESIAN_POINT ( 'NONE',  ( 14.43441819134413073, 3.316774720514428232, -28.36222020317436687 ) ) ;
#65545=EDGE_CURVE ( 'NONE', #32090, #40087, #32176, .T. ) ;
#65547=CARTESIAN_POINT ( 'NONE',  ( 31.65781406150966149, 5.771867554241929987, 28.25297929084410242 ) ) ;
#65548=AXIS2_PLACEMENT_3D ( 'NONE', #72914, #11496, #59183 ) ;
#65551=CARTESIAN_POINT ( 'NONE',  ( 14.61581676223891613, 3.316774720514426900, -27.35847991879931485 ) ) ;
#65563=EDGE_CURVE ( 'NONE', #11608, #35597, #35453, .T. ) ;
#65578=CARTESIAN_POINT ( 'NONE',  ( -23.71328795744024021, -5.965225279485594001, -17.58350715675015152 ) ) ;
#65601=ORIENTED_EDGE ( 'NONE', *, *, #45916, .F. ) ;
#65605=DIRECTION ( 'NONE',  ( 1.000000000000000000, 4.089440751051245812E-15, 0.000000000000000000 ) ) ;
#65620=CIRCLE ( 'NONE', #20237, 1.149999999999999911 ) ;
#65632=ORIENTED_EDGE ( 'NONE', *, *, #83283, .T. ) ;
#65667=EDGE_CURVE ( 'NONE', #71522, #35425, #49429, .T. ) ;
#65674=VECTOR ( 'NONE', #23696, 1000.000000000000000 ) ;
#65686=CARTESIAN_POINT ( 'NONE',  ( 22.65031661608483660, 500000.0000000000582, -20.71116937900383093 ) ) ;
#65688=AXIS2_PLACEMENT_3D ( 'NONE', #57968, #34621, #79777 ) ;
#65689=VERTEX_POINT ( 'NONE', #89966 ) ;
#65691=CARTESIAN_POINT ( 'NONE',  ( -10.21991166328316325, 3.845527176268170422, 29.42879868625613327 ) ) ;
#65709=FACE_OUTER_BOUND ( 'NONE', #31754, .T. ) ;
#65730=CARTESIAN_POINT ( 'NONE',  ( 22.02124265030973760, 3.456774720514426136, 16.20402280011862217 ) ) ;
#65735=EDGE_CURVE ( 'NONE', #58117, #12272, #51914, .T. ) ;
#65739=CARTESIAN_POINT ( 'NONE',  ( 5.325188327271017208, 5.356774720514426491, -25.45818409267644711 ) ) ;
#65746=CARTESIAN_POINT ( 'NONE',  ( 14.52511747680497933, -5.965225279485572685, -27.86035006098926559 ) ) ;
#65751=EDGE_CURVE ( 'NONE', #91850, #65428, #90960, .T. ) ;
#65758=CARTESIAN_POINT ( 'NONE',  ( -10.79305683637731228, 0.3587747205144057872, -27.49869550653261285 ) ) ;
#65766=AXIS2_PLACEMENT_3D ( 'NONE', #87423, #94534, #47873 ) ;
#65774=CARTESIAN_POINT ( 'NONE',  ( 14.46675407819882331, 3.972730170967898378, -28.29579275198952359 ) ) ;
#65792=CARTESIAN_POINT ( 'NONE',  ( -41.32836283488544638, -2.803225279485573207, 39.26872235229541985 ) ) ;
#65809=DIRECTION ( 'NONE',  ( 0.000000000000000000, -1.000000000000000000, 0.000000000000000000 ) ) ;
#65814=FACE_OUTER_BOUND ( 'NONE', #509, .T. ) ;
#65819=CARTESIAN_POINT ( 'NONE',  ( 26.73860345374794889, 5.356774720514427379, -3.111611894936215705 ) ) ;
#65833=CARTESIAN_POINT ( 'NONE',  ( 27.53860345374771867, 4.772774720514425972, -9.482392034746240483 ) ) ;
#65896=CARTESIAN_POINT ( 'NONE',  ( -28.98875734969026041, 0.3587747205144265483, 17.86602280011862476 ) ) ;
#65898=AXIS2_PLACEMENT_3D ( 'NONE', #598, #31549, #32553 ) ;
#65902=DIRECTION ( 'NONE',  ( -0.9980236263794188822, 0.000000000000000000, 0.06283980576413537855 ) ) ;
#65909=CIRCLE ( 'NONE', #20523, 28.96799999999999642 ) ;
#65916=PLANE ( 'NONE',  #83740 ) ;
#65938=VERTEX_POINT ( 'NONE', #3506 ) ;
#65941=AXIS2_PLACEMENT_3D ( 'NONE', #28019, #11290, #58480 ) ;
#65947=ADVANCED_FACE ( 'NONE', ( #73509 ), #4001, .F. ) ;
#65972=CARTESIAN_POINT ( 'NONE',  ( 0.000000000000000000, 2.682774720514426559, 0.000000000000000000 ) ) ;
#65989=EDGE_CURVE ( 'NONE', #54547, #15218, #11597, .T. ) ;
#65995=DIRECTION ( 'NONE',  ( 0.000000000000000000, 0.000000000000000000, -1.000000000000000000 ) ) ;
#65997=FACE_OUTER_BOUND ( 'NONE', #13977, .T. ) ;
#66003=( BOUNDED_SURFACE ( )  B_SPLINE_SURFACE ( 3, 2, ( 
 ( #68202, #14895, #58715 ),
 ( #15394, #89666, #91526 ),
 ( #7788, #38733, #45375 ),
 ( #83918, #69699, #181 ),
 ( #58230, #44874, #89169 ),
 ( #50606, #13896, #14396 ) ),
 .UNSPECIFIED., .F., .F., .T. ) 
 B_SPLINE_SURFACE_WITH_KNOTS ( ( 4, 2, 4 ),
 ( 3, 3 ),
 ( 0.001113071882895040263, 0.001219813747004279327, 0.001326555611113518392 ),
 ( 0.000000000000000000, 1.000000000000000000 ),
 .UNSPECIFIED. ) 
 GEOMETRIC_REPRESENTATION_ITEM ( )  RATIONAL_B_SPLINE_SURFACE ( (
 ( 1.000000000000000000, 0.7071067811865114905, 1.000000000000000000),
 ( 1.000000000000000000, 0.7264088502634352684, 1.000000000000000000),
 ( 1.000000000000000000, 0.7445305694446069378, 1.000000000000000000),
 ( 1.000000000000000000, 0.7788548593121751296, 1.000000000000000000),
 ( 1.000000000000000000, 0.7952519535464425138, 1.000000000000000000),
 ( 1.000000000000000000, 0.8096947957033885368, 1.000000000000000000) ) ) 
 REPRESENTATION_ITEM ( '' )  SURFACE ( )  );
#66018=AXIS2_PLACEMENT_3D ( 'NONE', #78425, #32260, #63230 ) ;
#66020=CARTESIAN_POINT ( 'NONE',  ( 9.492487079130338401, 5.851656861456516978, -26.75003832473357690 ) ) ;
#66039=VECTOR ( 'NONE', #34463, 1000.000000000000000 ) ;
#66041=CARTESIAN_POINT ( 'NONE',  ( -28.98875734969026041, 6.376774720514426953, 26.43402280011862615 ) ) ;
#66051=DIRECTION ( 'NONE',  ( 1.286817348990133408E-16, 0.000000000000000000, -1.000000000000000000 ) ) ;
#66058=CARTESIAN_POINT ( 'NONE',  ( -11.64875734969026233, -5.965225279485572685, 31.02402280011862246 ) ) ;
#66060=ORIENTED_EDGE ( 'NONE', *, *, #64364, .F. ) ;
#66077=DIRECTION ( 'NONE',  ( -1.334402673828313093E-16, -0.000000000000000000, -1.000000000000000000 ) ) ;
#66079=CARTESIAN_POINT ( 'NONE',  ( 29.80070917940689412, 6.376774720514426953, 27.39560796525321607 ) ) ;
#66083=EDGE_LOOP ( 'NONE', ( #2057, #80867, #79034, #72558 ) ) ;
#66086=VERTEX_POINT ( 'NONE', #45065 ) ;
#66103=AXIS2_PLACEMENT_3D ( 'NONE', #71333, #78921, #1318 ) ;
#66113=AXIS2_PLACEMENT_3D ( 'NONE', #4766, #29586, #43827 ) ;
#66125=CARTESIAN_POINT ( 'NONE',  ( -23.59123376470063960, 5.356774720514425603, 24.50402280011862288 ) ) ;
#66133=ORIENTED_EDGE ( 'NONE', *, *, #90693, .F. ) ;
#66135=CARTESIAN_POINT ( 'NONE',  ( 16.15056352287345121, 3.622774720514426949, -27.77856273171767398 ) ) ;
#66150=CARTESIAN_POINT ( 'NONE',  ( -23.31187512739357359, 6.376774720514425177, -17.31005501743528541 ) ) ;
#66155=LINE ( 'NONE', #57033, #6440 ) ;
#66156=ORIENTED_EDGE ( 'NONE', *, *, #37545, .F. ) ;
#66164=CARTESIAN_POINT ( 'NONE',  ( 15.08554537508427629, 5.152774720514429418, -26.79085230644757232 ) ) ;
#66177=LINE ( 'NONE', #44320, #11158 ) ;
#66183=CIRCLE ( 'NONE', #22384, 252.4458649670781085 ) ;
#66190=EDGE_LOOP ( 'NONE', ( #30831, #58933, #4996, #69503 ) ) ;
#66197=ORIENTED_EDGE ( 'NONE', *, *, #6823, .T. ) ;
#66198=CARTESIAN_POINT ( 'NONE',  ( 31.84105487026622683, 3.622774720514426949, -11.95870468328481984 ) ) ;
#66203=ORIENTED_EDGE ( 'NONE', *, *, #21354, .F. ) ;
#66221=CARTESIAN_POINT ( 'NONE',  ( 14.61581677259038692, 3.466180823938291855, -27.35847992067005308 ) ) ;
#66222=DIRECTION ( 'NONE',  ( -1.000000000000000000, 0.000000000000000000, 0.000000000000000000 ) ) ;
#66260=AXIS2_PLACEMENT_3D ( 'NONE', #87212, #475, #8596 ) ;
#66262=DIRECTION ( 'NONE',  ( 0.000000000000000000, 1.000000000000000000, 0.000000000000000000 ) ) ;
#66272=CARTESIAN_POINT ( 'NONE',  ( 22.81105451610979173, -1.475225279485572916, -18.46691820600746681 ) ) ;
#66282=LINE ( 'NONE', #82967, #30633 ) ;
#66301=VECTOR ( 'NONE', #56043, 999.9999999999998863 ) ;
#66306=LINE ( 'NONE', #75377, #79372 ) ;
#66308=CARTESIAN_POINT ( 'NONE',  ( 14.75122623597950700, 4.701663563191169182, -27.79036425924726217 ) ) ;
#66322=EDGE_CURVE ( 'NONE', #70795, #6012, #84110, .T. ) ;
#66330=ORIENTED_EDGE ( 'NONE', *, *, #19452, .T. ) ;
#66332=AXIS2_PLACEMENT_3D ( 'NONE', #64927, #34944, #49686 ) ;
#66359=DIRECTION ( 'NONE',  ( 0.6599726524652350657, 0.000000000000000000, -0.7512896232465892110 ) ) ;
#66391=CARTESIAN_POINT ( 'NONE',  ( 13.82660648177921914, -6.475225279485573360, -27.21585177491302332 ) ) ;
#66398=CARTESIAN_POINT ( 'NONE',  ( 33.61456970919608978, 3.316774720514426900, -11.35828564741662738 ) ) ;
#66421=ORIENTED_EDGE ( 'NONE', *, *, #90589, .T. ) ;
#66432=EDGE_LOOP ( 'NONE', ( #76939, #70008, #13956, #68801, #62932 ) ) ;
#66450=DIRECTION ( 'NONE',  ( 0.000000000000000000, 0.000000000000000000, -1.000000000000000000 ) ) ;
#66452=ORIENTED_EDGE ( 'NONE', *, *, #67709, .F. ) ;
#66464=CARTESIAN_POINT ( 'NONE',  ( -27.96875734969026084, 3.316774720514426456, 0.7300228001186309656 ) ) ;
#66465=CARTESIAN_POINT ( 'NONE',  ( 11.62916340711181284, 0.3587747205144265483, 28.75961759920349792 ) ) ;
#66472=ORIENTED_EDGE ( 'NONE', *, *, #89532, .T. ) ;
#66485=DIRECTION ( 'NONE',  ( 0.000000000000000000, 0.000000000000000000, 1.000000000000000000 ) ) ;
#66488=DIRECTION ( 'NONE',  ( 1.000000000000000000, -0.000000000000000000, -0.000000000000000000 ) ) ;
#66504=FACE_OUTER_BOUND ( 'NONE', #91713, .T. ) ;
#66507=CARTESIAN_POINT ( 'NONE',  ( 10.40578984036287302, -5.965225279485572685, -28.04626194901324965 ) ) ;
#66511=DIRECTION ( 'NONE',  ( -0.000000000000000000, 1.000000000000000000, -0.000000000000000000 ) ) ;
#66538=DIRECTION ( 'NONE',  ( 0.000000000000000000, -1.000000000000000000, 0.000000000000000000 ) ) ;
#66545=CIRCLE ( 'NONE', #60006, 28.45799999999999486 ) ;
#66546=DIRECTION ( 'NONE',  ( -0.000000000000000000, 1.000000000000000000, -0.000000000000000000 ) ) ;
#66553=EDGE_LOOP ( 'NONE', ( #85522, #6641, #55715, #51603 ) ) ;
#66555=CARTESIAN_POINT ( 'NONE',  ( 15.18017043975972058, 3.555325937910594813, -27.25057598448095675 ) ) ;
#66557=CARTESIAN_POINT ( 'NONE',  ( 22.81105451610979173, -6.475225279485573360, -17.31691820600746823 ) ) ;
#66565=DIRECTION ( 'NONE',  ( -0.000000000000000000, 1.000000000000000000, -0.000000000000000000 ) ) ;
#66597=FACE_OUTER_BOUND ( 'NONE', #76355, .T. ) ;
#66605=AXIS2_PLACEMENT_3D ( 'NONE', #63735, #57612, #17530 ) ;
#66607=AXIS2_PLACEMENT_3D ( 'NONE', #83868, #99083, #98084 ) ;
#66613=CARTESIAN_POINT ( 'NONE',  ( 29.73860345376319003, -1.477225279485574028, 19.84760796525321780 ) ) ;
#66629=EDGE_CURVE ( 'NONE', #13594, #19685, #13973, .T. ) ;
#66653=LINE ( 'NONE', #23413, #45172 ) ;
#66659=DIRECTION ( 'NONE',  ( 1.000000000000000000, -0.000000000000000000, -0.000000000000000000 ) ) ;
#66702=ORIENTED_EDGE ( 'NONE', *, *, #87931, .F. ) ;
#66710=VERTEX_POINT ( 'NONE', #8363 ) ;
#66717=DIRECTION ( 'NONE',  ( 0.000000000000000000, 0.000000000000000000, -1.000000000000000000 ) ) ;
#66732=CARTESIAN_POINT ( 'NONE',  ( 10.86264265030973952, 0.3587747205144257157, -27.62597719988137612 ) ) ;
#66764=EDGE_CURVE ( 'NONE', #86336, #42928, #39309, .T. ) ;
#66774=EDGE_CURVE ( 'NONE', #84269, #87661, #31192, .T. ) ;
#66775=CARTESIAN_POINT ( 'NONE',  ( 3.252401863874210264, -5.965225279485592225, -29.35688408629928858 ) ) ;
#66777=CIRCLE ( 'NONE', #21314, 2.499999999999998668 ) ;
#66780=DIRECTION ( 'NONE',  ( 1.000000000000000000, 0.000000000000000000, -0.000000000000000000 ) ) ;
#66811=CARTESIAN_POINT ( 'NONE',  ( 13.91401389203221406, -5.965225279485572685, 158.0376437107427137 ) ) ;
#66813=AXIS2_PLACEMENT_3D ( 'NONE', #67585, #44245, #75173 ) ;
#66824=PLANE ( 'NONE',  #70201 ) ;
#66829=ORIENTED_EDGE ( 'NONE', *, *, #88267, .T. ) ;
#66846=FACE_OUTER_BOUND ( 'NONE', #66553, .T. ) ;
#66853=CARTESIAN_POINT ( 'NONE',  ( 32.66876533700882845, -5.965225279485572685, -12.58926540598385557 ) ) ;
#66859=DIRECTION ( 'NONE',  ( -0.000000000000000000, -1.000000000000000000, -0.000000000000000000 ) ) ;
#66862=DIRECTION ( 'NONE',  ( -1.000000000000000000, -0.000000000000000000, -0.000000000000000000 ) ) ;
#66863=DIRECTION ( 'NONE',  ( -1.000000000000000000, -0.000000000000000000, -0.000000000000000000 ) ) ;
#66888=DIRECTION ( 'NONE',  ( -0.9952638024365005887, -0.000000000000000000, -0.09721092304694052555 ) ) ;
#66907=VECTOR ( 'NONE', #24148, 1000.000000000000114 ) ;
#66928=EDGE_LOOP ( 'NONE', ( #78674, #87698, #77766, #50796, #902, #75169, #86839, #58583, #29963, #95150, #92474, #22563, #60203, #85661, #100058, #66452, #30832, #46329, #81783, #92461, #57965, #47425, #82353, #100113 ) ) ;
#66960=ORIENTED_EDGE ( 'NONE', *, *, #21122, .T. ) ;
#66963=CARTESIAN_POINT ( 'NONE',  ( -28.47875734969025885, -5.965225279485572685, -0.08597719988136941216 ) ) ;
#66966=CARTESIAN_POINT ( 'NONE',  ( 10.22568704553358643, 3.316774720514425567, -27.02513721610328901 ) ) ;
#66985=ORIENTED_EDGE ( 'NONE', *, *, #74622, .T. ) ;
#66986=DIRECTION ( 'NONE',  ( 0.000000000000000000, 0.000000000000000000, -1.000000000000000000 ) ) ;
#66995=VECTOR ( 'NONE', #40605, 1000.000000000000000 ) ;
#67000=CARTESIAN_POINT ( 'NONE',  ( -19.37210865224160017, 0.3587747205143967943, -21.60955166348796297 ) ) ;
#67004=VECTOR ( 'NONE', #44530, 1000.000000000000000 ) ;
#67012=DIRECTION ( 'NONE',  ( 1.334402673828313339E-16, -0.000000000000000000, -1.000000000000000000 ) ) ;
#67020=EDGE_CURVE ( 'NONE', #39091, #10813, #43815, .T. ) ;
#67052=ORIENTED_EDGE ( 'NONE', *, *, #65203, .T. ) ;
#67060=VECTOR ( 'NONE', #48861, 1000.000000000000000 ) ;
#67065=CARTESIAN_POINT ( 'NONE',  ( -24.90875734969025501, 6.376774720514426953, 26.43402280011862615 ) ) ;
#67074=EDGE_LOOP ( 'NONE', ( #39350, #6035 ) ) ;
#67138=VECTOR ( 'NONE', #73758, 1000.000000000000000 ) ;
#67169=DIRECTION ( 'NONE',  ( 0.000000000000000000, 0.000000000000000000, -1.000000000000000000 ) ) ;
#67171=ORIENTED_EDGE ( 'NONE', *, *, #47078, .F. ) ;
#67186=CARTESIAN_POINT ( 'NONE',  ( 31.24279708945211098, 4.510509370595455536, 1.827416827591516357 ) ) ;
#67204=DIRECTION ( 'NONE',  ( 0.000000000000000000, 0.000000000000000000, -1.000000000000000000 ) ) ;
#67221=EDGE_CURVE ( 'NONE', #74870, #396, #32575, .T. ) ;
#67233=ORIENTED_EDGE ( 'NONE', *, *, #25735, .T. ) ;
#67239=DIRECTION ( 'NONE',  ( 0.000000000000000000, -1.000000000000000000, 0.000000000000000000 ) ) ;
#67247=CARTESIAN_POINT ( 'NONE',  ( 0.000000000000000000, -1.473225279485573802, 0.000000000000000000 ) ) ;
#67250=CARTESIAN_POINT ( 'NONE',  ( 2.449489742783178770, -16.94322527948557422, 2.499999999999999556 ) ) ;
#67260=DIRECTION ( 'NONE',  ( 0.000000000000000000, 1.000000000000000000, 0.000000000000000000 ) ) ;
#67266=CARTESIAN_POINT ( 'NONE',  ( 30.61558003201036726, 3.638743767327229151, 27.34189434213806535 ) ) ;
#67291=EDGE_LOOP ( 'NONE', ( #51974, #55374, #98749, #48320 ) ) ;
#67304=AXIS2_PLACEMENT_3D ( 'NONE', #33548, #49794, #64534 ) ;
#67311=ORIENTED_EDGE ( 'NONE', *, *, #91799, .F. ) ;
#67312=ORIENTED_EDGE ( 'NONE', *, *, #88779, .F. ) ;
#67313=CARTESIAN_POINT ( 'NONE',  ( 2.872281323269014752, -1.473225279485573358, 1.999999999999999556 ) ) ;
#67330=AXIS2_PLACEMENT_3D ( 'NONE', #83221, #90842, #97456 ) ;
#67336=CIRCLE ( 'NONE', #9021, 2.249999999999998668 ) ;
#67358=DIRECTION ( 'NONE',  ( -0.9831680378442392287, -0.000000000000000000, -0.1827036106964188000 ) ) ;
#67379=EDGE_CURVE ( 'NONE', #99263, #67734, #83743, .T. ) ;
#67380=DIRECTION ( 'NONE',  ( -0.000000000000000000, -0.000000000000000000, 1.000000000000000000 ) ) ;
#67381=CARTESIAN_POINT ( 'NONE',  ( 33.61456970919608978, 3.316774720514426900, -11.35828564741660962 ) ) ;
#67382=CARTESIAN_POINT ( 'NONE',  ( 10.86264265030973952, 0.3587747205144257157, -28.64597719988137570 ) ) ;
#67391=LINE ( 'NONE', #83087, #57705 ) ;
#67393=DIRECTION ( 'NONE',  ( 0.000000000000000000, 0.000000000000000000, 1.000000000000000000 ) ) ;
#67409=EDGE_LOOP ( 'NONE', ( #49669, #15442, #39730, #12423 ) ) ;
#67410=ORIENTED_EDGE ( 'NONE', *, *, #78715, .T. ) ;
#67426=VERTEX_POINT ( 'NONE', #51815 ) ;
#67429=DIRECTION ( 'NONE',  ( -0.000000000000000000, -1.000000000000000000, -0.000000000000000000 ) ) ;
#67430=ORIENTED_EDGE ( 'NONE', *, *, #73979, .T. ) ;
#67453=CARTESIAN_POINT ( 'NONE',  ( 12.99736557111424595, -6.475225279485574248, -27.13536621820933448 ) ) ;
#67472=DIRECTION ( 'NONE',  ( 0.000000000000000000, -1.000000000000000000, 0.000000000000000000 ) ) ;
#67477=CARTESIAN_POINT ( 'NONE',  ( 14.76093561896379214, -6.475225279485574248, -27.37148769130089931 ) ) ;
#67479=VECTOR ( 'NONE', #17804, 1000.000000000000114 ) ;
#67487=CARTESIAN_POINT ( 'NONE',  ( 15.32643653063177958, 3.577630190450218350, -27.14485409495429380 ) ) ;
#67495=EDGE_CURVE ( 'NONE', #49235, #38164, #27968, .T. ) ;
#67506=CARTESIAN_POINT ( 'NONE',  ( -19.77875734969026311, -6.143225279485574397, 27.31649921512899937 ) ) ;
#67511=CARTESIAN_POINT ( 'NONE',  ( -24.90875734969025501, 6.376774720514426953, 29.49402280011861777 ) ) ;
#67526=LINE ( 'NONE', #36557, #687 ) ;
#67530=DIRECTION ( 'NONE',  ( -0.000000000000000000, -1.000000000000000000, 0.000000000000000000 ) ) ;
#67533=ADVANCED_FACE ( 'NONE', ( #6123, #37075 ), #68040, .T. ) ;
#67550=EDGE_CURVE ( 'NONE', #30854, #47768, #76618, .T. ) ;
#67554=CARTESIAN_POINT ( 'NONE',  ( -0.02075734969026423599, 5.866774720514426278, -0.08597719988137648983 ) ) ;
#67585=CARTESIAN_POINT ( 'NONE',  ( -29.49875734969026198, 0.3587747205144265483, 2.362022800118626531 ) ) ;
#67594=LINE ( 'NONE', #97525, #18295 ) ;
#67600=VERTEX_POINT ( 'NONE', #17743 ) ;
#67611=EDGE_CURVE ( 'NONE', #87143, #94978, #25852, .T. ) ;
#67613=ORIENTED_EDGE ( 'NONE', *, *, #84721, .F. ) ;
#67617=DIRECTION ( 'NONE',  ( -0.9980236263794188822, 0.000000000000000000, 0.06283980576413539243 ) ) ;
#67626=CARTESIAN_POINT ( 'NONE',  ( -20.27875734969026311, 3.456774720514426136, 22.85402280011862430 ) ) ;
#67642=CARTESIAN_POINT ( 'NONE',  ( 9.478389368232452483, 2.682774720514426559, -23.17485683983816003 ) ) ;
#67664=FACE_OUTER_BOUND ( 'NONE', #80480, .T. ) ;
#67665=ORIENTED_EDGE ( 'NONE', *, *, #62029, .T. ) ;
#67666=ORIENTED_EDGE ( 'NONE', *, *, #20775, .F. ) ;
#67688=EDGE_CURVE ( 'NONE', #97596, #3302, #52277, .T. ) ;
#67694=ORIENTED_EDGE ( 'NONE', *, *, #93664, .T. ) ;
#67695=LINE ( 'NONE', #21479, #39725 ) ;
#67705=VERTEX_POINT ( 'NONE', #64655 ) ;
#67707=CARTESIAN_POINT ( 'NONE',  ( 14.64534568429317218, 3.754078354150065522, -27.31564152833324499 ) ) ;
#67708=CARTESIAN_POINT ( 'NONE',  ( 1.305682803664691249, -5.965225279485572685, 29.57950906855421991 ) ) ;
#67709=EDGE_CURVE ( 'NONE', #78496, #54952, #18445, .T. ) ;
#67714=VERTEX_POINT ( 'NONE', #33676 ) ;
#67734=VERTEX_POINT ( 'NONE', #81348 ) ;
#67765=CARTESIAN_POINT ( 'NONE',  ( 30.61317826727886526, 3.861502214243257125, 27.24847364799711613 ) ) ;
#67775=EDGE_CURVE ( 'NONE', #37481, #69074, #4226, .T. ) ;
#67788=DIRECTION ( 'NONE',  ( 0.9685340172660600322, 0.000000000000000000, -0.2488812114211667315 ) ) ;
#67797=ORIENTED_EDGE ( 'NONE', *, *, #21671, .F. ) ;
#67807=DIRECTION ( 'NONE',  ( 0.1875268396392986980, 0.000000000000000000, 0.9822594791677485837 ) ) ;
#67808=CARTESIAN_POINT ( 'NONE',  ( 29.77147767949874790, 5.356774720514425603, 26.15915692125051706 ) ) ;
#67821=CARTESIAN_POINT ( 'NONE',  ( -29.49875734969026198, -5.965225279485572685, 2.362022800118626531 ) ) ;
#67847=CYLINDRICAL_SURFACE ( 'NONE', #42315, 2.040000000000000036 ) ;
#67859=CARTESIAN_POINT ( 'NONE',  ( 5.271800844963591359, 0.3587747205143965168, -28.56638892015329745 ) ) ;
#67864=LINE ( 'NONE', #6452, #50712 ) ;
#67874=LINE ( 'NONE', #83576, #57107 ) ;
#67882=AXIS2_PLACEMENT_3D ( 'NONE', #70561, #47, #38609 ) ;
#67885=DIRECTION ( 'NONE',  ( 1.000000000000000000, -0.000000000000000000, -0.000000000000000000 ) ) ;
#67894=ADVANCED_FACE ( 'NONE', ( #985 ), #14193, .T. ) ;
#67899=ADVANCED_FACE ( 'NONE', ( #100416 ), #62905, .F. ) ;
#67926=DIRECTION ( 'NONE',  ( 0.000000000000000000, -1.000000000000000000, 0.000000000000000000 ) ) ;
#67933=ORIENTED_EDGE ( 'NONE', *, *, #36971, .F. ) ;
#67944=EDGE_LOOP ( 'NONE', ( #4798, #12496, #69910, #39502 ) ) ;
#67945=ORIENTED_EDGE ( 'NONE', *, *, #17601, .F. ) ;
#67950=EDGE_CURVE ( 'NONE', #58159, #80349, #54374, .T. ) ;
#67952=ORIENTED_EDGE ( 'NONE', *, *, #7411, .F. ) ;
#67975=CYLINDRICAL_SURFACE ( 'NONE', #81651, 27.94799999999999685 ) ;
#67977=VECTOR ( 'NONE', #60467, 1000.000000000000000 ) ;
#67990=LINE ( 'NONE', #6073, #79818 ) ;
#68012=EDGE_CURVE ( 'NONE', #91984, #67600, #85215, .T. ) ;
#68017=LINE ( 'NONE', #29435, #22588 ) ;
#68040=PLANE ( 'NONE',  #72262 ) ;
#68042=ORIENTED_EDGE ( 'NONE', *, *, #27693, .F. ) ;
#68053=ORIENTED_EDGE ( 'NONE', *, *, #45998, .T. ) ;
#68057=CARTESIAN_POINT ( 'NONE',  ( 32.48725517365867432, 4.170878844625590887, -0.8993273505261454304 ) ) ;
#68064=VERTEX_POINT ( 'NONE', #86219 ) ;
#68096=ADVANCED_FACE ( 'NONE', ( #17708 ), #79095, .T. ) ;
#68102=VECTOR ( 'NONE', #58162, 1000.000000000000000 ) ;
#68108=EDGE_LOOP ( 'NONE', ( #58471, #9470, #45295, #20936, #47472 ) ) ;
#68121=FACE_OUTER_BOUND ( 'NONE', #7336, .T. ) ;
#68122=CARTESIAN_POINT ( 'NONE',  ( -28.98875734969026396, 6.376774720514426953, -0.08597719988137648983 ) ) ;
#68131=ORIENTED_EDGE ( 'NONE', *, *, #60145, .F. ) ;
#68133=CARTESIAN_POINT ( 'NONE',  ( 30.43908124610670285, -1.477225279485574028, -13.86910542224428866 ) ) ;
#68135=DIRECTION ( 'NONE',  ( 1.000000000000000000, -0.000000000000000000, -0.000000000000000000 ) ) ;
#68160=ORIENTED_EDGE ( 'NONE', *, *, #59124, .T. ) ;
#68171=ORIENTED_EDGE ( 'NONE', *, *, #100279, .F. ) ;
#68172=CARTESIAN_POINT ( 'NONE',  ( -28.98875734969026396, 0.3587747205144262708, 0.1180228001186258285 ) ) ;
#68179=ORIENTED_EDGE ( 'NONE', *, *, #42463, .T. ) ;
#68191=CARTESIAN_POINT ( 'NONE',  ( -25.92875734969025814, 3.316774720514426456, 0.7300228001186309656 ) ) ;
#68194=ORIENTED_EDGE ( 'NONE', *, *, #48287, .F. ) ;
#68202=CARTESIAN_POINT ( 'NONE',  ( 31.84105487026594261, 5.152774720514426754, -11.95870468328485003 ) ) ;
#68208=CYLINDRICAL_SURFACE ( 'NONE', #61734, 0.8160000000000007248 ) ;
#68220=EDGE_CURVE ( 'NONE', #26340, #95272, #58281, .T. ) ;
#68233=CARTESIAN_POINT ( 'NONE',  ( 5.949073730962466833, -6.475225279485573360, -27.94053387008862188 ) ) ;
#68234=PLANE ( 'NONE',  #79652 ) ;
#68250=ORIENTED_EDGE ( 'NONE', *, *, #76942, .T. ) ;
#68253=CARTESIAN_POINT ( 'NONE',  ( -28.47875734969026240, -6.475225279485573360, 26.43402280011862615 ) ) ;
#68274=ORIENTED_EDGE ( 'NONE', *, *, #100279, .T. ) ;
#68276=CARTESIAN_POINT ( 'NONE',  ( 22.74089357256066535, 1.682774720514426114, -19.20396252371061863 ) ) ;
#68279=VERTEX_POINT ( 'NONE', #5474 ) ;
#68281=ORIENTED_EDGE ( 'NONE', *, *, #47680, .F. ) ;
#68311=ORIENTED_EDGE ( 'NONE', *, *, #68744, .F. ) ;
#68316=CIRCLE ( 'NONE', #82923, 130.7884398600581335 ) ;
#68317=VERTEX_POINT ( 'NONE', #36421 ) ;
#68327=EDGE_CURVE ( 'NONE', #654, #56438, #5834, .T. ) ;
#68329=ORIENTED_EDGE ( 'NONE', *, *, #59066, .T. ) ;
#68365=CARTESIAN_POINT ( 'NONE',  ( 3.509873074917118085, -5.965225279485572685, 29.15869884040363758 ) ) ;
#68368=CIRCLE ( 'NONE', #87848, 1.699999999999996625 ) ;
#68378=EDGE_CURVE ( 'NONE', #79832, #60562, #52650, .T. ) ;
#68386=CARTESIAN_POINT ( 'NONE',  ( 0.000000000000000000, 5.356774720514425603, 0.000000000000000000 ) ) ;
#68388=ADVANCED_FACE ( 'NONE', ( #30301 ), #71906, .T. ) ;
#68396=ORIENTED_EDGE ( 'NONE', *, *, #32985, .T. ) ;
#68411=ORIENTED_EDGE ( 'NONE', *, *, #46789, .T. ) ;
#68416=CARTESIAN_POINT ( 'NONE',  ( -28.98875734969026396, -5.965225279485572685, -0.08597719988137648983 ) ) ;
#68443=CARTESIAN_POINT ( 'NONE',  ( -65.05438548721848235, 6.376774720514426953, 0.7300228001186309656 ) ) ;
#68450=ADVANCED_FACE ( 'NONE', ( #26197 ), #40428, .F. ) ;
#68451=ORIENTED_EDGE ( 'NONE', *, *, #82074, .F. ) ;
#68455=ADVANCED_FACE ( 'NONE', ( #63281 ), #88107, .F. ) ;
#68475=LINE ( 'NONE', #60381, #436 ) ;
#68481=DIRECTION ( 'NONE',  ( -0.9496245541219264785, -6.845827386180410961E-16, -0.3133898629642195011 ) ) ;
#68483=ORIENTED_EDGE ( 'NONE', *, *, #28257, .F. ) ;
#68491=CARTESIAN_POINT ( 'NONE',  ( 30.56234178131493451, -2.630409229859051568, 24.79707536756607666 ) ) ;
#68504=CARTESIAN_POINT ( 'NONE',  ( -12.84880425037203011, -5.965225279485592225, -26.59900746623528534 ) ) ;
#68507=DIRECTION ( 'NONE',  ( -0.000000000000000000, -1.000000000000000000, -0.000000000000000000 ) ) ;
#68532=VERTEX_POINT ( 'NONE', #10466 ) ;
#68534=AXIS2_PLACEMENT_3D ( 'NONE', #65337, #11508, #74895 ) ;
#68536=DIRECTION ( 'NONE',  ( -0.000000000000000000, -1.000000000000000000, -0.000000000000000000 ) ) ;
#68546=PLANE ( 'NONE',  #31254 ) ;
#68550=DIRECTION ( 'NONE',  ( 0.000000000000000000, -1.000000000000000000, 0.000000000000000000 ) ) ;
#68570=AXIS2_PLACEMENT_3D ( 'NONE', #69233, #52023, #5839 ) ;
#68596=CARTESIAN_POINT ( 'NONE',  ( 8.159923944623203695, 3.316774720514428232, -28.14238247154670347 ) ) ;
#68617=LINE ( 'NONE', #55403, #44509 ) ;
#68654=ORIENTED_EDGE ( 'NONE', *, *, #92154, .T. ) ;
#68656=DIRECTION ( 'NONE',  ( 0.000000000000000000, 0.000000000000000000, 1.000000000000000000 ) ) ;
#68660=ORIENTED_EDGE ( 'NONE', *, *, #38133, .F. ) ;
#68667=CARTESIAN_POINT ( 'NONE',  ( 30.45304879119406039, 4.772774720514425972, -10.07140455160086212 ) ) ;
#68677=EDGE_LOOP ( 'NONE', ( #21126, #61069, #32203, #34592 ) ) ;
#68679=FACE_OUTER_BOUND ( 'NONE', #85017, .T. ) ;
#68692=DIRECTION ( 'NONE',  ( 0.000000000000000000, -1.000000000000000000, 0.000000000000000000 ) ) ;
#68695=ORIENTED_EDGE ( 'NONE', *, *, #70865, .T. ) ;
#68712=CIRCLE ( 'NONE', #24943, 1.835999999999983423 ) ;
#68744=EDGE_CURVE ( 'NONE', #40707, #43478, #7497, .T. ) ;
#68749=CARTESIAN_POINT ( 'NONE',  ( 30.45304879119406039, -1.477225279485574028, -10.07140455160086390 ) ) ;
#68760=LINE ( 'NONE', #14457, #12324 ) ;
#68787=CARTESIAN_POINT ( 'NONE',  ( 13.87573923102662121, 3.316774720514425123, -28.27006591627376508 ) ) ;
#68792=ORIENTED_EDGE ( 'NONE', *, *, #30567, .T. ) ;
#68793=CARTESIAN_POINT ( 'NONE',  ( 2.449489742783179214, -1.473225279485573358, 2.499999999999999112 ) ) ;
#68801=ORIENTED_EDGE ( 'NONE', *, *, #28977, .T. ) ;
#68815=ORIENTED_EDGE ( 'NONE', *, *, #58597, .F. ) ;
#68822=FACE_OUTER_BOUND ( 'NONE', #30096, .T. ) ;
#68827=VERTEX_POINT ( 'NONE', #13453 ) ;
#68833=ADVANCED_FACE ( 'NONE', ( #29686 ), #44428, .T. ) ;
#68852=DIRECTION ( 'NONE',  ( -0.09721092304694051167, 0.000000000000000000, 0.9952638024365005887 ) ) ;
#68870=CARTESIAN_POINT ( 'NONE',  ( 33.00535138976610483, -5.965225279485572685, -12.97242311383961066 ) ) ;
#68898=EDGE_CURVE ( 'NONE', #44666, #56810, #2749, .T. ) ;
#68900=ADVANCED_FACE ( 'NONE', ( #8845 ), #85460, .T. ) ;
#68907=CARTESIAN_POINT ( 'NONE',  ( -20.27875734969026311, 3.456774720514426136, 24.00402280011862288 ) ) ;
#68913=FACE_OUTER_BOUND ( 'NONE', #42709, .T. ) ;
#68922=DIRECTION ( 'NONE',  ( 0.000000000000000000, 0.000000000000000000, 1.000000000000000000 ) ) ;
#68929=EDGE_CURVE ( 'NONE', #43843, #79545, #35040, .T. ) ;
#68931=ORIENTED_EDGE ( 'NONE', *, *, #33554, .F. ) ;
#68966=ORIENTED_EDGE ( 'NONE', *, *, #16436, .T. ) ;
#68979=B_SPLINE_CURVE_WITH_KNOTS ( 'NONE', 3,
 ( #34110, #94494, #49848, #33601, #40215, #72672, #1658, #33101, #71168, #41222, #3171, #64585, #32595, #71670, #2168, #65083, #94994, #11262 ),
 .UNSPECIFIED., .F., .F.,
 ( 4, 2, 2, 2, 2, 2, 2, 2, 4 ),
 ( 0.000000000000000000, 0.0005980878512858794297, 0.001196175702571757558, 0.001794263553857635470, 0.002392351405143513382, 0.002990439256429391728, 0.003588527107715270073, 0.004186614959001148419, 0.004784702810287026764 ),
 .UNSPECIFIED. ) ;
#68994=DIRECTION ( 'NONE',  ( 0.000000000000000000, 0.000000000000000000, -1.000000000000000000 ) ) ;
#69002=CARTESIAN_POINT ( 'NONE',  ( 32.90495245295455362, 3.622774720514437607, -13.06061886496134861 ) ) ;
#69021=EDGE_LOOP ( 'NONE', ( #91021, #20939, #87385 ) ) ;
#69025=ORIENTED_EDGE ( 'NONE', *, *, #88517, .F. ) ;
#69041=CARTESIAN_POINT ( 'NONE',  ( 11.62916340711181284, -5.965225279485572685, 28.75961759920349792 ) ) ;
#69044=ORIENTED_EDGE ( 'NONE', *, *, #17015, .F. ) ;
#69074=VERTEX_POINT ( 'NONE', #49430 ) ;
#69079=VERTEX_POINT ( 'NONE', #58531 ) ;
#69082=VECTOR ( 'NONE', #13032, 1000.000000000000227 ) ;
#69086=CARTESIAN_POINT ( 'NONE',  ( 11.32485880260453293, 6.376774720514427841, -25.00877359051251148 ) ) ;
#69092=DIRECTION ( 'NONE',  ( 0.000000000000000000, 1.000000000000000000, 0.000000000000000000 ) ) ;
#69103=DIRECTION ( 'NONE',  ( -0.6599726524652340665, -3.117967031984456719E-15, 0.7512896232465900992 ) ) ;
#69118=LINE ( 'NONE', #45792, #3141 ) ;
#69134=ORIENTED_EDGE ( 'NONE', *, *, #26470, .T. ) ;
#69136=VERTEX_POINT ( 'NONE', #41816 ) ;
#69142=PLANE ( 'NONE',  #29183 ) ;
#69143=DIRECTION ( 'NONE',  ( -0.000000000000000000, -1.000000000000000000, 0.000000000000000000 ) ) ;
#69159=VECTOR ( 'NONE', #56869, 1000.000000000000000 ) ;
#69178=CARTESIAN_POINT ( 'NONE',  ( 26.29980976416808858, 5.126432557820720604, -7.297634155824876956 ) ) ;
#69179=CYLINDRICAL_SURFACE ( 'NONE', #52408, 1.836000000000000743 ) ;
#69180=EDGE_CURVE ( 'NONE', #88744, #33854, #36319, .T. ) ;
#69193=EDGE_CURVE ( 'NONE', #71418, #22347, #21542, .T. ) ;
#69201=EDGE_CURVE ( 'NONE', #40087, #35826, #69118, .T. ) ;
#69202=ORIENTED_EDGE ( 'NONE', *, *, #82531, .T. ) ;
#69219=PLANE ( 'NONE',  #87986 ) ;
#69223=( BOUNDED_SURFACE ( )  B_SPLINE_SURFACE ( 3, 2, ( 
 ( #18079, #79975, #82961 ),
 ( #89591, #43918, #60157 ),
 ( #67266, #28192, #36804 ),
 ( #67765, #4854, #36307 ),
 ( #13450, #29683, #97199 ),
 ( #13949, #20072, #75848 ),
 ( #11960, #51035, #59653 ),
 ( #28689, #20565, #37305 ),
 ( #43429, #91080, #81978 ),
 ( #90584, #44926, #27698 ),
 ( #29182, #35806, #98687 ),
 ( #59149, #12460, #6346 ) ),
 .UNSPECIFIED., .F., .F., .T. ) 
 B_SPLINE_SURFACE_WITH_KNOTS ( ( 4, 2, 2, 2, 2, 4 ),
 ( 3, 3 ),
 ( 5.963111948670274387E-19, 0.0004805055694112242209, 0.0007207583541168360603, 0.0009610111388224478997, 0.001441516708233671470, 0.001922022277644895149 ),
 ( 0.000000000000000000, 1.000000000000000000 ),
 .UNSPECIFIED. ) 
 GEOMETRIC_REPRESENTATION_ITEM ( )  RATIONAL_B_SPLINE_SURFACE ( (
 ( 1.000000000000000000, 0.6532382444175209857, 1.000000000000000000),
 ( 1.000000000000000000, 0.6532227097440629349, 1.000000000000000000),
 ( 1.000000000000000000, 0.6547852517831300734, 1.000000000000000000),
 ( 1.000000000000000000, 0.6591574828660964336, 1.000000000000000000),
 ( 1.000000000000000000, 0.6609310395923762016, 1.000000000000000000),
 ( 1.000000000000000000, 0.6650742797340818413, 1.000000000000000000),
 ( 1.000000000000000000, 0.6674600455423553846, 1.000000000000000000),
 ( 1.000000000000000000, 0.6751670852230186037, 1.000000000000000000),
 ( 1.000000000000000000, 0.6812390391297645786, 1.000000000000000000),
 ( 1.000000000000000000, 0.6938890553660238547, 1.000000000000000000),
 ( 1.000000000000000000, 0.7006220437376451393, 1.000000000000000000),
 ( 1.000000000000000000, 0.7071067811865475727, 1.000000000000000000) ) ) 
 REPRESENTATION_ITEM ( '' )  SURFACE ( )  );
#69233=CARTESIAN_POINT ( 'NONE',  ( 22.02124265030973760, -4.543225279485573864, 16.20402280011862217 ) ) ;
#69235=CIRCLE ( 'NONE', #20634, 129.7684398600581517 ) ;
#69248=VECTOR ( 'NONE', #63227, 1000.000000000000000 ) ;
#69261=ADVANCED_FACE ( 'NONE', ( #83844 ), #99549, .F. ) ;
#69263=DIRECTION ( 'NONE',  ( 0.7512896232465892110, -0.000000000000000000, 0.6599726524652350657 ) ) ;
#69266=DIRECTION ( 'NONE',  ( 0.000000000000000000, 1.000000000000000000, 0.000000000000000000 ) ) ;
#69299=CARTESIAN_POINT ( 'NONE',  ( -29.49875734969026198, -5.965225279485572685, 0.1180228001186258285 ) ) ;
#69303=ORIENTED_EDGE ( 'NONE', *, *, #57370, .T. ) ;
#69307=VECTOR ( 'NONE', #57846, 1000.000000000000000 ) ;
#69313=EDGE_CURVE ( 'NONE', #43106, #26765, #82580, .T. ) ;
#69317=FACE_OUTER_BOUND ( 'NONE', #29579, .T. ) ;
#69319=ORIENTED_EDGE ( 'NONE', *, *, #60001, .T. ) ;
#69355=AXIS2_PLACEMENT_3D ( 'NONE', #53519, #84442, #7311 ) ;
#69371=CARTESIAN_POINT ( 'NONE',  ( 31.29611288755342002, 5.755914996345237178, -2.011851919325042370 ) ) ;
#69379=VERTEX_POINT ( 'NONE', #22916 ) ;
#69393=ORIENTED_EDGE ( 'NONE', *, *, #96172, .F. ) ;
#69401=DIRECTION ( 'NONE',  ( 1.000000000000000000, -0.000000000000000000, -0.000000000000000000 ) ) ;
#69403=DIRECTION ( 'NONE',  ( -1.000000000000000000, -0.000000000000000000, -0.000000000000000000 ) ) ;
#69405=B_SPLINE_CURVE_WITH_KNOTS ( 'NONE', 3,
 ( #99390, #37500, #28888, #7547, #44120, #75048, #15155, #83163, #5544, #69450, #52729, #91286, #21756, #92277, #23258, #45619 ),
 .UNSPECIFIED., .F., .F.,
 ( 4, 2, 2, 2, 2, 2, 2, 4 ),
 ( 0.000000000000000000, 0.0004662014769087530121, 0.0009324029538175060243, 0.001398604430726259036, 0.001864805907635012049, 0.002331007384543765278, 0.002797208861452518073, 0.003729611815270027567 ),
 .UNSPECIFIED. ) ;
#69417=DIRECTION ( 'NONE',  ( 0.000000000000000000, 0.000000000000000000, -1.000000000000000000 ) ) ;
#69436=EDGE_CURVE ( 'NONE', #96941, #50118, #20928, .T. ) ;
#69441=DIRECTION ( 'NONE',  ( 0.000000000000000000, 0.000000000000000000, -1.000000000000000000 ) ) ;
#69445=DIRECTION ( 'NONE',  ( -0.9872275723272646575, 0.000000000000000000, -0.1593164160933058515 ) ) ;
#69450=CARTESIAN_POINT ( 'NONE',  ( 12.36220485508518685, 4.378682769551595300, -27.78718873729292582 ) ) ;
#69484=B_SPLINE_CURVE_WITH_KNOTS ( 'NONE', 3,
 ( #11234, #42702, #81744, #66555, #73637, #80246, #10739, #65054, #18841, #20323, #50307, #26469, #57433, #42211, #65551 ),
 .UNSPECIFIED., .F., .F.,
 ( 4, 2, 2, 2, 1, 2, 2, 4 ),
 ( 0.000000000000000000, 0.2500000000000124900, 0.3750000000000185962, 0.4375000000000195954, 0.4687500000000199285, 0.4843750000000200950, 0.5000000000000202061, 1.000000000000000000 ),
 .UNSPECIFIED. ) ;
#69497=ADVANCED_FACE ( 'NONE', ( #70626 ), #47295, .F. ) ;
#69503=ORIENTED_EDGE ( 'NONE', *, *, #41772, .T. ) ;
#69508=ADVANCED_FACE ( 'NONE', ( #15825 ), #27150, .T. ) ;
#69511=EDGE_CURVE ( 'NONE', #41503, #55229, #37164, .T. ) ;
#69539=AXIS2_PLACEMENT_3D ( 'NONE', #13150, #53237, #44121 ) ;
#69551=ORIENTED_EDGE ( 'NONE', *, *, #5950, .F. ) ;
#69552=PLANE ( 'NONE',  #76049 ) ;
#69563=VECTOR ( 'NONE', #27076, 1000.000000000000000 ) ;
#69589=DIRECTION ( 'NONE',  ( 1.046287966022745640E-14, 0.000000000000000000, -1.000000000000000000 ) ) ;
#69611=DIRECTION ( 'NONE',  ( 0.000000000000000000, 0.000000000000000000, -1.000000000000000000 ) ) ;
#69617=AXIS2_PLACEMENT_3D ( 'NONE', #42732, #58945, #35110 ) ;
#69633=CARTESIAN_POINT ( 'NONE',  ( 31.63505726983280297, 3.634951944882593988, 27.30823744647568674 ) ) ;
#69645=EDGE_LOOP ( 'NONE', ( #100117, #14343, #92139, #62082, #80767, #40328, #4445, #68131 ) ) ;
#69659=ORIENTED_EDGE ( 'NONE', *, *, #16430, .T. ) ;
#69661=DIRECTION ( 'NONE',  ( 0.9921023176230514551, 0.000000000000000000, -0.1254312216594016816 ) ) ;
#69680=CARTESIAN_POINT ( 'NONE',  ( 26.37445894957760828, 2.682774720514426559, -11.69480419648520986 ) ) ;
#69699=CARTESIAN_POINT ( 'NONE',  ( 33.25738712673413033, 4.772289986317655774, -12.75102155484566424 ) ) ;
#69700=AXIS2_PLACEMENT_3D ( 'NONE', #93891, #33496, #8160 ) ;
#69745=ORIENTED_EDGE ( 'NONE', *, *, #84953, .T. ) ;
#69752=ORIENTED_EDGE ( 'NONE', *, *, #67379, .T. ) ;
#69759=DIRECTION ( 'NONE',  ( 0.000000000000000000, 1.000000000000000000, 0.000000000000000000 ) ) ;
#69767=VECTOR ( 'NONE', #35525, 1000.000000000000000 ) ;
#69769=CARTESIAN_POINT ( 'NONE',  ( 25.61870917940689196, 0.3587747205144265483, 28.79814474876424768 ) ) ;
#69778=DIRECTION ( 'NONE',  ( 0.000000000000000000, 1.000000000000000000, 0.000000000000000000 ) ) ;
#69789=EDGE_LOOP ( 'NONE', ( #69025, #28642, #31948 ) ) ;
#69790=CARTESIAN_POINT ( 'NONE',  ( -29.49875734969025842, 0.3587747205144265483, 25.61802280011862720 ) ) ;
#69809=ORIENTED_EDGE ( 'NONE', *, *, #58645, .T. ) ;
#69824=ORIENTED_EDGE ( 'NONE', *, *, #94097, .F. ) ;
#69828=FACE_OUTER_BOUND ( 'NONE', #92967, .T. ) ;
#69851=DIRECTION ( 'NONE',  ( -0.000000000000000000, -1.000000000000000000, -0.000000000000000000 ) ) ;
#69852=VERTEX_POINT ( 'NONE', #89616 ) ;
#69864=DIRECTION ( 'NONE',  ( 0.000000000000000000, 0.000000000000000000, -1.000000000000000000 ) ) ;
#69872=CARTESIAN_POINT ( 'NONE',  ( 30.79432203307449711, 6.272817126675294119, 0.6151397435758989563 ) ) ;
#69881=CARTESIAN_POINT ( 'NONE',  ( 27.53860345374808105, 1.682774720514426114, -1.352392034746782823 ) ) ;
#69886=DIRECTION ( 'NONE',  ( -0.000000000000000000, 1.000000000000000000, -0.000000000000000000 ) ) ;
#69888=LINE ( 'NONE', #54674, #88144 ) ;
#69892=ORIENTED_EDGE ( 'NONE', *, *, #20780, .F. ) ;
#69902=VECTOR ( 'NONE', #23015, 1000.000000000000000 ) ;
#69906=ORIENTED_EDGE ( 'NONE', *, *, #88724, .T. ) ;
#69910=ORIENTED_EDGE ( 'NONE', *, *, #28634, .F. ) ;
#69930=AXIS2_PLACEMENT_3D ( 'NONE', #48229, #68692, #7271 ) ;
#69981=EDGE_LOOP ( 'NONE', ( #85705, #76417, #58446, #20147 ) ) ;
#69983=DIRECTION ( 'NONE',  ( 0.000000000000000000, 0.000000000000000000, -1.000000000000000000 ) ) ;
#69991=DIRECTION ( 'NONE',  ( -0.8264557562326033668, 0.000000000000000000, -0.5630016722799281448 ) ) ;
#69997=LINE ( 'NONE', #62397, #23463 ) ;
#70004=DIRECTION ( 'NONE',  ( 0.000000000000000000, 1.000000000000000000, -0.000000000000000000 ) ) ;
#70008=ORIENTED_EDGE ( 'NONE', *, *, #65735, .F. ) ;
#70016=ORIENTED_EDGE ( 'NONE', *, *, #75936, .T. ) ;
#70024=EDGE_LOOP ( 'NONE', ( #11267, #49207 ) ) ;
#70040=ADVANCED_FACE ( 'NONE', ( #39311 ), #84985, .F. ) ;
#70042=DIRECTION ( 'NONE',  ( -0.000000000000000000, 1.000000000000000000, -0.000000000000000000 ) ) ;
#70059=VERTEX_POINT ( 'NONE', #30197 ) ;
#70062=DIRECTION ( 'NONE',  ( 0.6599726524652352877, -0.000000000000000000, -0.7512896232465891000 ) ) ;
#70078=VERTEX_POINT ( 'NONE', #46933 ) ;
#70101=CARTESIAN_POINT ( 'NONE',  ( 17.47419131657910185, 0.3587747205144265483, 28.31804950686278843 ) ) ;
#70102=CARTESIAN_POINT ( 'NONE',  ( -29.49875734969026198, -5.965225279485572685, 2.362022800118626531 ) ) ;
#70120=VECTOR ( 'NONE', #79078, 1000.000000000000000 ) ;
#70122=ORIENTED_EDGE ( 'NONE', *, *, #73868, .F. ) ;
#70143=ORIENTED_EDGE ( 'NONE', *, *, #32964, .F. ) ;
#70155=EDGE_CURVE ( 'NONE', #98626, #6678, #78362, .T. ) ;
#70159=ORIENTED_EDGE ( 'NONE', *, *, #22832, .F. ) ;
#70165=DIRECTION ( 'NONE',  ( 0.000000000000000000, -0.000000000000000000, -1.000000000000000000 ) ) ;
#70179=FACE_OUTER_BOUND ( 'NONE', #54678, .T. ) ;
#70188=DIRECTION ( 'NONE',  ( 0.000000000000000000, 0.000000000000000000, -1.000000000000000000 ) ) ;
#70198=ORIENTED_EDGE ( 'NONE', *, *, #39000, .F. ) ;
#70201=AXIS2_PLACEMENT_3D ( 'NONE', #43962, #57703, #96749 ) ;
#70205=EDGE_CURVE ( 'NONE', #51748, #82017, #6458, .T. ) ;
#70230=CARTESIAN_POINT ( 'NONE',  ( 25.83488407601164383, 2.682774720514426559, -11.31196583263649558 ) ) ;
#70247=CARTESIAN_POINT ( 'NONE',  ( -2.701720430790311767, -5.965225279485594001, -28.90526747363640681 ) ) ;
#70251=LINE ( 'NONE', #31687, #66301 ) ;
#70261=LINE ( 'NONE', #78356, #62472 ) ;
#70272=EDGE_CURVE ( 'NONE', #82699, #47065, #89987, .T. ) ;
#70295=ORIENTED_EDGE ( 'NONE', *, *, #52113, .T. ) ;
#70303=CARTESIAN_POINT ( 'NONE',  ( 22.81105451610979173, 4.772774720514425972, -18.46691820600746681 ) ) ;
#70319=CARTESIAN_POINT ( 'NONE',  ( 30.76755528059973699, 5.112846897994304918, -0.3209731499738198157 ) ) ;
#70327=DIRECTION ( 'NONE',  ( 0.000000000000000000, -1.000000000000000000, 0.000000000000000000 ) ) ;
#70332=ADVANCED_FACE ( 'NONE', ( #67664 ), #91471, .F. ) ;
#70369=DIRECTION ( 'NONE',  ( 0.000000000000000000, -1.000000000000000000, 0.000000000000000000 ) ) ;
#70404=CARTESIAN_POINT ( 'NONE',  ( 29.71608694565284026, 4.561299274004467996, 27.78615310300602559 ) ) ;
#70412=CARTESIAN_POINT ( 'NONE',  ( 15.11782173391118889, 3.530785491095175921, -28.35562479723308016 ) ) ;
#70423=ORIENTED_EDGE ( 'NONE', *, *, #30203, .F. ) ;
#70425=DIRECTION ( 'NONE',  ( 0.000000000000000000, -1.478457507934778393E-16, -1.000000000000000000 ) ) ;
#70430=DIRECTION ( 'NONE',  ( -0.000000000000000000, 1.000000000000000000, -0.000000000000000000 ) ) ;
#70434=FACE_OUTER_BOUND ( 'NONE', #99594, .T. ) ;
#70436=ORIENTED_EDGE ( 'NONE', *, *, #18400, .T. ) ;
#70447=CARTESIAN_POINT ( 'NONE',  ( 4.784292611718075072, 3.316774720514426456, -25.54547254883186014 ) ) ;
#70463=LINE ( 'NONE', #54749, #21154 ) ;
#70467=DIRECTION ( 'NONE',  ( -1.334402673828313093E-16, -0.000000000000000000, -1.000000000000000000 ) ) ;
#70468=CARTESIAN_POINT ( 'NONE',  ( 14.61581670307174008, 2.682774720514426559, -27.35847990810646024 ) ) ;
#70483=ORIENTED_EDGE ( 'NONE', *, *, #27693, .T. ) ;
#70502=VERTEX_POINT ( 'NONE', #15341 ) ;
#70507=VECTOR ( 'NONE', #16212, 1000.000000000000000 ) ;
#70519=DIRECTION ( 'NONE',  ( 0.000000000000000000, 1.000000000000000000, -0.000000000000000000 ) ) ;
#70546=VECTOR ( 'NONE', #85964, 1000.000000000000000 ) ;
#70552=ORIENTED_EDGE ( 'NONE', *, *, #64587, .T. ) ;
#70557=CARTESIAN_POINT ( 'NONE',  ( 32.85081302853804885, 3.622774720514426949, -13.10817780685210643 ) ) ;
#70561=CARTESIAN_POINT ( 'NONE',  ( 0.000000000000000000, 1.826774720514426464, 0.000000000000000000 ) ) ;
#70579=FACE_OUTER_BOUND ( 'NONE', #80445, .T. ) ;
#70581=CARTESIAN_POINT ( 'NONE',  ( 5.271800844963591359, 3.316774720514426011, -28.56638892015329034 ) ) ;
#70614=AXIS2_PLACEMENT_3D ( 'NONE', #99051, #6713, #37666 ) ;
#70618=CARTESIAN_POINT ( 'NONE',  ( 13.91401389203221406, 6.376774720514426953, 158.0376437107427137 ) ) ;
#70619=CARTESIAN_POINT ( 'NONE',  ( 30.93860345374796594, -2.297196155479622526, 24.67598410064775294 ) ) ;
#70626=FACE_OUTER_BOUND ( 'NONE', #627, .T. ) ;
#70636=DIRECTION ( 'NONE',  ( 0.6599726524652352877, -0.000000000000000000, -0.7512896232465891000 ) ) ;
#70637=EDGE_LOOP ( 'NONE', ( #99746, #13889, #47181, #63435 ) ) ;
#70638=LINE ( 'NONE', #92961, #18520 ) ;
#70644=AXIS2_PLACEMENT_3D ( 'NONE', #64602, #95516, #73190 ) ;
#70653=AXIS2_PLACEMENT_3D ( 'NONE', #78673, #2095, #25410 ) ;
#70659=AXIS2_PLACEMENT_3D ( 'NONE', #90587, #21065, #36807 ) ;
#70679=ORIENTED_EDGE ( 'NONE', *, *, #32754, .T. ) ;
#70684=ORIENTED_EDGE ( 'NONE', *, *, #73670, .F. ) ;
#70695=EDGE_CURVE ( 'NONE', #22271, #9985, #73647, .T. ) ;
#70735=EDGE_CURVE ( 'NONE', #22648, #82699, #98796, .T. ) ;
#70737=DIRECTION ( 'NONE',  ( 0.000000000000000000, 0.000000000000000000, -1.000000000000000000 ) ) ;
#70752=ORIENTED_EDGE ( 'NONE', *, *, #39000, .T. ) ;
#70762=DIRECTION ( 'NONE',  ( 0.000000000000000000, -1.000000000000000000, 0.000000000000000000 ) ) ;
#70765=LINE ( 'NONE', #63674, #4164 ) ;
#70795=VERTEX_POINT ( 'NONE', #45199 ) ;
#70797=ORIENTED_EDGE ( 'NONE', *, *, #77957, .T. ) ;
#70809=DIRECTION ( 'NONE',  ( 0.000000000000000000, 0.000000000000000000, 1.000000000000000000 ) ) ;
#70851=CARTESIAN_POINT ( 'NONE',  ( 30.53060340732035982, 5.115583282868248816, -0.7333795357140852067 ) ) ;
#70865=EDGE_CURVE ( 'NONE', #48435, #18228, #90694, .T. ) ;
#70879=CARTESIAN_POINT ( 'NONE',  ( 22.02124265030973760, -4.543225279485573864, 16.20402280011862217 ) ) ;
#70884=EDGE_LOOP ( 'NONE', ( #54935, #58880, #48112, #26702 ) ) ;
#70904=ORIENTED_EDGE ( 'NONE', *, *, #44919, .T. ) ;
#70922=AXIS2_PLACEMENT_3D ( 'NONE', #75190, #5684, #50380 ) ;
#70932=ORIENTED_EDGE ( 'NONE', *, *, #64240, .F. ) ;
#70972=CARTESIAN_POINT ( 'NONE',  ( -0.02075734969026423599, 3.316774720514426456, -29.05397719988137339 ) ) ;
#70985=CARTESIAN_POINT ( 'NONE',  ( -12.65407072091356433, -5.965225279485572685, -26.15404995688568590 ) ) ;
#71005=CARTESIAN_POINT ( 'NONE',  ( 10.86264265030973952, 0.3587747205144257157, -28.64597719988137570 ) ) ;
#71010=PLANE ( 'NONE',  #35656 ) ;
#71014=TOROIDAL_SURFACE ( 'NONE', #22375, 25.90800000000000125, 2.040000000000000036 ) ;
#71032=ORIENTED_EDGE ( 'NONE', *, *, #73194, .T. ) ;
#71040=ORIENTED_EDGE ( 'NONE', *, *, #20328, .F. ) ;
#71042=ORIENTED_EDGE ( 'NONE', *, *, #68220, .T. ) ;
#71056=ORIENTED_EDGE ( 'NONE', *, *, #59514, .T. ) ;
#71075=CARTESIAN_POINT ( 'NONE',  ( 32.16024265030974050, -5.965225279485572685, 16.27760796525321751 ) ) ;
#71090=PLANE ( 'NONE',  #96854 ) ;
#71104=VERTEX_POINT ( 'NONE', #75512 ) ;
#71109=ORIENTED_EDGE ( 'NONE', *, *, #20213, .T. ) ;
#71125=LINE ( 'NONE', #55407, #17261 ) ;
#71133=DIRECTION ( 'NONE',  ( 0.000000000000000000, 0.000000000000000000, -1.000000000000000000 ) ) ;
#71135=VECTOR ( 'NONE', #76383, 1000.000000000000000 ) ;
#71168=CARTESIAN_POINT ( 'NONE',  ( 29.62646972375975096, 5.339663449004302009, 28.46301402826327731 ) ) ;
#71212=AXIS2_PLACEMENT_3D ( 'NONE', #25097, #96612, #79388 ) ;
#71216=AXIS2_PLACEMENT_3D ( 'NONE', #67642, #98564, #38668 ) ;
#71219=EDGE_CURVE ( 'NONE', #62056, #61220, #42119, .T. ) ;
#71230=LINE ( 'NONE', #79327, #99195 ) ;
#71243=DIRECTION ( 'NONE',  ( 1.240248834241861717E-14, 0.000000000000000000, -1.000000000000000000 ) ) ;
#71246=VERTEX_POINT ( 'NONE', #16122 ) ;
#71249=ORIENTED_EDGE ( 'NONE', *, *, #4542, .T. ) ;
#71253=EDGE_LOOP ( 'NONE', ( #79667, #81921, #97620, #5275 ) ) ;
#71318=EDGE_CURVE ( 'NONE', #50557, #16956, #47025, .T. ) ;
#71319=FACE_OUTER_BOUND ( 'NONE', #23462, .T. ) ;
#71333=CARTESIAN_POINT ( 'NONE',  ( 30.09341516180546350, -1.477225279485574028, -11.39311774897855756 ) ) ;
#71341=CARTESIAN_POINT ( 'NONE',  ( 27.53860345374808105, -1.477225279485574028, 19.84760796525321780 ) ) ;
#71354=CARTESIAN_POINT ( 'NONE',  ( 30.53060340732036337, 5.297812262124996785, 1.539714685317421505 ) ) ;
#71360=DIRECTION ( 'NONE',  ( 0.000000000000000000, 0.000000000000000000, 1.000000000000000000 ) ) ;
#71385=DIRECTION ( 'NONE',  ( -0.5630016722799281448, 5.365801633547210331E-16, 0.8264557562326034779 ) ) ;
#71394=CARTESIAN_POINT ( 'NONE',  ( 32.74291612378888061, 3.662501476888925467, -3.918438066536008346 ) ) ;
#71402=ORIENTED_EDGE ( 'NONE', *, *, #91518, .T. ) ;
#71404=ORIENTED_EDGE ( 'NONE', *, *, #13604, .T. ) ;
#71411=DIRECTION ( 'NONE',  ( 0.000000000000000000, 0.000000000000000000, -1.000000000000000000 ) ) ;
#71418=VERTEX_POINT ( 'NONE', #73917 ) ;
#71426=CARTESIAN_POINT ( 'NONE',  ( 14.76093561896379214, -6.475225279485573360, -27.88148769130088667 ) ) ;
#71444=CIRCLE ( 'NONE', #27687, 28.96799999999999287 ) ;
#71446=AXIS2_PLACEMENT_3D ( 'NONE', #13234, #5631, #36577 ) ;
#71448=CYLINDRICAL_SURFACE ( 'NONE', #72577, 251.4258649670780699 ) ;
#71470=DIRECTION ( 'NONE',  ( -0.6392559695863496705, -6.845827386180411947E-16, -0.7689940216596069522 ) ) ;
#71471=DIRECTION ( 'NONE',  ( 0.000000000000000000, 0.000000000000000000, 1.000000000000000000 ) ) ;
#71481=LINE ( 'NONE', #15170, #39229 ) ;
#71482=CARTESIAN_POINT ( 'NONE',  ( 29.73860345376319003, 5.356471260711259674, 19.84760796525321780 ) ) ;
#71491=EDGE_CURVE ( 'NONE', #70059, #81022, #4939, .T. ) ;
#71500=CARTESIAN_POINT ( 'NONE',  ( 33.64270623324222953, 3.650451339955370855, -11.69061897474703571 ) ) ;
#71508=VECTOR ( 'NONE', #27169, 1000.000000000000114 ) ;
#71519=DIRECTION ( 'NONE',  ( 0.000000000000000000, -1.000000000000000000, 0.000000000000000000 ) ) ;
#71522=VERTEX_POINT ( 'NONE', #84879 ) ;
#71525=ORIENTED_EDGE ( 'NONE', *, *, #57305, .F. ) ;
#71535=ORIENTED_EDGE ( 'NONE', *, *, #75182, .T. ) ;
#71538=ORIENTED_EDGE ( 'NONE', *, *, #68378, .F. ) ;
#71546=ADVANCED_FACE ( 'NONE', ( #14862 ), #51585, .T. ) ;
#71556=LINE ( 'NONE', #40098, #95466 ) ;
#71578=LINE ( 'NONE', #19268, #40073 ) ;
#71596=DIRECTION ( 'NONE',  ( 0.000000000000000000, 1.000000000000000000, -0.000000000000000000 ) ) ;
#71597=PLANE ( 'NONE',  #70653 ) ;
#71599=B_SPLINE_CURVE_WITH_KNOTS ( 'NONE', 3,
 ( #50154, #82091, #88712, #12574, #35914, #12067, #51649, #81093, #90701, #43041, #74475, #98294, #66391, #73481 ),
 .UNSPECIFIED., .F., .F.,
 ( 4, 2, 2, 2, 2, 2, 4 ),
 ( 0.000000000000000000, 0.002392375077555367480, 0.003588562616333051004, 0.004784750155110734093, 0.005980937693888416749, 0.007177125232666099405, 0.009569500310221466452 ),
 .UNSPECIFIED. ) ;
#71639=DIRECTION ( 'NONE',  ( 0.000000000000000000, -0.000000000000000000, -1.000000000000000000 ) ) ;
#71641=VECTOR ( 'NONE', #28300, 1000.000000000000000 ) ;
#71651=ORIENTED_EDGE ( 'NONE', *, *, #11628, .F. ) ;
#71662=EDGE_CURVE ( 'NONE', #4955, #61510, #16892, .T. ) ;
#71670=CARTESIAN_POINT ( 'NONE',  ( 29.70917971445138051, 6.219445159570049064, 27.14760184111773356 ) ) ;
#71691=CARTESIAN_POINT ( 'NONE',  ( 26.14999174255633463, 4.132774720517320866, -11.56127575336603286 ) ) ;
#71701=CARTESIAN_POINT ( 'NONE',  ( 10.46399479596398052, 3.105441387181091972, -27.03001098546561920 ) ) ;
#71703=CARTESIAN_POINT ( 'NONE',  ( 29.73860345376318293, 4.772799050253824227, -4.021133283355260879 ) ) ;
#71710=CARTESIAN_POINT ( 'NONE',  ( 10.86264265030973952, 0.3587747205144257157, -27.62597719988137612 ) ) ;
#71711=EDGE_CURVE ( 'NONE', #11676, #34861, #40579, .T. ) ;
#71741=DIRECTION ( 'NONE',  ( 0.000000000000000000, 0.000000000000000000, -1.000000000000000000 ) ) ;
#71749=CIRCLE ( 'NONE', #31245, 10.20000000000000107 ) ;
#71759=VERTEX_POINT ( 'NONE', #28377 ) ;
#71761=CARTESIAN_POINT ( 'NONE',  ( -10.13340495651384288, 4.304508339349029988, 30.35717091805029355 ) ) ;
#71763=FACE_OUTER_BOUND ( 'NONE', #27340, .T. ) ;
#71770=ORIENTED_EDGE ( 'NONE', *, *, #38947, .T. ) ;
#71780=CARTESIAN_POINT ( 'NONE',  ( 26.73860345374794534, 1.682774720514426114, -1.352392034746782823 ) ) ;
#71787=CARTESIAN_POINT ( 'NONE',  ( -53.01255352321339842, 4.772774720514425972, 35.59556822165056644 ) ) ;
#71789=VECTOR ( 'NONE', #2608, 1000.000000000000000 ) ;
#71793=DIRECTION ( 'NONE',  ( 0.000000000000000000, 0.000000000000000000, 1.000000000000000000 ) ) ;
#71799=ORIENTED_EDGE ( 'NONE', *, *, #25862, .F. ) ;
#71820=ORIENTED_EDGE ( 'NONE', *, *, #78715, .F. ) ;
#71822=CYLINDRICAL_SURFACE ( 'NONE', #89619, 22.69500000000000384 ) ;
#71882=AXIS2_PLACEMENT_3D ( 'NONE', #39496, #79550, #2946 ) ;
#71897=B_SPLINE_CURVE_WITH_KNOTS ( 'NONE', 3,
 ( #62215, #16511, #70319, #91639, #61222, #46981 ),
 .UNSPECIFIED., .F., .F.,
 ( 4, 2, 4 ),
 ( 0.001731663773559584266, 0.004550964303235467343, 0.007370264832911350636 ),
 .UNSPECIFIED. ) ;
#71906=( BOUNDED_SURFACE ( )  B_SPLINE_SURFACE ( 3, 2, ( 
 ( #15079, #60278, #46046 ),
 ( #84090, #54165, #91203 ),
 ( #76465, #7459, #69872 ),
 ( #45049, #29305, #38418 ),
 ( #22676, #14071, #69371 ),
 ( #47044, #21676, #100290 ),
 ( #77959, #83586, #30808 ),
 ( #61774, #99312, #92692 ) ),
 .UNSPECIFIED., .F., .F., .T. ) 
 B_SPLINE_SURFACE_WITH_KNOTS ( ( 4, 2, 2, 4 ),
 ( 3, 3 ),
 ( 0.04217399329892001364, 0.04593451325143335651, 0.04781477322769002447, 0.04969503320394669937 ),
 ( 0.000000000000000000, 1.000000000000000000 ),
 .UNSPECIFIED. ) 
 GEOMETRIC_REPRESENTATION_ITEM ( )  RATIONAL_B_SPLINE_SURFACE ( (
 ( 1.000000000000000000, 0.7071067811865475727, 1.000000000000000000),
 ( 1.000000000000000000, 0.7337798844374378016, 1.000000000000000000),
 ( 1.000000000000000000, 0.7590275050786486899, 1.000000000000000000),
 ( 1.000000000000000000, 0.7948576648490734975, 1.000000000000000000),
 ( 1.000000000000000000, 0.8064603411375558251, 1.000000000000000000),
 ( 1.000000000000000000, 0.8289835611541060967, 1.000000000000000000),
 ( 1.000000000000000000, 0.8399042809640585583, 1.000000000000000000),
 ( 1.000000000000000000, 0.8504728678901986028, 1.000000000000000000) ) ) 
 REPRESENTATION_ITEM ( '' )  SURFACE ( )  );
#71907=ORIENTED_EDGE ( 'NONE', *, *, #17760, .F. ) ;
#71917=ORIENTED_EDGE ( 'NONE', *, *, #90033, .T. ) ;
#71927=ORIENTED_EDGE ( 'NONE', *, *, #40914, .T. ) ;
#71932=VERTEX_POINT ( 'NONE', #16148 ) ;
#71933=EDGE_CURVE ( 'NONE', #74167, #46180, #64875, .T. ) ;
#71939=CARTESIAN_POINT ( 'NONE',  ( -27.83739072329610664, -5.965225279485592225, -8.084349702057698650 ) ) ;
#71981=B_SPLINE_CURVE_WITH_KNOTS ( 'NONE', 3,
 ( #95918, #72098, #56381, #3584, #43140, #80196, #2583, #10687, #34025, #81697, #48762, #26412 ),
 .UNSPECIFIED., .F., .F.,
 ( 4, 2, 2, 2, 2, 4 ),
 ( 8.673617379884035472E-19, 0.002088620103345146476, 0.003132930155017719064, 0.004177240206690291217, 0.006265860310035430321, 0.008354480413380570292 ),
 .UNSPECIFIED. ) ;
#71985=CARTESIAN_POINT ( 'NONE',  ( 30.42805396430595977, 4.988345540211635232, 19.84760796525322135 ) ) ;
#72003=CARTESIAN_POINT ( 'NONE',  ( 30.57287095715005520, -6.475225279485573360, 25.41160796525322141 ) ) ;
#72011=ADVANCED_FACE ( 'NONE', ( #87166 ), #8544, .F. ) ;
#72032=CARTESIAN_POINT ( 'NONE',  ( -65.05438548721848235, -6.475225279485573360, 0.7300228001186309656 ) ) ;
#72037=CARTESIAN_POINT ( 'NONE',  ( -13.89275734969026388, -5.965225279485572685, 31.02402280011862246 ) ) ;
#72087=CYLINDRICAL_SURFACE ( 'NONE', #82996, 252.4458649670781085 ) ;
#72088=AXIS2_PLACEMENT_3D ( 'NONE', #91540, #43392, #28654 ) ;
#72098=CARTESIAN_POINT ( 'NONE',  ( 5.959527149828093506, 3.316774720514425567, -28.45540529974545407 ) ) ;
#72101=LINE ( 'NONE', #2586, #27757 ) ;
#72115=AXIS2_PLACEMENT_3D ( 'NONE', #73989, #4485, #35433 ) ;
#72117=DIRECTION ( 'NONE',  ( -0.9997753877537054468, 0.000000000000000000, 0.02119372647572819943 ) ) ;
#72143=CARTESIAN_POINT ( 'NONE',  ( 29.72095141006403196, 6.296447751620394939, 26.96056093718771152 ) ) ;
#72159=VERTEX_POINT ( 'NONE', #27766 ) ;
#72167=ORIENTED_EDGE ( 'NONE', *, *, #85601, .F. ) ;
#72175=FACE_OUTER_BOUND ( 'NONE', #95549, .T. ) ;
#72189=DIRECTION ( 'NONE',  ( 0.000000000000000000, -1.000000000000000000, 0.000000000000000000 ) ) ;
#72195=LINE ( 'NONE', #1175, #67060 ) ;
#72198=FACE_OUTER_BOUND ( 'NONE', #46372, .T. ) ;
#72202=B_SPLINE_CURVE_WITH_KNOTS ( 'NONE', 3,
 ( #60854, #92278, #90791, #22755, #76048, #90290 ),
 .UNSPECIFIED., .F., .F.,
 ( 4, 2, 4 ),
 ( 0.0005551796157830859177, 0.008843260483942988470, 0.01713134135210289330 ),
 .UNSPECIFIED. ) ;
#72212=CYLINDRICAL_SURFACE ( 'NONE', #77842, 27.94799999999999685 ) ;
#72213=CARTESIAN_POINT ( 'NONE',  ( 282.9764569301858046, 5.152774720514427642, 20.79159422840526616 ) ) ;
#72218=DIRECTION ( 'NONE',  ( -1.838928956454364527E-13, 0.000000000000000000, -1.000000000000000000 ) ) ;
#72231=ADVANCED_FACE ( 'NONE', ( #60725 ), #76414, .F. ) ;
#72236=ADVANCED_FACE ( 'NONE', ( #66846 ), #97768, .F. ) ;
#72250=CARTESIAN_POINT ( 'NONE',  ( 28.87399897812681004, -1.477225279485574028, -12.57761096169975445 ) ) ;
#72262=AXIS2_PLACEMENT_3D ( 'NONE', #91856, #7628, #22330 ) ;
#72265=ORIENTED_EDGE ( 'NONE', *, *, #46047, .F. ) ;
#72267=CARTESIAN_POINT ( 'NONE',  ( -10.14776687836540070, 4.675267808546679227, 30.20327419389746382 ) ) ;
#72283=CARTESIAN_POINT ( 'NONE',  ( 32.25249349869194759, -1.477225279485574028, -12.65342752644895263 ) ) ;
#72321=EDGE_LOOP ( 'NONE', ( #49323, #71042, #91249, #74502, #45848, #32242, #13495 ) ) ;
#72324=TOROIDAL_SURFACE ( 'NONE', #35023, 80.18232118519038920, 8.160000000000000142 ) ;
#72327=ORIENTED_EDGE ( 'NONE', *, *, #25735, .F. ) ;
#72331=VECTOR ( 'NONE', #37210, 1000.000000000000000 ) ;
#72334=VERTEX_POINT ( 'NONE', #53110 ) ;
#72339=AXIS2_PLACEMENT_3D ( 'NONE', #57781, #59778, #83080 ) ;
#72356=CARTESIAN_POINT ( 'NONE',  ( 32.45853543194704116, -5.965225279485572685, 9.169203677920338080 ) ) ;
#72360=CARTESIAN_POINT ( 'NONE',  ( 11.95416678406013489, 5.152774720514426754, -26.25966023343078248 ) ) ;
#72367=CARTESIAN_POINT ( 'NONE',  ( 0.000000000000000000, -16.94322527948557422, 0.000000000000000000 ) ) ;
#72397=VECTOR ( 'NONE', #37664, 1000.000000000000114 ) ;
#72415=ORIENTED_EDGE ( 'NONE', *, *, #37962, .T. ) ;
#72436=DIRECTION ( 'NONE',  ( -0.9496245541219264785, 0.000000000000000000, -0.3133898629642195011 ) ) ;
#72443=EDGE_LOOP ( 'NONE', ( #42795, #18854, #43006, #94761 ) ) ;
#72445=CARTESIAN_POINT ( 'NONE',  ( -24.90875734969025501, -5.965225279485572685, 30.51402280011862089 ) ) ;
#72457=DIRECTION ( 'NONE',  ( -0.2488812114211667037, -0.000000000000000000, -0.9685340172660599212 ) ) ;
#72466=DIRECTION ( 'NONE',  ( 0.000000000000000000, -1.000000000000000000, 0.000000000000000000 ) ) ;
#72478=AXIS2_PLACEMENT_3D ( 'NONE', #21010, #75296, #82908 ) ;
#72479=PLANE ( 'NONE',  #76521 ) ;
#72481=ADVANCED_FACE ( 'NONE', ( #69317 ), #8417, .T. ) ;
#72489=ORIENTED_EDGE ( 'NONE', *, *, #97653, .T. ) ;
#72493=FACE_OUTER_BOUND ( 'NONE', #42093, .T. ) ;
#72518=LINE ( 'NONE', #65425, #21674 ) ;
#72537=AXIS2_PLACEMENT_3D ( 'NONE', #15975, #15479, #92602 ) ;
#72558=ORIENTED_EDGE ( 'NONE', *, *, #36265, .T. ) ;
#72573=ORIENTED_EDGE ( 'NONE', *, *, #87761, .F. ) ;
#72575=DIRECTION ( 'NONE',  ( 0.000000000000000000, 0.000000000000000000, 1.000000000000000000 ) ) ;
#72577=AXIS2_PLACEMENT_3D ( 'NONE', #79035, #63850, #49616 ) ;
#72599=EDGE_CURVE ( 'NONE', #3035, #80243, #76259, .T. ) ;
#72605=CARTESIAN_POINT ( 'NONE',  ( 13.10664265030973930, -5.965225279485574461, -27.62597719988137612 ) ) ;
#72615=ORIENTED_EDGE ( 'NONE', *, *, #24387, .F. ) ;
#72616=CARTESIAN_POINT ( 'NONE',  ( 26.73860345374794178, 5.356774720514427379, -3.781275721883787355 ) ) ;
#72629=VECTOR ( 'NONE', #74343, 1000.000000000000000 ) ;
#72653=EDGE_LOOP ( 'NONE', ( #60182, #33145, #60096, #38072 ) ) ;
#72656=ORIENTED_EDGE ( 'NONE', *, *, #55821, .F. ) ;
#72669=CARTESIAN_POINT ( 'NONE',  ( 19.75748517575715368, -5.965225279485572685, 28.87153971905864580 ) ) ;
#72672=CARTESIAN_POINT ( 'NONE',  ( 29.59852343658945983, 4.673870278164355518, 28.90818992718861224 ) ) ;
#72695=EDGE_CURVE ( 'NONE', #91850, #63208, #22796, .T. ) ;
#72698=PLANE ( 'NONE',  #25391 ) ;
#72699=VECTOR ( 'NONE', #84703, 1000.000000000000114 ) ;
#72705=CARTESIAN_POINT ( 'NONE',  ( 22.81105451610979173, 2.682774720514426559, -18.46691820600746681 ) ) ;
#72711=EDGE_LOOP ( 'NONE', ( #37449, #8801, #12299, #8490 ) ) ;
#72714=CARTESIAN_POINT ( 'NONE',  ( 24.71017632900191074, 5.356774720514427379, 1.647607965253217399 ) ) ;
#72722=ADVANCED_FACE ( 'NONE', ( #21509 ), #68208, .F. ) ;
#72734=VECTOR ( 'NONE', #45176, 1000.000000000000000 ) ;
#72767=CARTESIAN_POINT ( 'NONE',  ( -10.12061615367207601, 3.718318319926830373, 30.49412484105965859 ) ) ;
#72788=CARTESIAN_POINT ( 'NONE',  ( 22.02124265030973760, 3.456774720514426136, 16.20402280011862217 ) ) ;
#72819=DIRECTION ( 'NONE',  ( 0.000000000000000000, 0.000000000000000000, -1.000000000000000000 ) ) ;
#72853=DIRECTION ( 'NONE',  ( 0.000000000000000000, -1.000000000000000000, 0.000000000000000000 ) ) ;
#72859=DIRECTION ( 'NONE',  ( 0.000000000000000000, 0.000000000000000000, -1.000000000000000000 ) ) ;
#72860=CARTESIAN_POINT ( 'NONE',  ( 14.78484767477523398, 5.152774720514430307, -28.43034250232788551 ) ) ;
#72861=CARTESIAN_POINT ( 'NONE',  ( 15.22325621495362391, 3.582999323269832725, -27.23549315679322547 ) ) ;
#72888=DIRECTION ( 'NONE',  ( -0.6392559695863502256, -6.454799914155189828E-16, -0.7689940216596065081 ) ) ;
#72911=CARTESIAN_POINT ( 'NONE',  ( 14.47945362154702664, 3.630796101029369005, -28.34983287945846087 ) ) ;
#72914=CARTESIAN_POINT ( 'NONE',  ( 22.81105451610979173, -1.477225279485574028, -18.46691820600746681 ) ) ;
#72927=DIRECTION ( 'NONE',  ( 0.000000000000000000, 0.000000000000000000, 1.000000000000000000 ) ) ;
#72944=EDGE_LOOP ( 'NONE', ( #38293, #97701, #48848, #26337, #49979 ) ) ;
#72945=ADVANCED_FACE ( 'NONE', ( #63611 ), #72212, .F. ) ;
#72952=VECTOR ( 'NONE', #61551, 1000.000000000000000 ) ;
#72959=PLANE ( 'NONE',  #9274 ) ;
#72964=VECTOR ( 'NONE', #88799, 1000.000000000000000 ) ;
#72983=CARTESIAN_POINT ( 'NONE',  ( 32.15269211224249091, 4.540774720514427543, 3.401810532325273417 ) ) ;
#73001=CARTESIAN_POINT ( 'NONE',  ( 33.61456970919608978, 3.316774720514426900, -11.35828564741662028 ) ) ;
#73011=CARTESIAN_POINT ( 'NONE',  ( 0.000000000000000000, -1.473225279485573802, 0.000000000000000000 ) ) ;
#73014=DIRECTION ( 'NONE',  ( 0.000000000000000000, -0.000000000000000000, -1.000000000000000000 ) ) ;
#73031=CARTESIAN_POINT ( 'NONE',  ( 15.92621150404962016, -6.475225279485573360, -27.29681269571043245 ) ) ;
#73043=CIRCLE ( 'NONE', #85984, 3.570000000000003837 ) ;
#73047=ORIENTED_EDGE ( 'NONE', *, *, #29367, .F. ) ;
#73105=CARTESIAN_POINT ( 'NONE',  ( 5.105333984060716368, 3.311071866383498374, -27.56005651598365347 ) ) ;
#73124=FACE_OUTER_BOUND ( 'NONE', #67944, .T. ) ;
#73137=VERTEX_POINT ( 'NONE', #36630 ) ;
#73139=CARTESIAN_POINT ( 'NONE',  ( 31.67047468188955150, 5.333900073052421753, 28.72484383265714314 ) ) ;
#73142=VERTEX_POINT ( 'NONE', #61481 ) ;
#73149=VECTOR ( 'NONE', #84563, 1000.000000000000000 ) ;
#73151=ORIENTED_EDGE ( 'NONE', *, *, #82188, .F. ) ;
#73158=ORIENTED_EDGE ( 'NONE', *, *, #92154, .F. ) ;
#73172=LINE ( 'NONE', #34610, #40429 ) ;
#73190=DIRECTION ( 'NONE',  ( 0.1875268396392987258, 0.000000000000000000, 0.9822594791677485837 ) ) ;
#73192=CARTESIAN_POINT ( 'NONE',  ( -24.90875734969025501, -5.965225279485572685, 30.00402280011862288 ) ) ;
#73194=EDGE_CURVE ( 'NONE', #4626, #14296, #55228, .T. ) ;
#73227=EDGE_LOOP ( 'NONE', ( #9615, #31227, #50691, #86887 ) ) ;
#73265=EDGE_CURVE ( 'NONE', #3225, #80003, #71444, .T. ) ;
#73272=FACE_OUTER_BOUND ( 'NONE', #52035, .T. ) ;
#73289=ADVANCED_FACE ( 'NONE', ( #25409, #11187, #17803 ), #64509, .F. ) ;
#73298=ADVANCED_FACE ( 'NONE', ( #25910 ), #87814, .F. ) ;
#73335=CARTESIAN_POINT ( 'NONE',  ( 5.109298100551870725, 5.356774720514425603, -27.55941679637891895 ) ) ;
#73343=CARTESIAN_POINT ( 'NONE',  ( 7.462166178408539352, -5.965225279485572685, -27.67315496249664974 ) ) ;
#73348=AXIS2_PLACEMENT_3D ( 'NONE', #54122, #15531, #10934 ) ;
#73353=CARTESIAN_POINT ( 'NONE',  ( 5.095029512766671154, 3.302735871364486098, -27.56177443937556859 ) ) ;
#73364=VECTOR ( 'NONE', #41273, 1000.000000000000000 ) ;
#73366=CARTESIAN_POINT ( 'NONE',  ( 15.30669619680802995, 3.489325088183165224, -28.51986054853846753 ) ) ;
#73369=DIRECTION ( 'NONE',  ( 0.000000000000000000, -1.000000000000000000, 0.000000000000000000 ) ) ;
#73383=AXIS2_PLACEMENT_3D ( 'NONE', #49275, #56887, #34533 ) ;
#73396=VECTOR ( 'NONE', #68481, 1000.000000000000000 ) ;
#73404=VERTEX_POINT ( 'NONE', #9179 ) ;
#73416=ORIENTED_EDGE ( 'NONE', *, *, #59058, .F. ) ;
#73431=CARTESIAN_POINT ( 'NONE',  ( 5.996070682796505125, 3.316774720514426900, -27.41631156547456882 ) ) ;
#73457=VECTOR ( 'NONE', #55387, 1000.000000000000000 ) ;
#73481=CARTESIAN_POINT ( 'NONE',  ( 14.61581670307174008, -6.475225279485573360, -27.35847990810646024 ) ) ;
#73487=EDGE_CURVE ( 'NONE', #24258, #92190, #55879, .T. ) ;
#73493=EDGE_CURVE ( 'NONE', #17738, #80017, #72101, .T. ) ;
#73498=VECTOR ( 'NONE', #2387, 1000.000000000000000 ) ;
#73509=FACE_OUTER_BOUND ( 'NONE', #3053, .T. ) ;
#73524=DIRECTION ( 'NONE',  ( 0.000000000000000000, 0.000000000000000000, -1.000000000000000000 ) ) ;
#73537=CARTESIAN_POINT ( 'NONE',  ( 29.80070917940689768, 3.316774720514426456, 27.39560796525317343 ) ) ;
#73539=VECTOR ( 'NONE', #95792, 1000.000000000000114 ) ;
#73576=AXIS2_PLACEMENT_3D ( 'NONE', #80378, #4258, #74748 ) ;
#73599=PLANE ( 'NONE',  #59406 ) ;
#73603=ORIENTED_EDGE ( 'NONE', *, *, #21348, .T. ) ;
#73605=CARTESIAN_POINT ( 'NONE',  ( 12.46200043076872888, 4.205547148226783882, -28.02060279727989922 ) ) ;
#73615=ADVANCED_FACE ( 'NONE', ( #66504 ), #36510, .F. ) ;
#73620=LINE ( 'NONE', #37049, #96366 ) ;
#73637=CARTESIAN_POINT ( 'NONE',  ( 15.14729487507453243, 3.547625430422813420, -27.26914648819303721 ) ) ;
#73643=ORIENTED_EDGE ( 'NONE', *, *, #46484, .F. ) ;
#73647=LINE ( 'NONE', #11246, #29123 ) ;
#73656=ORIENTED_EDGE ( 'NONE', *, *, #91967, .T. ) ;
#73667=ORIENTED_EDGE ( 'NONE', *, *, #77957, .F. ) ;
#73670=EDGE_CURVE ( 'NONE', #78496, #21581, #44634, .T. ) ;
#73671=ORIENTED_EDGE ( 'NONE', *, *, #70695, .T. ) ;
#73674=DIRECTION ( 'NONE',  ( 0.000000000000000000, 0.000000000000000000, -1.000000000000000000 ) ) ;
#73686=CARTESIAN_POINT ( 'NONE',  ( 5.271800844963591359, 3.316774720514426456, -28.56638892015329034 ) ) ;
#73693=AXIS2_PLACEMENT_3D ( 'NONE', #61273, #99309, #45045 ) ;
#73703=AXIS2_PLACEMENT_3D ( 'NONE', #4418, #95757, #97255 ) ;
#73705=EDGE_CURVE ( 'NONE', #43884, #44101, #23647, .T. ) ;
#73715=CARTESIAN_POINT ( 'NONE',  ( 30.61643171304413613, -6.475225279485573360, 27.37433008668288181 ) ) ;
#73756=CARTESIAN_POINT ( 'NONE',  ( 8.443068886831737174, 5.148414450533975284, -25.96590744588278454 ) ) ;
#73758=DIRECTION ( 'NONE',  ( -0.000000000000000000, -1.000000000000000000, -0.000000000000000000 ) ) ;
#73804=ORIENTED_EDGE ( 'NONE', *, *, #21257, .T. ) ;
#73806=ORIENTED_EDGE ( 'NONE', *, *, #39555, .F. ) ;
#73812=CARTESIAN_POINT ( 'NONE',  ( 31.48454476783385658, 4.132774720514426292, -1.134026763942596494 ) ) ;
#73817=EDGE_CURVE ( 'NONE', #35826, #75060, #17043, .T. ) ;
#73821=CARTESIAN_POINT ( 'NONE',  ( 8.309867465290103894, 5.356774720514426491, -25.05695269341429920 ) ) ;
#73835=DIRECTION ( 'NONE',  ( -0.000000000000000000, 1.000000000000000000, -0.000000000000000000 ) ) ;
#73838=AXIS2_PLACEMENT_3D ( 'NONE', #41952, #35332, #90109 ) ;
#73846=CARTESIAN_POINT ( 'NONE',  ( -20.27875734969026311, -4.543225279485573864, 24.00402280011862288 ) ) ;
#73847=CARTESIAN_POINT ( 'NONE',  ( 11.86515846156731335, 3.316774720514427788, -28.09350142571734921 ) ) ;
#73848=CARTESIAN_POINT ( 'NONE',  ( 14.73162737928355170, 3.582999323269832725, -27.37940951657878941 ) ) ;
#73849=ADVANCED_FACE ( 'NONE', ( #92660 ), #23139, .T. ) ;
#73852=AXIS2_PLACEMENT_3D ( 'NONE', #76975, #7469, #44048 ) ;
#73855=VECTOR ( 'NONE', #41803, 1000.000000000000227 ) ;
#73866=PLANE ( 'NONE',  #53335 ) ;
#73867=LINE ( 'NONE', #87601, #41916 ) ;
#73868=EDGE_CURVE ( 'NONE', #16956, #50557, #24480, .T. ) ;
#73875=DIRECTION ( 'NONE',  ( 0.000000000000000000, 0.000000000000000000, -1.000000000000000000 ) ) ;
#73878=CARTESIAN_POINT ( 'NONE',  ( 15.58962545129235799, -6.475225279485573360, -26.91365498785467025 ) ) ;
#73909=EDGE_LOOP ( 'NONE', ( #42806, #27489, #72167, #24239 ) ) ;
#73911=ORIENTED_EDGE ( 'NONE', *, *, #24894, .T. ) ;
#73917=CARTESIAN_POINT ( 'NONE',  ( 22.33191539159815164, 4.132774720514426292, -16.26852658953823649 ) ) ;
#73928=ORIENTED_EDGE ( 'NONE', *, *, #58245, .T. ) ;
#73929=AXIS2_PLACEMENT_3D ( 'NONE', #45747, #83800, #20897 ) ;
#73934=VERTEX_POINT ( 'NONE', #33778 ) ;
#73938=EDGE_CURVE ( 'NONE', #42281, #98946, #81459, .T. ) ;
#73953=EDGE_CURVE ( 'NONE', #74213, #55518, #10432, .T. ) ;
#73954=DIRECTION ( 'NONE',  ( 0.000000000000000000, 0.000000000000000000, 1.000000000000000000 ) ) ;
#73974=CARTESIAN_POINT ( 'NONE',  ( -10.16634758543296613, -6.475225279485573360, 30.00402280011862288 ) ) ;
#73979=EDGE_CURVE ( 'NONE', #27949, #38058, #27670, .T. ) ;
#73989=CARTESIAN_POINT ( 'NONE',  ( 1.305682803664691249, -5.965225279485572685, 29.57950906855421991 ) ) ;
#73992=VECTOR ( 'NONE', #2781, 1000.000000000000000 ) ;
#74006=EDGE_CURVE ( 'NONE', #18475, #96754, #49516, .T. ) ;
#74008=CARTESIAN_POINT ( 'NONE',  ( 29.73860345376319358, -1.477225279485574028, -8.849814207987163783 ) ) ;
#74010=CARTESIAN_POINT ( 'NONE',  ( 13.91401389203221406, 5.356774720514425603, 158.0376437107427137 ) ) ;
#74049=CARTESIAN_POINT ( 'NONE',  ( 0.000000000000000000, -1.473225279485573802, 4.300000000000000711 ) ) ;
#74051=VERTEX_POINT ( 'NONE', #13420 ) ;
#74060=VERTEX_POINT ( 'NONE', #6810 ) ;
#74067=CARTESIAN_POINT ( 'NONE',  ( 12.99736557111424595, 3.316774720514426900, -27.13536621820933448 ) ) ;
#74071=ADVANCED_FACE ( 'NONE', ( #76310 ), #82932, .F. ) ;
#74078=LINE ( 'NONE', #4571, #27085 ) ;
#74095=DIRECTION ( 'NONE',  ( -0.000000000000000000, -1.000000000000000000, -0.000000000000000000 ) ) ;
#74110=DIRECTION ( 'NONE',  ( 0.000000000000000000, -0.000000000000000000, -1.000000000000000000 ) ) ;
#74130=ORIENTED_EDGE ( 'NONE', *, *, #10133, .T. ) ;
#74132=CARTESIAN_POINT ( 'NONE',  ( 29.61860529676591369, 5.187414344753652706, 28.58826086137218780 ) ) ;
#74134=CARTESIAN_POINT ( 'NONE',  ( 29.80070917940689412, -5.965225279485572685, 27.39560796525321607 ) ) ;
#74167=VERTEX_POINT ( 'NONE', #78803 ) ;
#74175=CARTESIAN_POINT ( 'NONE',  ( 1.175186991919855872, 6.376774720514426953, 28.89597625626659649 ) ) ;
#74181=VERTEX_POINT ( 'NONE', #84933 ) ;
#74189=DIRECTION ( 'NONE',  ( 0.000000000000000000, -0.000000000000000000, -1.000000000000000000 ) ) ;
#74213=VERTEX_POINT ( 'NONE', #86438 ) ;
#74214=CARTESIAN_POINT ( 'NONE',  ( 10.48383480065558615, 3.481296116130239149, -27.02502823977714286 ) ) ;
#74227=DIRECTION ( 'NONE',  ( 0.000000000000000000, 0.000000000000000000, -1.000000000000000000 ) ) ;
#74248=ORIENTED_EDGE ( 'NONE', *, *, #9583, .F. ) ;
#74261=VERTEX_POINT ( 'NONE', #38255 ) ;
#74274=EDGE_CURVE ( 'NONE', #71246, #42693, #1711, .T. ) ;
#74279=CARTESIAN_POINT ( 'NONE',  ( -29.49875734969026198, -5.965225279485572685, 2.362022800118626531 ) ) ;
#74311=ADVANCED_FACE ( 'NONE', ( #85429 ), #100130, .T. ) ;
#74319=ORIENTED_EDGE ( 'NONE', *, *, #70735, .T. ) ;
#74321=DIRECTION ( 'NONE',  ( -8.334928612639484546E-17, -1.000000000000000000, -7.321843366904296032E-17 ) ) ;
#74323=ORIENTED_EDGE ( 'NONE', *, *, #73817, .F. ) ;
#74327=AXIS2_PLACEMENT_3D ( 'NONE', #29170, #4843, #51025 ) ;
#74343=DIRECTION ( 'NONE',  ( -0.000000000000000000, -1.000000000000000000, -0.000000000000000000 ) ) ;
#74346=DIRECTION ( 'NONE',  ( 0.000000000000000000, 0.000000000000000000, -1.000000000000000000 ) ) ;
#74356=CARTESIAN_POINT ( 'NONE',  ( 30.32108885906865936, 5.356774720514427379, 3.274824222184972822 ) ) ;
#74382=DIRECTION ( 'NONE',  ( -0.000000000000000000, -1.000000000000000000, -0.000000000000000000 ) ) ;
#74410=ORIENTED_EDGE ( 'NONE', *, *, #44663, .F. ) ;
#74442=LINE ( 'NONE', #14022, #95116 ) ;
#74443=CARTESIAN_POINT ( 'NONE',  ( 22.81105451610979173, 500000.0000000000582, -18.46691820600746681 ) ) ;
#74446=DIRECTION ( 'NONE',  ( 0.000000000000000000, -0.000000000000000000, 1.000000000000000000 ) ) ;
#74459=CIRCLE ( 'NONE', #64791, 2.249999999999998668 ) ;
#74462=EDGE_LOOP ( 'NONE', ( #3425, #8420, #74410, #49770 ) ) ;
#74467=AXIS2_PLACEMENT_3D ( 'NONE', #66079, #75151, #44219 ) ;
#74473=CARTESIAN_POINT ( 'NONE',  ( 14.52511747680497933, -6.475225279485573360, -27.86035006098926559 ) ) ;
#74475=CARTESIAN_POINT ( 'NONE',  ( 11.84174468958795323, -6.475225279485574248, -27.06880646454217043 ) ) ;
#74479=DIRECTION ( 'NONE',  ( -0.000000000000000000, -0.000000000000000000, 1.000000000000000000 ) ) ;
#74484=EDGE_LOOP ( 'NONE', ( #95606, #96363, #84580, #20183 ) ) ;
#74502=ORIENTED_EDGE ( 'NONE', *, *, #88517, .T. ) ;
#74508=VERTEX_POINT ( 'NONE', #25031 ) ;
#74525=VERTEX_POINT ( 'NONE', #13791 ) ;
#74528=PLANE ( 'NONE',  #5682 ) ;
#74529=CIRCLE ( 'NONE', #24331, 2.249999999999998668 ) ;
#74542=EDGE_CURVE ( 'NONE', #40372, #36906, #21397, .T. ) ;
#74545=AXIS2_PLACEMENT_3D ( 'NONE', #8353, #53178, #6493 ) ;
#74546=EDGE_LOOP ( 'NONE', ( #53812, #98607, #49367, #1742, #55425, #75157, #57928 ) ) ;
#74549=CIRCLE ( 'NONE', #32403, 2.500000000000000444 ) ;
#74556=DIRECTION ( 'NONE',  ( -3.246014568247801031E-12, 0.000000000000000000, 1.000000000000000000 ) ) ;
#74557=CARTESIAN_POINT ( 'NONE',  ( 11.80640562518893866, -6.475225279485576024, -27.06722565682295567 ) ) ;
#74573=DIRECTION ( 'NONE',  ( -0.000000000000000000, 1.000000000000000000, -0.000000000000000000 ) ) ;
#74574=CARTESIAN_POINT ( 'NONE',  ( -20.77875734969026311, 5.356774720514426491, 27.45402280011862217 ) ) ;
#74585=LINE ( 'NONE', #11683, #78872 ) ;
#74588=VERTEX_POINT ( 'NONE', #51882 ) ;
#74590=CARTESIAN_POINT ( 'NONE',  ( 10.70203014590133783, 5.295085572968130094, -27.33604350180555187 ) ) ;
#74596=CARTESIAN_POINT ( 'NONE',  ( 33.55334901790278224, 3.914284326356132659, -11.46592497341461758 ) ) ;
#74601=DIRECTION ( 'NONE',  ( -0.6599726524652352877, 0.000000000000000000, 0.7512896232465892110 ) ) ;
#74603=AXIS2_PLACEMENT_3D ( 'NONE', #55713, #39470, #46088 ) ;
#74604=FACE_OUTER_BOUND ( 'NONE', #96250, .T. ) ;
#74608=DIRECTION ( 'NONE',  ( -1.226388327005079762E-16, 0.000000000000000000, 1.000000000000000000 ) ) ;
#74610=LINE ( 'NONE', #6604, #96439 ) ;
#74613=EDGE_CURVE ( 'NONE', #14296, #81702, #83803, .T. ) ;
#74622=EDGE_CURVE ( 'NONE', #10305, #70795, #99024, .T. ) ;
#74702=CARTESIAN_POINT ( 'NONE',  ( -20.27875734969026311, -6.143225279485574397, 26.25402280011862288 ) ) ;
#74725=ORIENTED_EDGE ( 'NONE', *, *, #86242, .T. ) ;
#74732=ADVANCED_FACE ( 'NONE', ( #46763 ), #41376, .T. ) ;
#74733=EDGE_LOOP ( 'NONE', ( #54884, #61450 ) ) ;
#74736=VECTOR ( 'NONE', #96183, 1000.000000000000000 ) ;
#74748=DIRECTION ( 'NONE',  ( 0.000000000000000000, 0.000000000000000000, 1.000000000000000000 ) ) ;
#74777=EDGE_LOOP ( 'NONE', ( #43568, #98231, #81397 ) ) ;
#74793=EDGE_CURVE ( 'NONE', #96596, #19596, #52178, .T. ) ;
#74810=CARTESIAN_POINT ( 'NONE',  ( 10.73283225838973642, 5.356774720506346732, -27.03068772369604744 ) ) ;
#74814=VECTOR ( 'NONE', #29413, 1000.000000000000000 ) ;
#74861=EDGE_CURVE ( 'NONE', #82569, #24683, #97437, .T. ) ;
#74870=VERTEX_POINT ( 'NONE', #35548 ) ;
#74871=DIRECTION ( 'NONE',  ( 0.000000000000000000, 0.000000000000000000, 1.000000000000000000 ) ) ;
#74875=ORIENTED_EDGE ( 'NONE', *, *, #20547, .F. ) ;
#74876=ORIENTED_EDGE ( 'NONE', *, *, #8305, .F. ) ;
#74885=AXIS2_PLACEMENT_3D ( 'NONE', #99988, #83285, #21374 ) ;
#74894=ORIENTED_EDGE ( 'NONE', *, *, #36502, .F. ) ;
#74895=DIRECTION ( 'NONE',  ( 0.000000000000000000, 0.000000000000000000, -1.000000000000000000 ) ) ;
#74900=EDGE_LOOP ( 'NONE', ( #10802, #34951 ) ) ;
#74901=CARTESIAN_POINT ( 'NONE',  ( -29.49875734969026198, 0.3587747205144265483, 2.362022800118626531 ) ) ;
#74913=CARTESIAN_POINT ( 'NONE',  ( 14.76093561896378326, 3.316774720514426456, -26.55548769130088260 ) ) ;
#74915=AXIS2_PLACEMENT_3D ( 'NONE', #61838, #93261, #77532 ) ;
#74926=LINE ( 'NONE', #99269, #95814 ) ;
#74928=AXIS2_PLACEMENT_3D ( 'NONE', #73846, #29162, #52511 ) ;
#74935=EDGE_CURVE ( 'NONE', #38058, #70059, #68316, .T. ) ;
#74937=DIRECTION ( 'NONE',  ( 0.000000000000000000, -1.000000000000000000, 0.000000000000000000 ) ) ;
#74952=VECTOR ( 'NONE', #50759, 1000.000000000000000 ) ;
#74966=DIRECTION ( 'NONE',  ( -0.9921023176230513441, 0.000000000000000000, 0.1254312216594016538 ) ) ;
#74967=VECTOR ( 'NONE', #31597, 1000.000000000000000 ) ;
#74993=ORIENTED_EDGE ( 'NONE', *, *, #67611, .F. ) ;
#75007=ORIENTED_EDGE ( 'NONE', *, *, #60128, .T. ) ;
#75015=CARTESIAN_POINT ( 'NONE',  ( 3.176458874063926352, -5.965225279485592225, -28.85257003503889095 ) ) ;
#75016=ORIENTED_EDGE ( 'NONE', *, *, #44039, .T. ) ;
#75024=AXIS2_PLACEMENT_3D ( 'NONE', #36402, #75445, #68852 ) ;
#75039=DIRECTION ( 'NONE',  ( -0.06283980576413537855, -0.000000000000000000, -0.9980236263794188822 ) ) ;
#75042=LINE ( 'NONE', #44611, #32911 ) ;
#75045=CIRCLE ( 'NONE', #68534, 1.699999999999998401 ) ;
#75048=CARTESIAN_POINT ( 'NONE',  ( 11.92750898180832131, 4.915819049120522699, -27.17522536519172860 ) ) ;
#75060=VERTEX_POINT ( 'NONE', #48157 ) ;
#75067=DIRECTION ( 'NONE',  ( -0.000000000000000000, -0.000000000000000000, -1.000000000000000000 ) ) ;
#75070=CARTESIAN_POINT ( 'NONE',  ( 31.04236049493789906, -5.965225279485572685, 19.84760796525321780 ) ) ;
#75077=DIRECTION ( 'NONE',  ( 0.7512896232465892110, -0.000000000000000000, 0.6599726524652350657 ) ) ;
#75090=CARTESIAN_POINT ( 'NONE',  ( 32.25183987940364005, -5.965225279485572685, 2.026414261721653176 ) ) ;
#75092=LINE ( 'NONE', #60401, #42453 ) ;
#75097=PLANE ( 'NONE',  #25669 ) ;
#75102=DIRECTION ( 'NONE',  ( 0.000000000000000000, 0.000000000000000000, -1.000000000000000000 ) ) ;
#75103=DIRECTION ( 'NONE',  ( -0.000000000000000000, -1.000000000000000000, -0.000000000000000000 ) ) ;
#75106=ADVANCED_FACE ( 'NONE', ( #56778 ), #33411, .F. ) ;
#75110=CARTESIAN_POINT ( 'NONE',  ( -19.69812919673063689, 0.3587747205143964613, -22.00173861453436430 ) ) ;
#75123=ADVANCED_FACE ( 'NONE', ( #72493 ), #41542, .T. ) ;
#75128=ORIENTED_EDGE ( 'NONE', *, *, #61885, .T. ) ;
#75136=( BOUNDED_SURFACE ( )  B_SPLINE_SURFACE ( 3, 2, ( 
 ( #72360, #97185, #73847 ),
 ( #88581, #2855, #19054 ),
 ( #18556, #50512, #28175 ),
 ( #33788, #72860, #81957 ) ),
 .UNSPECIFIED., .F., .F., .T. ) 
 B_SPLINE_SURFACE_WITH_KNOTS ( ( 4, 4 ),
 ( 3, 3 ),
 ( 0.01105101719324316605, 0.01425305434006712661 ),
 ( 0.000000000000000000, 1.000000000000000000 ),
 .UNSPECIFIED. ) 
 GEOMETRIC_REPRESENTATION_ITEM ( )  RATIONAL_B_SPLINE_SURFACE ( (
 ( 1.000000000000000000, 0.7071067811865476838, 1.000000000000000000),
 ( 1.000000000000000000, 0.7071067811865476838, 1.000000000000000000),
 ( 1.000000000000000000, 0.7071067811865469066, 1.000000000000000000),
 ( 1.000000000000000000, 0.7071067811865469066, 1.000000000000000000) ) ) 
 REPRESENTATION_ITEM ( '' )  SURFACE ( )  );
#75150=EDGE_LOOP ( 'NONE', ( #87041, #86136, #19386, #15284 ) ) ;
#75151=DIRECTION ( 'NONE',  ( -0.000000000000000000, -1.000000000000000000, -0.000000000000000000 ) ) ;
#75152=DIRECTION ( 'NONE',  ( -1.000000000000000000, 0.000000000000000000, -0.000000000000000000 ) ) ;
#75157=ORIENTED_EDGE ( 'NONE', *, *, #42949, .F. ) ;
#75169=ORIENTED_EDGE ( 'NONE', *, *, #6082, .F. ) ;
#75173=DIRECTION ( 'NONE',  ( -0.000000000000000000, 0.000000000000000000, 1.000000000000000000 ) ) ;
#75182=EDGE_CURVE ( 'NONE', #79519, #65212, #64904, .T. ) ;
#75187=ORIENTED_EDGE ( 'NONE', *, *, #71318, .F. ) ;
#75190=CARTESIAN_POINT ( 'NONE',  ( 30.09341516180546350, 2.682774720514426559, -11.39311774897855756 ) ) ;
#75193=EDGE_CURVE ( 'NONE', #31628, #41503, #71599, .T. ) ;
#75199=DIRECTION ( 'NONE',  ( 0.000000000000000000, 1.000000000000000000, 0.000000000000000000 ) ) ;
#75200=CARTESIAN_POINT ( 'NONE',  ( 22.81105451610979173, -6.475225279485573360, -18.46691820600746681 ) ) ;
#75204=CARTESIAN_POINT ( 'NONE',  ( -19.80875734969026425, 0.3587747205144265483, 31.02402280011862246 ) ) ;
#75207=FACE_OUTER_BOUND ( 'NONE', #96083, .T. ) ;
#75219=EDGE_CURVE ( 'NONE', #51956, #44056, #55787, .T. ) ;
#75232=DIRECTION ( 'NONE',  ( -0.000000000000000000, 1.000000000000000000, -0.000000000000000000 ) ) ;
#75250=VERTEX_POINT ( 'NONE', #34922 ) ;
#75255=ORIENTED_EDGE ( 'NONE', *, *, #46940, .T. ) ;
#75267=ORIENTED_EDGE ( 'NONE', *, *, #74613, .T. ) ;
#75275=ORIENTED_EDGE ( 'NONE', *, *, #76930, .F. ) ;
#75296=DIRECTION ( 'NONE',  ( 0.000000000000000000, 0.000000000000000000, -1.000000000000000000 ) ) ;
#75302=EDGE_CURVE ( 'NONE', #62563, #35826, #58756, .T. ) ;
#75306=CARTESIAN_POINT ( 'NONE',  ( 15.97264540888995299, 3.316774720514426456, -27.93485543958162154 ) ) ;
#75337=DIRECTION ( 'NONE',  ( 0.000000000000000000, 0.000000000000000000, -1.000000000000000000 ) ) ;
#75346=CARTESIAN_POINT ( 'NONE',  ( 32.88562546571908740, 0.3587747205144265483, -5.083907541707153754 ) ) ;
#75351=CARTESIAN_POINT ( 'NONE',  ( 0.000000000000000000, -16.94322527948557422, 0.000000000000000000 ) ) ;
#75363=LINE ( 'NONE', #20581, #48136 ) ;
#75366=EDGE_CURVE ( 'NONE', #79593, #45825, #92060, .T. ) ;
#75371=ADVANCED_FACE ( 'NONE', ( #84077 ), #29296, .F. ) ;
#75377=CARTESIAN_POINT ( 'NONE',  ( 32.45853543194704116, 0.3587747205144265483, 9.169203677920338080 ) ) ;
#75382=ORIENTED_EDGE ( 'NONE', *, *, #63892, .F. ) ;
#75390=AXIS2_PLACEMENT_3D ( 'NONE', #28672, #59135, #6329 ) ;
#75394=DIRECTION ( 'NONE',  ( -1.000000000000000000, -0.000000000000000000, -0.000000000000000000 ) ) ;
#75412=CIRCLE ( 'NONE', #15439, 28.96799999999999642 ) ;
#75413=AXIS2_PLACEMENT_3D ( 'NONE', #9983, #40445, #23698 ) ;
#75432=CARTESIAN_POINT ( 'NONE',  ( -29.49875734969025842, -5.965225279485572685, 25.61802280011862720 ) ) ;
#75445=DIRECTION ( 'NONE',  ( -0.9952638024365006997, 0.000000000000000000, -0.09721092304694052555 ) ) ;
#75450=VERTEX_POINT ( 'NONE', #8461 ) ;
#75458=DIRECTION ( 'NONE',  ( -0.000000000000000000, -1.000000000000000000, -0.000000000000000000 ) ) ;
#75460=ORIENTED_EDGE ( 'NONE', *, *, #81524, .F. ) ;
#75461=LINE ( 'NONE', #90706, #58894 ) ;
#75464=CARTESIAN_POINT ( 'NONE',  ( 24.71017632900191074, 5.356774720514427379, 1.647607965253217399 ) ) ;
#75467=EDGE_CURVE ( 'NONE', #83063, #52175, #67874, .T. ) ;
#75479=DIRECTION ( 'NONE',  ( 0.000000000000000000, 1.000000000000000000, -0.000000000000000000 ) ) ;
#75487=ORIENTED_EDGE ( 'NONE', *, *, #65735, .T. ) ;
#75489=ORIENTED_EDGE ( 'NONE', *, *, #17601, .T. ) ;
#75495=CIRCLE ( 'NONE', #52776, 28.45799999999999486 ) ;
#75512=CARTESIAN_POINT ( 'NONE',  ( 0.000000000000000000, 1.826774720514426464, 4.300000000000000711 ) ) ;
#75521=CIRCLE ( 'NONE', #70922, 2.499999999999998668 ) ;
#75531=LINE ( 'NONE', #89781, #37555 ) ;
#75532=ORIENTED_EDGE ( 'NONE', *, *, #38073, .T. ) ;
#75559=DIRECTION ( 'NONE',  ( -0.000000000000000000, 1.000000000000000000, -0.000000000000000000 ) ) ;
#75563=AXIS2_PLACEMENT_3D ( 'NONE', #138, #84373, #23452 ) ;
#75564=DIRECTION ( 'NONE',  ( 0.000000000000000000, 0.000000000000000000, -1.000000000000000000 ) ) ;
#75566=EDGE_CURVE ( 'NONE', #91875, #95021, #64783, .T. ) ;
#75572=VECTOR ( 'NONE', #87714, 1000.000000000000000 ) ;
#75585=CARTESIAN_POINT ( 'NONE',  ( 30.77564450787170003, -1.477225279485574028, -9.689394075852828081 ) ) ;
#75595=CARTESIAN_POINT ( 'NONE',  ( 30.54789914928607431, -0.2637885907592280588, 23.75907673500033113 ) ) ;
#75598=CYLINDRICAL_SURFACE ( 'NONE', #25805, 2.499999999999998668 ) ;
#75611=ORIENTED_EDGE ( 'NONE', *, *, #98456, .T. ) ;
#75615=CIRCLE ( 'NONE', #88615, 3.500000000000000000 ) ;
#75619=EDGE_LOOP ( 'NONE', ( #24466, #4764, #50096, #60415 ) ) ;
#75623=ADVANCED_FACE ( 'NONE', ( #68121 ), #89458, .T. ) ;
#75644=EDGE_LOOP ( 'NONE', ( #91495, #57545, #40834, #62219, #58506, #8745, #87618, #11146 ) ) ;
#75662=AXIS2_PLACEMENT_3D ( 'NONE', #94904, #55867, #16779 ) ;
#75684=VECTOR ( 'NONE', #72457, 1000.000000000000227 ) ;
#75691=DIRECTION ( 'NONE',  ( 0.000000000000000000, 0.000000000000000000, 1.000000000000000000 ) ) ;
#75692=CIRCLE ( 'NONE', #88692, 251.9358649670780892 ) ;
#75697=CARTESIAN_POINT ( 'NONE',  ( 282.9764569301858046, 3.316774720514426900, 20.79159422840526616 ) ) ;
#75719=CARTESIAN_POINT ( 'NONE',  ( 22.11414358107865397, 4.215138183568805985, -16.31598992311990415 ) ) ;
#75721=CARTESIAN_POINT ( 'NONE',  ( -27.96875734969026084, -6.143225279485574397, 23.50402280011861933 ) ) ;
#75734=EDGE_CURVE ( 'NONE', #24351, #62056, #87862, .T. ) ;
#75737=CARTESIAN_POINT ( 'NONE',  ( -28.47875734969026240, -5.965225279485572685, 26.43402280011862615 ) ) ;
#75748=ADVANCED_FACE ( 'NONE', ( #76162 ), #99498, .T. ) ;
#75770=ORIENTED_EDGE ( 'NONE', *, *, #36044, .T. ) ;
#75775=VECTOR ( 'NONE', #86178, 1000.000000000000000 ) ;
#75791=DIRECTION ( 'NONE',  ( -0.000000000000000000, -1.000000000000000000, -0.000000000000000000 ) ) ;
#75816=DIRECTION ( 'NONE',  ( 7.994117400814786717E-16, 0.000000000000000000, -1.000000000000000000 ) ) ;
#75833=LINE ( 'NONE', #67250, #60940 ) ;
#75838=PLANE ( 'NONE',  #3757 ) ;
#75848=CARTESIAN_POINT ( 'NONE',  ( 29.71615239255367413, 4.563867803339911156, 27.78418661847934246 ) ) ;
#75872=ORIENTED_EDGE ( 'NONE', *, *, #99713, .T. ) ;
#75928=LINE ( 'NONE', #28270, #69082 ) ;
#75934=FACE_OUTER_BOUND ( 'NONE', #72653, .T. ) ;
#75935=CARTESIAN_POINT ( 'NONE',  ( 3.509873074917118085, 0.3587747205144265483, 29.15869884040363758 ) ) ;
#75936=EDGE_CURVE ( 'NONE', #85295, #3492, #40630, .T. ) ;
#75945=CARTESIAN_POINT ( 'NONE',  ( 2.872281323269014752, -16.94322527948557422, 1.999999999999999556 ) ) ;
#75961=ORIENTED_EDGE ( 'NONE', *, *, #71933, .T. ) ;
#75965=VECTOR ( 'NONE', #27768, 1000.000000000000000 ) ;
#75979=DIRECTION ( 'NONE',  ( -0.9872275723272648795, 0.000000000000000000, -0.1593164160933056017 ) ) ;
#75992=ORIENTED_EDGE ( 'NONE', *, *, #48402, .T. ) ;
#76001=CARTESIAN_POINT ( 'NONE',  ( -0.02075734969026423599, 3.316774720514426456, -0.08597719988137648983 ) ) ;
#76004=ORIENTED_EDGE ( 'NONE', *, *, #33632, .F. ) ;
#76005=DIRECTION ( 'NONE',  ( 0.000000000000000000, -1.000000000000000000, 0.000000000000000000 ) ) ;
#76009=ORIENTED_EDGE ( 'NONE', *, *, #8562, .F. ) ;
#76019=EDGE_CURVE ( 'NONE', #34838, #29304, #21417, .T. ) ;
#76036=FACE_BOUND ( 'NONE', #5425, .T. ) ;
#76047=DIRECTION ( 'NONE',  ( -0.000000000000000000, -1.000000000000000000, -0.000000000000000000 ) ) ;
#76048=CARTESIAN_POINT ( 'NONE',  ( 30.53060340732035982, 4.751309003483179083, 17.08946163269322227 ) ) ;
#76049=AXIS2_PLACEMENT_3D ( 'NONE', #31, #47213, #76635 ) ;
#76063=CIRCLE ( 'NONE', #8132, 22.69500000000000384 ) ;
#76065=ADVANCED_FACE ( 'NONE', ( #10172 ), #72087, .T. ) ;
#76066=CARTESIAN_POINT ( 'NONE',  ( 30.53060340732036337, -1.477225279485574028, -8.442346167188908623 ) ) ;
#76069=DIRECTION ( 'NONE',  ( -0.000000000000000000, -1.000000000000000000, -0.000000000000000000 ) ) ;
#76084=EDGE_LOOP ( 'NONE', ( #41902, #58158, #68053, #32494, #96817, #44686 ) ) ;
#76096=DIRECTION ( 'NONE',  ( 0.000000000000000000, 0.000000000000000000, 1.000000000000000000 ) ) ;
#76097=CARTESIAN_POINT ( 'NONE',  ( 11.96754062809080743, 2.682774720514426559, -27.06850815473629979 ) ) ;
#76098=CARTESIAN_POINT ( 'NONE',  ( -28.84663072490566194, -5.965225279485572685, 28.73989617533406715 ) ) ;
#76126=ORIENTED_EDGE ( 'NONE', *, *, #85670, .F. ) ;
#76140=ORIENTED_EDGE ( 'NONE', *, *, #94626, .T. ) ;
#76161=CARTESIAN_POINT ( 'NONE',  ( -2.704906987277321040, 0.3587747205144061757, -28.92935364444904778 ) ) ;
#76162=FACE_OUTER_BOUND ( 'NONE', #72443, .T. ) ;
#76172=ADVANCED_FACE ( 'NONE', ( #69828 ), #30759, .F. ) ;
#76188=VECTOR ( 'NONE', #51684, 1000.000000000000000 ) ;
#76194=VERTEX_POINT ( 'NONE', #53618 ) ;
#76201=EDGE_CURVE ( 'NONE', #37481, #16105, #311, .T. ) ;
#76222=CARTESIAN_POINT ( 'NONE',  ( 20.84816453548659609, 4.362175914522286035, -17.34246194398105345 ) ) ;
#76229=DIRECTION ( 'NONE',  ( -0.000000000000000000, -1.000000000000000000, -0.000000000000000000 ) ) ;
#76237=DIRECTION ( 'NONE',  ( -0.000000000000000000, -1.000000000000000000, -0.000000000000000000 ) ) ;
#76244=DIRECTION ( 'NONE',  ( 0.000000000000000000, 0.000000000000000000, 1.000000000000000000 ) ) ;
#76252=PLANE ( 'NONE',  #91791 ) ;
#76254=ADVANCED_FACE ( 'NONE', ( #23129 ), #22629, .T. ) ;
#76259=CIRCLE ( 'NONE', #66605, 28.96799999999999287 ) ;
#76265=ORIENTED_EDGE ( 'NONE', *, *, #21034, .T. ) ;
#76282=DIRECTION ( 'NONE',  ( 0.000000000000000000, 1.000000000000000000, 0.000000000000000000 ) ) ;
#76310=FACE_OUTER_BOUND ( 'NONE', #11824, .T. ) ;
#76318=CARTESIAN_POINT ( 'NONE',  ( 22.02124265030973760, 3.456774720514426136, 15.05402280011862004 ) ) ;
#76353=DIRECTION ( 'NONE',  ( 0.000000000000000000, -1.000000000000000000, 0.000000000000000000 ) ) ;
#76355=EDGE_LOOP ( 'NONE', ( #78834, #38742, #7865, #43264 ) ) ;
#76379=ADVANCED_FACE ( 'NONE', ( #9416 ), #47894, .F. ) ;
#76383=DIRECTION ( 'NONE',  ( 1.000000000000000000, 0.000000000000000000, 0.000000000000000000 ) ) ;
#76406=VERTEX_POINT ( 'NONE', #19031 ) ;
#76414=PLANE ( 'NONE',  #95693 ) ;
#76416=ORIENTED_EDGE ( 'NONE', *, *, #36138, .T. ) ;
#76417=ORIENTED_EDGE ( 'NONE', *, *, #680, .F. ) ;
#76421=CARTESIAN_POINT ( 'NONE',  ( 32.54628039735602130, 5.044004387208919304, -11.78547710168594165 ) ) ;
#76431=VECTOR ( 'NONE', #7394, 1000.000000000000000 ) ;
#76444=EDGE_CURVE ( 'NONE', #88649, #33103, #12414, .T. ) ;
#76461=LINE ( 'NONE', #67382, #84097 ) ;
#76465=CARTESIAN_POINT ( 'NONE',  ( 32.33465265239741626, 4.457608646344818126, 0.9133233228923198777 ) ) ;
#76480=CARTESIAN_POINT ( 'NONE',  ( 11.22434917415779054, 4.132774715458839232, -26.87660878605755599 ) ) ;
#76492=ORIENTED_EDGE ( 'NONE', *, *, #53376, .T. ) ;
#76508=AXIS2_PLACEMENT_3D ( 'NONE', #7534, #86158, #47112 ) ;
#76515=FACE_OUTER_BOUND ( 'NONE', #31591, .T. ) ;
#76521=AXIS2_PLACEMENT_3D ( 'NONE', #2464, #64889, #19168 ) ;
#76557=VECTOR ( 'NONE', #80900, 1000.000000000000000 ) ;
#76569=CARTESIAN_POINT ( 'NONE',  ( 11.62916340711181284, 0.3587747205144265483, 28.75961759920349792 ) ) ;
#76586=LINE ( 'NONE', #67506, #96944 ) ;
#76588=VERTEX_POINT ( 'NONE', #16914 ) ;
#76596=CARTESIAN_POINT ( 'NONE',  ( 30.56047832681638354, -2.297196155479634516, 24.67598410064775649 ) ) ;
#76605=ORIENTED_EDGE ( 'NONE', *, *, #29316, .F. ) ;
#76606=DIRECTION ( 'NONE',  ( 0.06486421869277853025, 0.000000000000000000, -0.9978940991575084851 ) ) ;
#76618=LINE ( 'NONE', #23333, #57645 ) ;
#76621=ORIENTED_EDGE ( 'NONE', *, *, #54136, .T. ) ;
#76635=DIRECTION ( 'NONE',  ( -0.9913618264504691080, 0.000000000000000000, 0.1311553622875927805 ) ) ;
#76636=CARTESIAN_POINT ( 'NONE',  ( 32.23865423223558935, 4.540774720514431095, 2.161924922174277341 ) ) ;
#76643=VERTEX_POINT ( 'NONE', #12288 ) ;
#76667=DIRECTION ( 'NONE',  ( 0.000000000000000000, 0.000000000000000000, -1.000000000000000000 ) ) ;
#76668=FACE_OUTER_BOUND ( 'NONE', #9144, .T. ) ;
#76673=VECTOR ( 'NONE', #90324, 1000.000000000000000 ) ;
#76678=CARTESIAN_POINT ( 'NONE',  ( 10.86431179148764770, 6.376774720514933215, -28.05678185045468709 ) ) ;
#76688=DIRECTION ( 'NONE',  ( -1.334402673828313093E-16, -0.000000000000000000, -1.000000000000000000 ) ) ;
#76700=CARTESIAN_POINT ( 'NONE',  ( 29.73860345376318293, 5.356514366721292220, 19.42370904364366169 ) ) ;
#76702=DIRECTION ( 'NONE',  ( 0.000000000000000000, 1.000000000000000000, 0.000000000000000000 ) ) ;
#76713=VERTEX_POINT ( 'NONE', #3704 ) ;
#76715=EDGE_CURVE ( 'NONE', #22708, #35597, #4698, .T. ) ;
#76717=AXIS2_PLACEMENT_3D ( 'NONE', #74443, #27280, #11542 ) ;
#76724=CARTESIAN_POINT ( 'NONE',  ( 14.92699176545193041, 5.063793094955937768, -27.26229911407734008 ) ) ;
#76789=FACE_OUTER_BOUND ( 'NONE', #67291, .T. ) ;
#76793=LINE ( 'NONE', #191, #4272 ) ;
#76820=CARTESIAN_POINT ( 'NONE',  ( -24.97666371003640151, -5.965225279485592225, -15.72894043976419098 ) ) ;
#76823=DIRECTION ( 'NONE',  ( -0.7512896232465891000, 0.000000000000000000, -0.6599726524652352877 ) ) ;
#76831=PLANE ( 'NONE',  #7907 ) ;
#76842=CARTESIAN_POINT ( 'NONE',  ( 11.56983764158150052, -5.965225279485572685, 28.29037853177889517 ) ) ;
#76855=VERTEX_POINT ( 'NONE', #47256 ) ;
#76864=VERTEX_POINT ( 'NONE', #46755 ) ;
#76866=CARTESIAN_POINT ( 'NONE',  ( -10.40290173325841216, 5.356774720514425603, 27.45402280011861862 ) ) ;
#76878=EDGE_CURVE ( 'NONE', #77258, #88353, #8694, .T. ) ;
#76892=CARTESIAN_POINT ( 'NONE',  ( 22.02124265030973760, 5.356774720514425603, 19.55402280011862004 ) ) ;
#76902=AXIS2_PLACEMENT_3D ( 'NONE', #61616, #87429, #57506 ) ;
#76903=DIRECTION ( 'NONE',  ( 7.904402583950632871E-14, 0.000000000000000000, -1.000000000000000000 ) ) ;
#76913=EDGE_CURVE ( 'NONE', #20097, #25992, #14403, .T. ) ;
#76920=DIRECTION ( 'NONE',  ( -1.000000000000000000, 0.000000000000000000, 0.000000000000000000 ) ) ;
#76924=DIRECTION ( 'NONE',  ( 0.4009304992412300872, 0.000000000000000000, 0.9161084732596779245 ) ) ;
#76930=EDGE_CURVE ( 'NONE', #27962, #17829, #26419, .T. ) ;
#76939=ORIENTED_EDGE ( 'NONE', *, *, #9336, .F. ) ;
#76942=EDGE_CURVE ( 'NONE', #92857, #48435, #62004, .T. ) ;
#76943=AXIS2_PLACEMENT_3D ( 'NONE', #73537, #28858, #19728 ) ;
#76964=CARTESIAN_POINT ( 'NONE',  ( 29.64064043116815128, -5.965225279485572685, 28.71191112024341408 ) ) ;
#76975=CARTESIAN_POINT ( 'NONE',  ( -11.64875734969026233, -5.965225279485572685, 31.02402280011862246 ) ) ;
#76978=LINE ( 'NONE', #61289, #65674 ) ;
#76989=ORIENTED_EDGE ( 'NONE', *, *, #634, .F. ) ;
#77007=EDGE_LOOP ( 'NONE', ( #92134, #77733, #18980, #52891 ) ) ;
#77029=EDGE_CURVE ( 'NONE', #24683, #88649, #34033, .T. ) ;
#77036=CARTESIAN_POINT ( 'NONE',  ( -24.90875734969025501, -5.965225279485572685, 26.43402280011862615 ) ) ;
#77043=EDGE_CURVE ( 'NONE', #89884, #49235, #19785, .T. ) ;
#77059=LINE ( 'NONE', #39008, #57329 ) ;
#77083=LINE ( 'NONE', #30420, #72699 ) ;
#77089=AXIS2_PLACEMENT_3D ( 'NONE', #72213, #16910, #79805 ) ;
#77093=VECTOR ( 'NONE', #81755, 1000.000000000000000 ) ;
#77103=EDGE_LOOP ( 'NONE', ( #23125, #44222, #40315, #7272 ) ) ;
#77105=ORIENTED_EDGE ( 'NONE', *, *, #27648, .T. ) ;
#77118=ORIENTED_EDGE ( 'NONE', *, *, #83283, .F. ) ;
#77124=EDGE_CURVE ( 'NONE', #86083, #5378, #68475, .T. ) ;
#77131=EDGE_CURVE ( 'NONE', #71104, #37448, #57172, .T. ) ;
#77144=EDGE_LOOP ( 'NONE', ( #85136, #36919 ) ) ;
#77152=AXIS2_PLACEMENT_3D ( 'NONE', #44767, #84307, #75691 ) ;
#77163=DIRECTION ( 'NONE',  ( 0.000000000000000000, 0.000000000000000000, -1.000000000000000000 ) ) ;
#77172=CARTESIAN_POINT ( 'NONE',  ( 30.53060340732035982, -1.477225279485574028, 19.84760796525321780 ) ) ;
#77174=DIRECTION ( 'NONE',  ( 0.000000000000000000, -1.000000000000000000, 0.000000000000000000 ) ) ;
#77200=AXIS2_PLACEMENT_3D ( 'NONE', #12181, #81709, #4594 ) ;
#77201=CARTESIAN_POINT ( 'NONE',  ( 14.98985047787450320, 3.577630190450212577, -26.76169638709854226 ) ) ;
#77205=B_SPLINE_CURVE_WITH_KNOTS ( 'NONE', 3,
 ( #1678, #32617, #69178, #30612, #61587, #92507, #22978, #33622, #64604, #26515, #57479, #4177, #11280, #34129, #79284, #40732, #9778, #56976, #10787, #3189, #50354, #71691 ),
 .UNSPECIFIED., .F., .F.,
 ( 4, 2, 2, 2, 2, 2, 2, 2, 2, 2, 4 ),
 ( 2.109901731184535120E-07, 0.0007177669497569155819, 0.001435322909340712699, 0.001794100889132610064, 0.002152878868924507430, 0.002870434828508297825, 0.003587990788092088653, 0.003946768767883982766, 0.004305546747675877313, 0.005023102707259665539, 0.005740658666843454633 ),
 .UNSPECIFIED. ) ;
#77225=CARTESIAN_POINT ( 'NONE',  ( -15.82668884360736961, 1.684774720514424118, 42.07822029717483758 ) ) ;
#77228=ORIENTED_EDGE ( 'NONE', *, *, #90946, .F. ) ;
#77231=ORIENTED_EDGE ( 'NONE', *, *, #62439, .F. ) ;
#77235=CARTESIAN_POINT ( 'NONE',  ( -19.69812919673063689, -5.965225279485592225, -22.00173861453435720 ) ) ;
#77243=PLANE ( 'NONE',  #30439 ) ;
#77258=VERTEX_POINT ( 'NONE', #17683 ) ;
#77279=ORIENTED_EDGE ( 'NONE', *, *, #34131, .T. ) ;
#77297=ORIENTED_EDGE ( 'NONE', *, *, #80364, .F. ) ;
#77310=DIRECTION ( 'NONE',  ( -0.000000000000000000, 1.000000000000000000, -0.000000000000000000 ) ) ;
#77312=EDGE_CURVE ( 'NONE', #61929, #27949, #13456, .T. ) ;
#77324=AXIS2_PLACEMENT_3D ( 'NONE', #58961, #82285, #5163 ) ;
#77343=AXIS2_PLACEMENT_3D ( 'NONE', #88817, #49765, #11184 ) ;
#77363=VECTOR ( 'NONE', #55477, 1000.000000000000000 ) ;
#77385=ORIENTED_EDGE ( 'NONE', *, *, #20213, .F. ) ;
#77388=ORIENTED_EDGE ( 'NONE', *, *, #49612, .F. ) ;
#77410=DIRECTION ( 'NONE',  ( -0.000000000000000000, -1.000000000000000000, -0.000000000000000000 ) ) ;
#77419=AXIS2_PLACEMENT_3D ( 'NONE', #95180, #72853, #88574 ) ;
#77422=FACE_OUTER_BOUND ( 'NONE', #25314, .T. ) ;
#77427=DIRECTION ( 'NONE',  ( 0.000000000000000000, -0.000000000000000000, -1.000000000000000000 ) ) ;
#77438=DIRECTION ( 'NONE',  ( 0.7512896232465891000, 0.000000000000000000, 0.6599726524652351767 ) ) ;
#77441=CARTESIAN_POINT ( 'NONE',  ( -22.05275734969026047, -5.965225279485572685, 30.51402280011862089 ) ) ;
#77456=EDGE_CURVE ( 'NONE', #44339, #38457, #45854, .T. ) ;
#77457=EDGE_LOOP ( 'NONE', ( #50751, #38835, #3137, #67945 ) ) ;
#77463=CARTESIAN_POINT ( 'NONE',  ( -28.98875734969026396, -5.965225279485572685, 0.1180228001186258285 ) ) ;
#77475=EDGE_LOOP ( 'NONE', ( #3746, #31038, #33138, #58557, #76416, #22885, #19749, #25489, #72327 ) ) ;
#77487=VERTEX_POINT ( 'NONE', #19669 ) ;
#77495=CARTESIAN_POINT ( 'NONE',  ( 29.70264281947218876, 3.584400861594816856, 28.19233905662918005 ) ) ;
#77498=LINE ( 'NONE', #61308, #62650 ) ;
#77508=CARTESIAN_POINT ( 'NONE',  ( 15.29947330337542688, 3.316774720514426456, -27.16854002387010070 ) ) ;
#77510=EDGE_CURVE ( 'NONE', #92435, #31493, #67864, .T. ) ;
#77520=ADVANCED_FACE ( 'NONE', ( #99770 ), #84068, .F. ) ;
#77532=DIRECTION ( 'NONE',  ( 0.000000000000000000, 0.000000000000000000, 1.000000000000000000 ) ) ;
#77560=AXIS2_PLACEMENT_3D ( 'NONE', #57244, #10541, #39995 ) ;
#77569=VECTOR ( 'NONE', #31215, 1000.000000000000000 ) ;
#77578=ORIENTED_EDGE ( 'NONE', *, *, #80369, .T. ) ;
#77583=CARTESIAN_POINT ( 'NONE',  ( -11.64875734969026233, 0.3587747205144265483, 30.51402280011862089 ) ) ;
#77587=ORIENTED_EDGE ( 'NONE', *, *, #55865, .F. ) ;
#77641=LINE ( 'NONE', #24367, #66995 ) ;
#77651=CARTESIAN_POINT ( 'NONE',  ( 11.22434917415779054, 4.132774715458839232, -26.87660878605755599 ) ) ;
#77670=DIRECTION ( 'NONE',  ( 1.000000000000000000, 0.000000000000000000, 0.000000000000000000 ) ) ;
#77672=DIRECTION ( 'NONE',  ( 0.000000000000000000, 0.000000000000000000, -1.000000000000000000 ) ) ;
#77683=CARTESIAN_POINT ( 'NONE',  ( 9.002841642506252740, 6.376774720514426065, -25.01329513651794656 ) ) ;
#77684=VECTOR ( 'NONE', #97285, 1000.000000000000000 ) ;
#77699=DIRECTION ( 'NONE',  ( -0.8264557562326033668, -6.845827386180409975E-16, -0.5630016722799281448 ) ) ;
#77717=CARTESIAN_POINT ( 'NONE',  ( 31.63608488009066733, 3.316774720514426456, 27.34773273846990804 ) ) ;
#77725=LINE ( 'NONE', #77225, #95614 ) ;
#77733=ORIENTED_EDGE ( 'NONE', *, *, #59058, .T. ) ;
#77740=DIRECTION ( 'NONE',  ( 1.232047923278981953E-16, -1.000000000000000000, 0.000000000000000000 ) ) ;
#77745=LINE ( 'NONE', #62055, #56260 ) ;
#77754=VERTEX_POINT ( 'NONE', #7439 ) ;
#77755=LINE ( 'NONE', #15367, #95749 ) ;
#77761=VECTOR ( 'NONE', #11862, 1000.000000000000000 ) ;
#77762=DIRECTION ( 'NONE',  ( -0.000000000000000000, -1.000000000000000000, -0.000000000000000000 ) ) ;
#77766=ORIENTED_EDGE ( 'NONE', *, *, #34693, .F. ) ;
#77769=ORIENTED_EDGE ( 'NONE', *, *, #67020, .F. ) ;
#77773=EDGE_LOOP ( 'NONE', ( #28837, #91360, #70159, #81483 ) ) ;
#77790=PLANE ( 'NONE',  #65766 ) ;
#77836=DIRECTION ( 'NONE',  ( 0.000000000000000000, -1.000000000000000000, 0.000000000000000000 ) ) ;
#77839=DIRECTION ( 'NONE',  ( -0.000000000000000000, -1.000000000000000000, -0.000000000000000000 ) ) ;
#77842=AXIS2_PLACEMENT_3D ( 'NONE', #88432, #88932, #56994 ) ;
#77860=ORIENTED_EDGE ( 'NONE', *, *, #81154, .F. ) ;
#77892=FACE_OUTER_BOUND ( 'NONE', #3427, .T. ) ;
#77907=LINE ( 'NONE', #46984, #2003 ) ;
#77918=AXIS2_PLACEMENT_3D ( 'NONE', #54127, #85051, #77427 ) ;
#77920=CARTESIAN_POINT ( 'NONE',  ( -32.30247028140506416, 1.684774720514426560, 27.60502002861223048 ) ) ;
#77928=CARTESIAN_POINT ( 'NONE',  ( 26.14999174255633463, 4.132774720517320866, -11.56127575336603286 ) ) ;
#77934=CARTESIAN_POINT ( 'NONE',  ( 1.175186991919851431, 0.3587747205144265483, 28.89597625626659649 ) ) ;
#77935=ADVANCED_FACE ( 'NONE', ( #38139 ), #44263, .T. ) ;
#77944=EDGE_CURVE ( 'NONE', #73404, #49834, #53386, .T. ) ;
#77946=DIRECTION ( 'NONE',  ( 7.109281096390894329E-15, 0.000000000000000000, 1.000000000000000000 ) ) ;
#77957=EDGE_CURVE ( 'NONE', #24998, #48069, #86408, .T. ) ;
#77959=CARTESIAN_POINT ( 'NONE',  ( 32.70752563734568952, 3.536205085657706082, -3.307643893017725212 ) ) ;
#77968=CARTESIAN_POINT ( 'NONE',  ( 32.53135143123563466, -5.965225279485572685, 6.926385399448451885 ) ) ;
#77982=EDGE_LOOP ( 'NONE', ( #25616, #71402, #50218, #20687 ) ) ;
#77997=ORIENTED_EDGE ( 'NONE', *, *, #24203, .F. ) ;
#77999=CARTESIAN_POINT ( 'NONE',  ( 14.70320764097967547, 3.414808732104102518, -28.39448918867740801 ) ) ;
#78001=ORIENTED_EDGE ( 'NONE', *, *, #81891, .T. ) ;
#78004=DIRECTION ( 'NONE',  ( 1.000000000000000000, 0.000000000000000000, 1.251281512149627050E-16 ) ) ;
#78020=ORIENTED_EDGE ( 'NONE', *, *, #22351, .F. ) ;
#78031=FACE_OUTER_BOUND ( 'NONE', #82737, .T. ) ;
#78036=CARTESIAN_POINT ( 'NONE',  ( 14.43441819135927950, 3.316774720514427344, -28.36222020317712378 ) ) ;
#78039=EDGE_CURVE ( 'NONE', #5376, #77258, #79710, .T. ) ;
#78044=EDGE_CURVE ( 'NONE', #38164, #97904, #93424, .T. ) ;
#78053=DIRECTION ( 'NONE',  ( -0.06283980576413537855, -0.000000000000000000, -0.9980236263794188822 ) ) ;
#78059=EDGE_CURVE ( 'NONE', #74051, #84269, #16307, .T. ) ;
#78084=EDGE_CURVE ( 'NONE', #33683, #94497, #86326, .T. ) ;
#78150=LINE ( 'NONE', #55351, #36601 ) ;
#78186=CARTESIAN_POINT ( 'NONE',  ( -23.62875734969026453, -6.143225279485574397, 24.50402280011862288 ) ) ;
#78190=CARTESIAN_POINT ( 'NONE',  ( 4.784292611721462585, 6.376774720514426953, -25.54547254883130947 ) ) ;
#78200=CARTESIAN_POINT ( 'NONE',  ( 14.76093561896378326, 3.316774720514426456, -26.55548769130088260 ) ) ;
#78204=CARTESIAN_POINT ( 'NONE',  ( 22.02124265030973760, 5.356774720514425603, 12.85402280011862430 ) ) ;
#78208=EDGE_CURVE ( 'NONE', #58683, #27962, #59382, .T. ) ;
#78213=CARTESIAN_POINT ( 'NONE',  ( -29.49875734969026198, -5.965225279485572685, 10.11402280011862587 ) ) ;
#78222=CARTESIAN_POINT ( 'NONE',  ( -65.05438548721848235, 6.376774720514426953, 30.51402280011862089 ) ) ;
#78230=CARTESIAN_POINT ( 'NONE',  ( 15.77315497053715987, 4.795106742339076078, -28.11009842133919534 ) ) ;
#78255=CIRCLE ( 'NONE', #55622, 130.7884398600581335 ) ;
#78356=CARTESIAN_POINT ( 'NONE',  ( 33.69795529655567634, 0.6647747205144264315, 23.11160796525322070 ) ) ;
#78362=LINE ( 'NONE', #33709, #84231 ) ;
#78366=LINE ( 'NONE', #18480, #58323 ) ;
#78367=DIRECTION ( 'NONE',  ( 0.000000000000000000, -1.000000000000000000, 0.000000000000000000 ) ) ;
#78392=CARTESIAN_POINT ( 'NONE',  ( 0.000000000000000000, -1.473225279485573802, 0.000000000000000000 ) ) ;
#78402=VERTEX_POINT ( 'NONE', #40036 ) ;
#78404=EDGE_CURVE ( 'NONE', #54320, #74213, #88222, .T. ) ;
#78424=DIRECTION ( 'NONE',  ( -0.7682573101345366862, 0.000000000000000000, 0.6401411605457395515 ) ) ;
#78425=CARTESIAN_POINT ( 'NONE',  ( 0.000000000000000000, -1.473225279485573802, 0.000000000000000000 ) ) ;
#78434=DIRECTION ( 'NONE',  ( -0.000000000000000000, -1.000000000000000000, -0.000000000000000000 ) ) ;
#78442=FACE_OUTER_BOUND ( 'NONE', #79245, .T. ) ;
#78447=CARTESIAN_POINT ( 'NONE',  ( 15.97264540888995299, 3.405665504423739609, -27.93485543958162864 ) ) ;
#78449=CARTESIAN_POINT ( 'NONE',  ( 14.61581670307174008, -6.475225279485573360, -27.35847990810646024 ) ) ;
#78463=CARTESIAN_POINT ( 'NONE',  ( 15.32643653063177958, 2.682774720514426559, -27.14485409495429380 ) ) ;
#78468=DIRECTION ( 'NONE',  ( 0.9161084732596779245, -5.365801633547218220E-16, -0.4009304992412300317 ) ) ;
#78489=ORIENTED_EDGE ( 'NONE', *, *, #61931, .T. ) ;
#78496=VERTEX_POINT ( 'NONE', #81096 ) ;
#78497=CARTESIAN_POINT ( 'NONE',  ( 29.71896661235086157, 4.666145129001815661, 27.69970538640514235 ) ) ;
#78512=ORIENTED_EDGE ( 'NONE', *, *, #35220, .T. ) ;
#78555=CARTESIAN_POINT ( 'NONE',  ( 15.10352928271630724, 2.682774720514426559, -27.29968155418892195 ) ) ;
#78563=CARTESIAN_POINT ( 'NONE',  ( -0.02075734969026423599, -6.475225279485573360, -0.08597719988137648983 ) ) ;
#78583=ORIENTED_EDGE ( 'NONE', *, *, #50981, .F. ) ;
#78591=FACE_OUTER_BOUND ( 'NONE', #9971, .T. ) ;
#78604=EDGE_CURVE ( 'NONE', #91590, #94426, #42555, .T. ) ;
#78621=VERTEX_POINT ( 'NONE', #4970 ) ;
#78639=EDGE_LOOP ( 'NONE', ( #88983, #26260, #28121, #71056 ) ) ;
#78652=EDGE_CURVE ( 'NONE', #57426, #59325, #75461, .T. ) ;
#78663=LINE ( 'NONE', #40130, #62170 ) ;
#78666=DIRECTION ( 'NONE',  ( 0.000000000000000000, -1.000000000000000000, 0.000000000000000000 ) ) ;
#78673=CARTESIAN_POINT ( 'NONE',  ( -28.47875734969025885, -5.965225279485572685, -0.08597719988137300651 ) ) ;
#78674=ORIENTED_EDGE ( 'NONE', *, *, #10960, .T. ) ;
#78679=AXIS2_PLACEMENT_3D ( 'NONE', #99916, #60897, #69991 ) ;
#78684=CARTESIAN_POINT ( 'NONE',  ( 7.822518687475809251, 6.376774720514094774, -28.18023264526767591 ) ) ;
#78685=EDGE_CURVE ( 'NONE', #88761, #13521, #36915, .T. ) ;
#78693=CARTESIAN_POINT ( 'NONE',  ( -41.32836283488544638, -2.803225279485573207, 39.26872235229541985 ) ) ;
#78697=ORIENTED_EDGE ( 'NONE', *, *, #29367, .T. ) ;
#78701=LINE ( 'NONE', #37662, #81803 ) ;
#78715=EDGE_CURVE ( 'NONE', #62896, #88543, #44030, .T. ) ;
#78748=AXIS2_PLACEMENT_3D ( 'NONE', #75351, #98691, #83466 ) ;
#78750=DIRECTION ( 'NONE',  ( -0.000000000000000000, 1.000000000000000000, -1.084202172485504434E-16 ) ) ;
#78766=CARTESIAN_POINT ( 'NONE',  ( 0.000000000000000000, -16.94322527948557422, 0.000000000000000000 ) ) ;
#78776=CIRCLE ( 'NONE', #62580, 27.94799999999999685 ) ;
#78780=ORIENTED_EDGE ( 'NONE', *, *, #76913, .F. ) ;
#78781=CARTESIAN_POINT ( 'NONE',  ( 10.86264265030973952, 0.3587747205144257157, -28.64597719988137570 ) ) ;
#78793=DIRECTION ( 'NONE',  ( -0.000000000000000000, 1.000000000000000000, -0.000000000000000000 ) ) ;
#78803=CARTESIAN_POINT ( 'NONE',  ( 4.784292611718076849, 5.356774720514425603, -25.54547254883186014 ) ) ;
#78810=DIRECTION ( 'NONE',  ( 0.000000000000000000, -1.000000000000000000, 0.000000000000000000 ) ) ;
#78811=AXIS2_PLACEMENT_3D ( 'NONE', #90355, #67530, #27958 ) ;
#78812=AXIS2_PLACEMENT_3D ( 'NONE', #71787, #58074, #47949 ) ;
#78821=AXIS2_PLACEMENT_3D ( 'NONE', #20067, #43425, #52522 ) ;
#78834=ORIENTED_EDGE ( 'NONE', *, *, #17185, .F. ) ;
#78836=CARTESIAN_POINT ( 'NONE',  ( 30.53060340732035982, 4.594240983522013266, 19.84760796525321780 ) ) ;
#78837=CARTESIAN_POINT ( 'NONE',  ( 22.81105451610979173, 500000.0000000000582, -18.46691820600746681 ) ) ;
#78849=CIRCLE ( 'NONE', #75662, 3.349999999999998757 ) ;
#78861=VERTEX_POINT ( 'NONE', #9965 ) ;
#78867=ORIENTED_EDGE ( 'NONE', *, *, #64465, .T. ) ;
#78872=VECTOR ( 'NONE', #42666, 1000.000000000000000 ) ;
#78877=DIRECTION ( 'NONE',  ( -0.000000000000000000, -0.000000000000000000, -1.000000000000000000 ) ) ;
#78883=ORIENTED_EDGE ( 'NONE', *, *, #20660, .F. ) ;
#78886=DIRECTION ( 'NONE',  ( 1.420947339892994047E-14, 0.000000000000000000, -1.000000000000000000 ) ) ;
#78889=VECTOR ( 'NONE', #56217, 1000.000000000000000 ) ;
#78893=AXIS2_PLACEMENT_3D ( 'NONE', #86644, #406, #31357 ) ;
#78909=CARTESIAN_POINT ( 'NONE',  ( -17.66201745896767505, -5.965225279485572685, -23.06272557202527906 ) ) ;
#78912=CARTESIAN_POINT ( 'NONE',  ( -19.69812919673063689, -5.965225279485592225, -22.00173861453435720 ) ) ;
#78921=DIRECTION ( 'NONE',  ( -0.000000000000000000, 1.000000000000000000, -0.000000000000000000 ) ) ;
#78924=CIRCLE ( 'NONE', #25476, 3.060000000000000053 ) ;
#78949=CARTESIAN_POINT ( 'NONE',  ( -27.25988310792305214, 0.3587747205144265483, 30.32664379231667695 ) ) ;
#78960=CARTESIAN_POINT ( 'NONE',  ( 33.74607884027702909, -5.965225279485572685, -4.999864028243830916 ) ) ;
#78973=EDGE_CURVE ( 'NONE', #50260, #56810, #25514, .T. ) ;
#78974=ORIENTED_EDGE ( 'NONE', *, *, #46423, .F. ) ;
#78981=ORIENTED_EDGE ( 'NONE', *, *, #47135, .F. ) ;
#78991=VERTEX_POINT ( 'NONE', #78781 ) ;
#78996=ORIENTED_EDGE ( 'NONE', *, *, #30315, .F. ) ;
#79022=CARTESIAN_POINT ( 'NONE',  ( 9.402885806365684829, -5.965225279485572685, 29.04108526060719342 ) ) ;
#79026=ORIENTED_EDGE ( 'NONE', *, *, #46736, .T. ) ;
#79034=ORIENTED_EDGE ( 'NONE', *, *, #78044, .F. ) ;
#79035=CARTESIAN_POINT ( 'NONE',  ( 282.9764569301858046, 6.376774720514426953, 20.79159422840526616 ) ) ;
#79072=CARTESIAN_POINT ( 'NONE',  ( 14.52511747680497933, -6.475225279485573360, -27.86035006098926559 ) ) ;
#79078=DIRECTION ( 'NONE',  ( 0.000000000000000000, 1.000000000000000000, 0.000000000000000000 ) ) ;
#79086=CARTESIAN_POINT ( 'NONE',  ( 33.29716795723528833, 4.396921096972350007, -11.57973373708315989 ) ) ;
#79095=PLANE ( 'NONE',  #4180 ) ;
#79113=ORIENTED_EDGE ( 'NONE', *, *, #18962, .T. ) ;
#79114=AXIS2_PLACEMENT_3D ( 'NONE', #72367, #59506, #12310 ) ;
#79120=DIRECTION ( 'NONE',  ( 1.000000000000000000, 0.000000000000000000, -0.000000000000000000 ) ) ;
#79125=LINE ( 'NONE', #72037, #23704 ) ;
#79128=ORIENTED_EDGE ( 'NONE', *, *, #21402, .F. ) ;
#79136=ORIENTED_EDGE ( 'NONE', *, *, #66629, .F. ) ;
#79145=CARTESIAN_POINT ( 'NONE',  ( 15.29947330337542688, 3.316774720514426456, -27.16854002387010070 ) ) ;
#79152=ORIENTED_EDGE ( 'NONE', *, *, #46684, .T. ) ;
#79153=ORIENTED_EDGE ( 'NONE', *, *, #5776, .F. ) ;
#79160=FACE_BOUND ( 'NONE', #38463, .T. ) ;
#79197=CARTESIAN_POINT ( 'NONE',  ( 29.73860345376319358, 14.82721238576592704, -4.021109907510727943 ) ) ;
#79200=EDGE_LOOP ( 'NONE', ( #37979, #22315, #23380, #97305 ) ) ;
#79209=DIRECTION ( 'NONE',  ( -0.000000000000000000, 1.000000000000000000, -0.000000000000000000 ) ) ;
#79215=ORIENTED_EDGE ( 'NONE', *, *, #71662, .F. ) ;
#79227=CIRCLE ( 'NONE', #32304, 1.149999999999998135 ) ;
#79230=CARTESIAN_POINT ( 'NONE',  ( 31.68813401132594976, 4.191046033661508297, 29.35543347196376729 ) ) ;
#79232=VECTOR ( 'NONE', #91122, 1000.000000000000000 ) ;
#79234=EDGE_LOOP ( 'NONE', ( #66133, #67694, #3052, #51917 ) ) ;
#79245=EDGE_LOOP ( 'NONE', ( #2147, #75872, #43840, #39728, #91351 ) ) ;
#79247=AXIS2_PLACEMENT_3D ( 'NONE', #57041, #42812, #79349 ) ;
#79262=ORIENTED_EDGE ( 'NONE', *, *, #20090, .F. ) ;
#79263=DIRECTION ( 'NONE',  ( 0.000000000000000000, 0.000000000000000000, -1.000000000000000000 ) ) ;
#79268=CARTESIAN_POINT ( 'NONE',  ( 11.62916340711181284, 0.3587747205144265483, 28.75961759920349792 ) ) ;
#79279=FACE_OUTER_BOUND ( 'NONE', #87627, .T. ) ;
#79284=CARTESIAN_POINT ( 'NONE',  ( 25.13432252085998186, 4.913094919796972881, -10.17719671683694571 ) ) ;
#79289=ORIENTED_EDGE ( 'NONE', *, *, #52750, .T. ) ;
#79296=CYLINDRICAL_SURFACE ( 'NONE', #4876, 129.7684398600581517 ) ;
#79306=ORIENTED_EDGE ( 'NONE', *, *, #16129, .T. ) ;
#79310=AXIS2_PLACEMENT_3D ( 'NONE', #17494, #57578, #71793 ) ;
#79327=CARTESIAN_POINT ( 'NONE',  ( 11.62916340711181284, -5.965225279485572685, 28.75961759920349792 ) ) ;
#79349=DIRECTION ( 'NONE',  ( 0.000000000000000000, 0.000000000000000000, -1.000000000000000000 ) ) ;
#79372=VECTOR ( 'NONE', #11991, 1000.000000000000000 ) ;
#79373=EDGE_LOOP ( 'NONE', ( #85991, #100010, #27847, #79535 ) ) ;
#79376=FACE_OUTER_BOUND ( 'NONE', #35692, .T. ) ;
#79380=VECTOR ( 'NONE', #40852, 1000.000000000000000 ) ;
#79388=DIRECTION ( 'NONE',  ( 0.000000000000000000, 0.000000000000000000, -1.000000000000000000 ) ) ;
#79390=DIRECTION ( 'NONE',  ( -0.000000000000000000, 1.000000000000000000, -0.000000000000000000 ) ) ;
#79396=ORIENTED_EDGE ( 'NONE', *, *, #50409, .F. ) ;
#79399=ORIENTED_EDGE ( 'NONE', *, *, #90567, .T. ) ;
#79419=CARTESIAN_POINT ( 'NONE',  ( 27.86270917940689174, 0.3587747205144265483, 29.49402280011862487 ) ) ;
#79431=CARTESIAN_POINT ( 'NONE',  ( 31.25756411700558601, 5.804570343751186634, -1.813502816810933949 ) ) ;
#79437=EDGE_CURVE ( 'NONE', #39077, #31334, #15006, .T. ) ;
#79440=DIRECTION ( 'NONE',  ( -0.000000000000000000, 1.000000000000000000, -0.000000000000000000 ) ) ;
#79442=AXIS2_PLACEMENT_3D ( 'NONE', #7236, #69143, #68656 ) ;
#79450=CARTESIAN_POINT ( 'NONE',  ( 5.097264368844747651, 3.299463065352477908, -27.56135813788838718 ) ) ;
#79458=DIRECTION ( 'NONE',  ( 0.000000000000000000, -1.000000000000000000, 0.000000000000000000 ) ) ;
#79500=ORIENTED_EDGE ( 'NONE', *, *, #25130, .T. ) ;
#79511=DIRECTION ( 'NONE',  ( -0.9496245541219264785, -6.845827386180410961E-16, -0.3133898629642195011 ) ) ;
#79519=VERTEX_POINT ( 'NONE', #69299 ) ;
#79532=PLANE ( 'NONE',  #44882 ) ;
#79535=ORIENTED_EDGE ( 'NONE', *, *, #92795, .F. ) ;
#79538=PLANE ( 'NONE',  #92791 ) ;
#79540=AXIS2_PLACEMENT_3D ( 'NONE', #804, #77410, #47486 ) ;
#79545=VERTEX_POINT ( 'NONE', #31232 ) ;
#79548=EDGE_CURVE ( 'NONE', #55067, #44101, #30729, .T. ) ;
#79550=DIRECTION ( 'NONE',  ( -1.000000000000000000, 0.000000000000000000, -0.000000000000000000 ) ) ;
#79555=EDGE_CURVE ( 'NONE', #74261, #61510, #23605, .T. ) ;
#79566=DIRECTION ( 'NONE',  ( -0.4009304992412300317, -6.845827386180410961E-16, -0.9161084732596779245 ) ) ;
#79593=VERTEX_POINT ( 'NONE', #95138 ) ;
#79598=CARTESIAN_POINT ( 'NONE',  ( -22.05275734969026047, -5.965225279485572685, 31.02402280011862246 ) ) ;
#79629=VERTEX_POINT ( 'NONE', #34740 ) ;
#79652=AXIS2_PLACEMENT_3D ( 'NONE', #90072, #22528, #5329 ) ;
#79667=ORIENTED_EDGE ( 'NONE', *, *, #62556, .F. ) ;
#79682=CARTESIAN_POINT ( 'NONE',  ( 1.408343819019456028E-16, -16.94322527948557422, 1.149999999999999911 ) ) ;
#79699=DIRECTION ( 'NONE',  ( -0.000000000000000000, -0.000000000000000000, -1.000000000000000000 ) ) ;
#79706=AXIS2_PLACEMENT_3D ( 'NONE', #96635, #66222, #97632 ) ;
#79710=LINE ( 'NONE', #70102, #73457 ) ;
#79729=B_SPLINE_CURVE_WITH_KNOTS ( 'NONE', 3,
 ( #76596, #60906, #36052, #75595, #21312, #51785 ),
 .UNSPECIFIED., .F., .F.,
 ( 4, 2, 4 ),
 ( 0.004212217532642030179, 0.005885052055372081044, 0.007557886578102131908 ),
 .UNSPECIFIED. ) ;
#79746=VERTEX_POINT ( 'NONE', #69680 ) ;
#79763=CARTESIAN_POINT ( 'NONE',  ( -10.21384395349166496, -6.475225279485573360, 29.49402280011861777 ) ) ;
#79766=FACE_OUTER_BOUND ( 'NONE', #45472, .T. ) ;
#79777=DIRECTION ( 'NONE',  ( -1.000000000000000000, 0.000000000000000000, -0.000000000000000000 ) ) ;
#79805=DIRECTION ( 'NONE',  ( 0.000000000000000000, 0.000000000000000000, 1.000000000000000000 ) ) ;
#79818=VECTOR ( 'NONE', #51763, 1000.000000000000000 ) ;
#79832=VERTEX_POINT ( 'NONE', #37233 ) ;
#79861=CARTESIAN_POINT ( 'NONE',  ( 22.02124265030973760, -4.543225279485573864, 16.20402280011862217 ) ) ;
#79865=ORIENTED_EDGE ( 'NONE', *, *, #20668, .F. ) ;
#79866=DIRECTION ( 'NONE',  ( 0.000000000000000000, 1.000000000000000000, 0.000000000000000000 ) ) ;
#79879=EDGE_CURVE ( 'NONE', #36769, #65212, #162, .T. ) ;
#79884=DIRECTION ( 'NONE',  ( -0.7071067811865474617, 0.000000000000000000, -0.7071067811865474617 ) ) ;
#79885=DIRECTION ( 'NONE',  ( -0.000000000000000000, -1.000000000000000000, 0.000000000000000000 ) ) ;
#79894=ORIENTED_EDGE ( 'NONE', *, *, #28693, .T. ) ;
#79911=VERTEX_POINT ( 'NONE', #91010 ) ;
#79919=EDGE_CURVE ( 'NONE', #39840, #24258, #38836, .T. ) ;
#79922=CARTESIAN_POINT ( 'NONE',  ( 14.76093561896379214, -5.965225279485572685, -26.55548769130089681 ) ) ;
#79923=ORIENTED_EDGE ( 'NONE', *, *, #14540, .T. ) ;
#79933=CARTESIAN_POINT ( 'NONE',  ( 30.32108885906865936, 6.376774720514426953, 3.274824222184972822 ) ) ;
#79938=CIRCLE ( 'NONE', #68570, 2.249999999999998668 ) ;
#79940=ORIENTED_EDGE ( 'NONE', *, *, #84721, .T. ) ;
#79955=CARTESIAN_POINT ( 'NONE',  ( 14.76093561896379214, 3.316774720514426456, -26.55548769130089681 ) ) ;
#79962=VECTOR ( 'NONE', #66888, 1000.000000000000227 ) ;
#79963=DIRECTION ( 'NONE',  ( -0.8264557562326033668, -6.845827386180409975E-16, -0.5630016722799281448 ) ) ;
#79965=CARTESIAN_POINT ( 'NONE',  ( 15.31892417638225012, 3.658177093025726023, -28.50911884272268182 ) ) ;
#79969=DIRECTION ( 'NONE',  ( 0.000000000000000000, -0.000000000000000000, -1.000000000000000000 ) ) ;
#79975=CARTESIAN_POINT ( 'NONE',  ( 30.64109438017208120, 3.316774720514426456, 28.31981406664616330 ) ) ;
#79980=ORIENTED_EDGE ( 'NONE', *, *, #62758, .T. ) ;
#79993=PLANE ( 'NONE',  #75413 ) ;
#80003=VERTEX_POINT ( 'NONE', #40727 ) ;
#80009=AXIS2_PLACEMENT_3D ( 'NONE', #68191, #61085, #99118 ) ;
#80017=VERTEX_POINT ( 'NONE', #47844 ) ;
#80024=ORIENTED_EDGE ( 'NONE', *, *, #87345, .F. ) ;
#80030=ORIENTED_EDGE ( 'NONE', *, *, #47278, .F. ) ;
#80033=DIRECTION ( 'NONE',  ( -0.000000000000000000, -1.000000000000000000, 0.000000000000000000 ) ) ;
#80036=ADVANCED_FACE ( 'NONE', ( #56473, #79279 ), #48855, .T. ) ;
#80048=ORIENTED_EDGE ( 'NONE', *, *, #30397, .T. ) ;
#80081=ORIENTED_EDGE ( 'NONE', *, *, #14933, .F. ) ;
#80097=CARTESIAN_POINT ( 'NONE',  ( 33.50227909998848475, 4.005981270903656188, -11.48786002470558643 ) ) ;
#80113=CARTESIAN_POINT ( 'NONE',  ( 32.53135143123563466, 0.3587747205144265483, 6.926385399448451885 ) ) ;
#80114=ADVANCED_FACE ( 'NONE', ( #88911 ), #96509, .F. ) ;
#80130=CARTESIAN_POINT ( 'NONE',  ( 30.53060340732036337, 1.682774720514426114, 3.744237563515920634E-15 ) ) ;
#80136=EDGE_CURVE ( 'NONE', #28190, #52365, #44727, .T. ) ;
#80140=AXIS2_PLACEMENT_3D ( 'NONE', #23802, #100408, #69983 ) ;
#80149=DIRECTION ( 'NONE',  ( 0.000000000000000000, -0.000000000000000000, -1.000000000000000000 ) ) ;
#80169=ORIENTED_EDGE ( 'NONE', *, *, #19140, .F. ) ;
#80173=CARTESIAN_POINT ( 'NONE',  ( 9.402885806365684829, -5.965225279485572685, 29.04108526060719342 ) ) ;
#80174=CARTESIAN_POINT ( 'NONE',  ( 0.000000000000000000, -16.94322527948557422, -1.149999999999999911 ) ) ;
#80196=CARTESIAN_POINT ( 'NONE',  ( 8.720681858489903959, 3.316774720514428232, -28.09278397295777197 ) ) ;
#80211=ORIENTED_EDGE ( 'NONE', *, *, #84654, .F. ) ;
#80218=FACE_OUTER_BOUND ( 'NONE', #51351, .T. ) ;
#80239=VERTEX_POINT ( 'NONE', #1052 ) ;
#80243=VERTEX_POINT ( 'NONE', #17779 ) ;
#80246=CARTESIAN_POINT ( 'NONE',  ( 15.09050776547575090, 3.531431454755690869, -27.29583770106899365 ) ) ;
#80252=ADVANCED_FACE ( 'NONE', ( #24875 ), #31994, .F. ) ;
#80268=DIRECTION ( 'NONE',  ( 0.000000000000000000, -0.000000000000000000, 1.000000000000000000 ) ) ;
#80273=EDGE_LOOP ( 'NONE', ( #46975, #6778, #66203, #38123 ) ) ;
#80289=CIRCLE ( 'NONE', #27061, 251.9358649670780892 ) ;
#80293=EDGE_LOOP ( 'NONE', ( #23795, #82687, #58071, #54458 ) ) ;
#80297=VECTOR ( 'NONE', #20836, 1000.000000000000000 ) ;
#80312=VERTEX_POINT ( 'NONE', #47225 ) ;
#80322=ORIENTED_EDGE ( 'NONE', *, *, #36947, .F. ) ;
#80335=LINE ( 'NONE', #97058, #62442 ) ;
#80349=VERTEX_POINT ( 'NONE', #80174 ) ;
#80361=AXIS2_PLACEMENT_3D ( 'NONE', #16570, #78468, #1866 ) ;
#80364=EDGE_CURVE ( 'NONE', #13454, #52986, #76063, .T. ) ;
#80365=ORIENTED_EDGE ( 'NONE', *, *, #44166, .F. ) ;
#80369=EDGE_CURVE ( 'NONE', #86861, #58117, #74549, .T. ) ;
#80371=CARTESIAN_POINT ( 'NONE',  ( -27.25988310792305214, -5.965225279485572685, 30.32664379231667695 ) ) ;
#80375=CARTESIAN_POINT ( 'NONE',  ( 9.679460662220623846, 4.838530677111208433, -26.38948590882341705 ) ) ;
#80378=CARTESIAN_POINT ( 'NONE',  ( 282.9764569301858046, 4.540774720514427543, 20.79159422840526616 ) ) ;
#80382=ORIENTED_EDGE ( 'NONE', *, *, #40627, .F. ) ;
#80384=LINE ( 'NONE', #85993, #100360 ) ;
#80386=CARTESIAN_POINT ( 'NONE',  ( 31.82032313667048484, -5.965225279485572685, 9.148483289431936782 ) ) ;
#80387=EDGE_CURVE ( 'NONE', #14248, #16991, #55079, .T. ) ;
#80391=CARTESIAN_POINT ( 'NONE',  ( -19.80875734969026425, -5.965225279485572685, 31.02402280011862246 ) ) ;
#80420=VECTOR ( 'NONE', #79458, 1000.000000000000000 ) ;
#80425=DIRECTION ( 'NONE',  ( 0.000000000000000000, 0.000000000000000000, -1.000000000000000000 ) ) ;
#80434=CIRCLE ( 'NONE', #78812, 91.74549126261078413 ) ;
#80444=CARTESIAN_POINT ( 'NONE',  ( 0.000000000000000000, 1.826774720514426464, 0.000000000000000000 ) ) ;
#80445=EDGE_LOOP ( 'NONE', ( #8990, #11639, #94502 ) ) ;
#80450=CARTESIAN_POINT ( 'NONE',  ( 15.58962545129234556, 1.684774720514426560, -26.91365498785467736 ) ) ;
#80460=CARTESIAN_POINT ( 'NONE',  ( 33.74124265030975067, 3.622774720514426949, -12.32597719988138252 ) ) ;
#80461=CARTESIAN_POINT ( 'NONE',  ( 14.85834502026402681, 2.682774720514426559, -27.37203305628894867 ) ) ;
#80480=EDGE_LOOP ( 'NONE', ( #58457, #39681, #88360, #2386 ) ) ;
#80481=FACE_OUTER_BOUND ( 'NONE', #16017, .T. ) ;
#80488=ORIENTED_EDGE ( 'NONE', *, *, #86302, .T. ) ;
#80495=CARTESIAN_POINT ( 'NONE',  ( 9.315600972258334167, 0.3587747205144265483, 28.35070303307545458 ) ) ;
#80505=ORIENTED_EDGE ( 'NONE', *, *, #28523, .T. ) ;
#80509=CARTESIAN_POINT ( 'NONE',  ( 14.63527791052757898, 4.349658986764157298, -28.08406249416238154 ) ) ;
#80515=AXIS2_PLACEMENT_3D ( 'NONE', #52850, #31504, #38618 ) ;
#80540=LINE ( 'NONE', #88665, #31231 ) ;
#80541=ORIENTED_EDGE ( 'NONE', *, *, #83324, .F. ) ;
#80558=CARTESIAN_POINT ( 'NONE',  ( 31.82032313667048484, 0.3587747205144265483, 9.148483289431938559 ) ) ;
#80565=CARTESIAN_POINT ( 'NONE',  ( -22.05275734969026047, -5.965225279485572685, 30.51402280011862089 ) ) ;
#80595=LINE ( 'NONE', #82097, #54225 ) ;
#80606=CARTESIAN_POINT ( 'NONE',  ( 33.74607884027702909, -5.965225279485572685, -4.999864028243830916 ) ) ;
#80608=AXIS2_PLACEMENT_3D ( 'NONE', #64242, #41384, #33768 ) ;
#80630=AXIS2_PLACEMENT_3D ( 'NONE', #31400, #92788, #30393 ) ;
#80644=VERTEX_POINT ( 'NONE', #27649 ) ;
#80658=DIRECTION ( 'NONE',  ( 0.000000000000000000, 1.000000000000000000, 0.000000000000000000 ) ) ;
#80675=ORIENTED_EDGE ( 'NONE', *, *, #98511, .F. ) ;
#80678=CARTESIAN_POINT ( 'NONE',  ( 22.81105451610979173, -6.475225279485573360, -18.46691820600746681 ) ) ;
#80679=AXIS2_PLACEMENT_3D ( 'NONE', #74913, #28758, #59721 ) ;
#80694=EDGE_LOOP ( 'NONE', ( #20983, #71907, #9509, #14990 ) ) ;
#80695=CARTESIAN_POINT ( 'NONE',  ( 30.53060340732036693, 4.132774720514426292, -2.322449884495168870 ) ) ;
#80719=VECTOR ( 'NONE', #29969, 1000.000000000000000 ) ;
#80721=CARTESIAN_POINT ( 'NONE',  ( 26.73860345374794534, 5.058662225110310828, -7.113848178280766099 ) ) ;
#80735=PLANE ( 'NONE',  #15363 ) ;
#80736=DIRECTION ( 'NONE',  ( 0.000000000000000000, 0.000000000000000000, -1.000000000000000000 ) ) ;
#80740=CARTESIAN_POINT ( 'NONE',  ( 14.66599494348427335, 4.455096676454847859, -28.01208847159952597 ) ) ;
#80747=CARTESIAN_POINT ( 'NONE',  ( 31.63284457977613684, 3.861502214243257125, 27.22238481897691287 ) ) ;
#80761=CARTESIAN_POINT ( 'NONE',  ( -28.84663072490566194, 0.3587747205144265483, 28.73989617533406715 ) ) ;
#80767=ORIENTED_EDGE ( 'NONE', *, *, #80387, .T. ) ;
#80768=DIRECTION ( 'NONE',  ( -0.000000000000000000, -1.000000000000000000, 0.000000000000000000 ) ) ;
#80769=DIRECTION ( 'NONE',  ( -0.000000000000000000, -1.000000000000000000, -0.000000000000000000 ) ) ;
#80774=LINE ( 'NONE', #10762, #48273 ) ;
#80795=CARTESIAN_POINT ( 'NONE',  ( 33.96422015159436114, -5.965225279485572685, -7.233236000911337449 ) ) ;
#80798=FACE_OUTER_BOUND ( 'NONE', #10385, .T. ) ;
#80803=FACE_OUTER_BOUND ( 'NONE', #30705, .T. ) ;
#80804=AXIS2_PLACEMENT_3D ( 'NONE', #19804, #29418, #98422 ) ;
#80810=CARTESIAN_POINT ( 'NONE',  ( 22.02124265030973760, -4.543225279485573864, 16.20402280011862217 ) ) ;
#80840=VECTOR ( 'NONE', #59393, 1000.000000000000227 ) ;
#80863=CARTESIAN_POINT ( 'NONE',  ( -29.49875734969025842, -5.965225279485572685, 25.61802280011862720 ) ) ;
#80867=ORIENTED_EDGE ( 'NONE', *, *, #22011, .F. ) ;
#80877=CLOSED_SHELL ( 'NONE', ( #1910, #92787, #84652, #53974, #26051, #45781, #34373, #98017, #20662, #80252, #31646, #37733, #41180, #55843, #9446, #56864, #82899, #27569, #72945, #80986, #88383, #99523, #68833, #92213, #27096, #50716, #15985, #55219, #88629, #7517, #37861, #51615, #50791, #73289, #38084, #8231, #16074, #30367, #75123, #8429, #59525, #20387, #5536, #22539, #51390, #96279, #65947, #1451, #19295, #74311, #8806, #96641, #11283, #41940, #84264, #54827, #12705, #18150, #57168, #76065, #46578, #3524, #100413, #94224, #14410, #10204, #81825, #8416, #64320, #76379, #83702, #91263, #70040, #69497, #8104, #83508, #800, #88263, #54409, #38415, #39664, #4662, #32044, #19102, #42763, #22806, #49239, #7444, #41690, #72722, #95711, #55852, #48990, #94797, #72236, #30408, #67894, #12934, #64373, #72481, #71546, #16654, #86557, #3166, #54964, #57373, #88572, #22917, #14288, #57728, #38817, #84497, #91028, #31796, #74732, #60680, #19984, #49661, #75623, #83081, #68388, #77935, #16419, #69508, #86814, #4707, #37212, #100192, #49129, #55728, #76172, #97656, #44987, #54507, #31259, #80945, #87815, #62445, #73298, #74071, #28806, #64426, #50910, #9319, #10384, #57274, #50610, #48530, #10715, #21137, #60263, #80114, #77520, #19225, #87454, #91253, #64415, #47698, #15635, #96770, #93299, #1897, #88849, #60262, #83218, #28691, #6839, #16543, #24278, #19655, #70332, #45178, #43771, #53849, #21803, #29135, #52417, #69261, #90464, #72231, #39485, #97268, #28182, #49590, #19723, #82259, #75106, #83810, #48325, #75371, #64538, #11348, #38647, #73615, #55568, #99026, #33628, #52647, #26643, #34221, #75748, #72011, #84958, #83047, #18208, #19339, #67899, #91398, #22609, #26858, #60774, #53053, #64634, #28147, #68450, #58610, #39835, #35874, #5906, #34811, #88843, #52075, #21667, #95951, #32649, #12242, #54390, #54594, #68096, #10721, #22947, #58520, #12087, #98094, #54463, #99730, #88610, #17135, #53359, #41085, #37275, #76254, #43590, #32720, #84279, #37143, #82362, #12001, #81883, #6356, #11268, #85162, #36938, #41897, #60222, #39567, #67533, #2520, #22534, #21516, #99463, #68900, #8423, #17245, #57121, #7851, #82668, #58055, #14806, #46569, #22056, #39361, #54702, #28759, #20681, #84469, #83512, #80036, #95772, #68455, #54074, #73849, #18569 ) ) ;
#80890=CARTESIAN_POINT ( 'NONE',  ( 11.56983764158150407, 0.3587747205144265483, 28.29037853177889517 ) ) ;
#80900=DIRECTION ( 'NONE',  ( -0.000000000000000000, -1.000000000000000000, -0.000000000000000000 ) ) ;
#80920=VECTOR ( 'NONE', #28111, 1000.000000000000000 ) ;
#80923=AXIS2_PLACEMENT_3D ( 'NONE', #78222, #54405, #10229 ) ;
#80927=DIRECTION ( 'NONE',  ( -0.9831680378442393398, 0.000000000000000000, -0.1827036106964188000 ) ) ;
#80945=ADVANCED_FACE ( 'NONE', ( #54472 ), #85408, .F. ) ;
#80973=AXIS2_PLACEMENT_3D ( 'NONE', #43508, #74446, #4937 ) ;
#80984=CIRCLE ( 'NONE', #90690, 1.530000000000002469 ) ;
#80985=ORIENTED_EDGE ( 'NONE', *, *, #48552, .F. ) ;
#80986=ADVANCED_FACE ( 'NONE', ( #56987 ), #79296, .F. ) ;
#80998=AXIS2_PLACEMENT_3D ( 'NONE', #8290, #84908, #46355 ) ;
#81022=VERTEX_POINT ( 'NONE', #10294 ) ;
#81033=CARTESIAN_POINT ( 'NONE',  ( -24.90875734969025501, 5.356774720514425603, 26.43402280011862615 ) ) ;
#81056=LINE ( 'NONE', #11538, #34059 ) ;
#81077=CARTESIAN_POINT ( 'NONE',  ( -24.90875734969025501, -6.475225279485573360, 26.43402280011862615 ) ) ;
#81093=CARTESIAN_POINT ( 'NONE',  ( 10.24966870126729646, -6.475225279485571583, -27.02528057709740850 ) ) ;
#81096=CARTESIAN_POINT ( 'NONE',  ( -23.31187512739357715, 0.3587747205144061202, -17.31005501743528541 ) ) ;
#81101=ORIENTED_EDGE ( 'NONE', *, *, #87842, .T. ) ;
#81111=AXIS2_PLACEMENT_3D ( 'NONE', #14999, #93117, #39838 ) ;
#81138=ORIENTED_EDGE ( 'NONE', *, *, #65147, .F. ) ;
#81141=EDGE_CURVE ( 'NONE', #35597, #32574, #34068, .T. ) ;
#81147=CARTESIAN_POINT ( 'NONE',  ( 0.000000000000000000, -16.94322527948557422, 0.000000000000000000 ) ) ;
#81154=EDGE_CURVE ( 'NONE', #82392, #64064, #25736, .T. ) ;
#81205=CARTESIAN_POINT ( 'NONE',  ( 5.101312121039179637, 3.305285905532577839, -27.56070534847060571 ) ) ;
#81215=CARTESIAN_POINT ( 'NONE',  ( 11.29837800214456855, 4.960377205085137575, -27.59811486027058436 ) ) ;
#81221=DIRECTION ( 'NONE',  ( -0.000000000000000000, -1.000000000000000000, 0.000000000000000000 ) ) ;
#81233=CARTESIAN_POINT ( 'NONE',  ( 15.12110981444426372, 4.119741627009140927, -28.36351442485845453 ) ) ;
#81235=DIRECTION ( 'NONE',  ( -0.6392559695863496705, -6.845827386180411947E-16, -0.7689940216596069522 ) ) ;
#81240=CARTESIAN_POINT ( 'NONE',  ( 31.68084058116266988, 4.801908866063379300, 29.09855526763849198 ) ) ;
#81247=CIRCLE ( 'NONE', #14813, 4.300000000000000711 ) ;
#81265=PLANE ( 'NONE',  #19139 ) ;
#81270=LINE ( 'NONE', #4655, #12446 ) ;
#81271=CARTESIAN_POINT ( 'NONE',  ( -28.98875734969026396, -5.965225279485572685, -0.08597719988137648983 ) ) ;
#81272=ORIENTED_EDGE ( 'NONE', *, *, #45308, .T. ) ;
#81293=DIRECTION ( 'NONE',  ( 0.000000000000000000, 0.000000000000000000, -1.000000000000000000 ) ) ;
#81326=VECTOR ( 'NONE', #28926, 1000.000000000000114 ) ;
#81343=ORIENTED_EDGE ( 'NONE', *, *, #13716, .T. ) ;
#81348=CARTESIAN_POINT ( 'NONE',  ( 29.68479148105952348, 4.772774720514425972, -9.431263391055120238 ) ) ;
#81381=ORIENTED_EDGE ( 'NONE', *, *, #10028, .F. ) ;
#81382=DIRECTION ( 'NONE',  ( 0.000000000000000000, 1.000000000000000000, 0.000000000000000000 ) ) ;
#81386=EDGE_CURVE ( 'NONE', #17142, #78402, #54861, .T. ) ;
#81397=ORIENTED_EDGE ( 'NONE', *, *, #73194, .F. ) ;
#81411=DIRECTION ( 'NONE',  ( 0.9496245541219264785, 0.000000000000000000, 0.3133898629642195011 ) ) ;
#81421=CARTESIAN_POINT ( 'NONE',  ( 14.61581676225028126, 3.316774720514426456, -27.35847991880135766 ) ) ;
#81433=VECTOR ( 'NONE', #33777, 1000.000000000000000 ) ;
#81434=CARTESIAN_POINT ( 'NONE',  ( 31.52563388547018874, 4.132774720514424516, -1.605328387144967728 ) ) ;
#81444=CARTESIAN_POINT ( 'NONE',  ( 7.732492003039795669, 3.316774720515257791, -27.16032169665734486 ) ) ;
#81459=LINE ( 'NONE', #58130, #71508 ) ;
#81466=CARTESIAN_POINT ( 'NONE',  ( 17.51792015816173986, -5.965225279485572685, 29.01255224319336889 ) ) ;
#81479=CARTESIAN_POINT ( 'NONE',  ( 13.10664265030973930, -5.965225279485574461, -28.64597719988137570 ) ) ;
#81483=ORIENTED_EDGE ( 'NONE', *, *, #93228, .F. ) ;
#81512=ORIENTED_EDGE ( 'NONE', *, *, #83075, .T. ) ;
#81516=DIRECTION ( 'NONE',  ( 0.000000000000000000, -1.000000000000000000, 0.000000000000000000 ) ) ;
#81518=CARTESIAN_POINT ( 'NONE',  ( 14.79186724892429439, 4.799335165223686417, -27.67512533972776723 ) ) ;
#81524=EDGE_CURVE ( 'NONE', #93008, #80349, #43630, .T. ) ;
#81531=ORIENTED_EDGE ( 'NONE', *, *, #89096, .T. ) ;
#81542=DIRECTION ( 'NONE',  ( 0.000000000000000000, 0.000000000000000000, -1.000000000000000000 ) ) ;
#81552=ORIENTED_EDGE ( 'NONE', *, *, #25976, .F. ) ;
#81580=CARTESIAN_POINT ( 'NONE',  ( -17.64648606763744354, -5.965225279485594001, -23.04404205923972526 ) ) ;
#81583=VECTOR ( 'NONE', #38620, 1000.000000000000000 ) ;
#81615=DIRECTION ( 'NONE',  ( 0.7071067811865474617, 0.000000000000000000, 0.7071067811865474617 ) ) ;
#81638=ORIENTED_EDGE ( 'NONE', *, *, #99818, .T. ) ;
#81641=ORIENTED_EDGE ( 'NONE', *, *, #26756, .T. ) ;
#81645=AXIS2_PLACEMENT_3D ( 'NONE', #43141, #81698, #12170 ) ;
#81648=EDGE_LOOP ( 'NONE', ( #49559, #45952, #33655, #30579 ) ) ;
#81649=LINE ( 'NONE', #34974, #34812 ) ;
#81651=AXIS2_PLACEMENT_3D ( 'NONE', #29894, #38009, #60372 ) ;
#81697=CARTESIAN_POINT ( 'NONE',  ( 12.20502328318355545, 3.316774720514426011, -28.10533714397569582 ) ) ;
#81698=DIRECTION ( 'NONE',  ( 0.000000000000000000, 1.000000000000000000, -0.000000000000000000 ) ) ;
#81702=VERTEX_POINT ( 'NONE', #60861 ) ;
#81709=DIRECTION ( 'NONE',  ( 0.000000000000000000, 1.000000000000000000, -0.000000000000000000 ) ) ;
#81717=EDGE_LOOP ( 'NONE', ( #61833, #88149, #96465, #31176 ) ) ;
#81725=DIRECTION ( 'NONE',  ( 0.000000000000000000, -0.000000000000000000, -1.000000000000000000 ) ) ;
#81733=DIRECTION ( 'NONE',  ( 2.910297583984928910E-15, -1.000000000000000000, -3.056206645085457922E-15 ) ) ;
#81740=CARTESIAN_POINT ( 'NONE',  ( 29.62673903083957683, 5.344535611318891988, 28.45872576146958011 ) ) ;
#81741=AXIS2_PLACEMENT_3D ( 'NONE', #72032, #70519, #47689 ) ;
#81744=CARTESIAN_POINT ( 'NONE',  ( 15.26487859601603780, 3.572416542244653659, -27.19734615108692211 ) ) ;
#81755=DIRECTION ( 'NONE',  ( -0.000000000000000000, 1.000000000000000000, -0.000000000000000000 ) ) ;
#81756=CARTESIAN_POINT ( 'NONE',  ( 13.91401389203221406, -5.965225279485572685, 158.0376437107427137 ) ) ;
#81759=ORIENTED_EDGE ( 'NONE', *, *, #51163, .T. ) ;
#81783=ORIENTED_EDGE ( 'NONE', *, *, #53212, .F. ) ;
#81786=LINE ( 'NONE', #74175, #64388 ) ;
#81803=VECTOR ( 'NONE', #61013, 1000.000000000000000 ) ;
#81815=AXIS2_PLACEMENT_3D ( 'NONE', #61928, #61432, #38074 ) ;
#81823=CARTESIAN_POINT ( 'NONE',  ( 10.54812756816019892, 3.634129942730893070, -27.00766266717979747 ) ) ;
#81825=ADVANCED_FACE ( 'NONE', ( #83170 ), #29893, .T. ) ;
#81837=DIRECTION ( 'NONE',  ( 0.000000000000000000, 1.155373159085149695E-17, 1.000000000000000000 ) ) ;
#81867=DIRECTION ( 'NONE',  ( -0.000000000000000000, -0.000000000000000000, -1.000000000000000000 ) ) ;
#81883=ADVANCED_FACE ( 'NONE', ( #95297 ), #49143, .F. ) ;
#81887=LINE ( 'NONE', #59062, #14200 ) ;
#81891=EDGE_CURVE ( 'NONE', #47172, #83063, #70463, .T. ) ;
#81897=CARTESIAN_POINT ( 'NONE',  ( 31.35973677934181936, 4.378374783736292741, 0.3342810658314839256 ) ) ;
#81905=ORIENTED_EDGE ( 'NONE', *, *, #49, .F. ) ;
#81921=ORIENTED_EDGE ( 'NONE', *, *, #76019, .F. ) ;
#81932=ORIENTED_EDGE ( 'NONE', *, *, #98102, .T. ) ;
#81934=CARTESIAN_POINT ( 'NONE',  ( 5.865642684142210683, 5.356774720514426491, -25.36740469599890702 ) ) ;
#81947=EDGE_CURVE ( 'NONE', #67714, #85130, #16664, .T. ) ;
#81955=TOROIDAL_SURFACE ( 'NONE', #57866, 3.060000000000000053, 3.060000000000000053 ) ;
#81957=CARTESIAN_POINT ( 'NONE',  ( 14.78484767477523576, 3.316774720514427344, -28.43034250232788551 ) ) ;
#81974=CARTESIAN_POINT ( 'NONE',  ( 31.62034159138974232, 4.397688677369781196, -2.670054032269984834 ) ) ;
#81978=CARTESIAN_POINT ( 'NONE',  ( 29.73620800866979863, 5.101103159685075106, 27.18593991345460381 ) ) ;
#82004=VERTEX_POINT ( 'NONE', #88190 ) ;
#82017=VERTEX_POINT ( 'NONE', #28274 ) ;
#82018=CARTESIAN_POINT ( 'NONE',  ( 13.10664265030973930, 0.3587747205144256601, -27.62597719988137612 ) ) ;
#82023=VERTEX_POINT ( 'NONE', #3954 ) ;
#82028=DIRECTION ( 'NONE',  ( -0.7512896232465892110, 0.000000000000000000, -0.6599726524652350657 ) ) ;
#82034=AXIS2_PLACEMENT_3D ( 'NONE', #75200, #45758, #38132 ) ;
#82057=CARTESIAN_POINT ( 'NONE',  ( 31.27206728860909024, 4.132774720514318822, -3.930752063305056332 ) ) ;
#82074=EDGE_CURVE ( 'NONE', #20580, #12021, #4943, .T. ) ;
#82089=CARTESIAN_POINT ( 'NONE',  ( 12.16765770914787304, -6.475225279485573360, -27.57618308014988173 ) ) ;
#82091=CARTESIAN_POINT ( 'NONE',  ( 5.885012508251304730, -6.475225279485574248, -27.43431635654696521 ) ) ;
#82097=CARTESIAN_POINT ( 'NONE',  ( 10.86264265030973952, -5.965225279485574461, -28.64597719988137570 ) ) ;
#82116=CARTESIAN_POINT ( 'NONE',  ( 20.57455539870835537, 2.682774720514426559, -18.22080502500613974 ) ) ;
#82139=EDGE_CURVE ( 'NONE', #88045, #95809, #73043, .T. ) ;
#82140=ORIENTED_EDGE ( 'NONE', *, *, #18978, .T. ) ;
#82147=DIRECTION ( 'NONE',  ( -0.000000000000000000, -1.000000000000000000, -0.000000000000000000 ) ) ;
#82152=LINE ( 'NONE', #66464, #1053 ) ;
#82154=DIRECTION ( 'NONE',  ( 0.9978940991575084851, 0.000000000000000000, 0.06486421869277853025 ) ) ;
#82156=VERTEX_POINT ( 'NONE', #51120 ) ;
#82159=AXIS2_PLACEMENT_3D ( 'NONE', #64805, #57182, #50057 ) ;
#82169=CARTESIAN_POINT ( 'NONE',  ( 5.851028665930490646, -6.475225279485576024, -27.43979700150094558 ) ) ;
#82181=DIRECTION ( 'NONE',  ( -0.000000000000000000, 1.000000000000000000, -0.000000000000000000 ) ) ;
#82188=EDGE_CURVE ( 'NONE', #5380, #91850, #10555, .T. ) ;
#82217=DIRECTION ( 'NONE',  ( 0.000000000000000000, -1.000000000000000000, 0.000000000000000000 ) ) ;
#82220=CYLINDRICAL_SURFACE ( 'NONE', #37247, 2.249999999999998668 ) ;
#82221=DIRECTION ( 'NONE',  ( 0.000000000000000000, 0.000000000000000000, -1.000000000000000000 ) ) ;
#82224=VECTOR ( 'NONE', #81867, 1000.000000000000000 ) ;
#82233=CARTESIAN_POINT ( 'NONE',  ( 29.60459817610514932, 4.854569207680477838, 28.81138945959710185 ) ) ;
#82259=ADVANCED_FACE ( 'NONE', ( #75934 ), #82556, .F. ) ;
#82268=VERTEX_POINT ( 'NONE', #30262 ) ;
#82285=DIRECTION ( 'NONE',  ( -0.000000000000000000, -1.000000000000000000, -0.000000000000000000 ) ) ;
#82309=ORIENTED_EDGE ( 'NONE', *, *, #57848, .F. ) ;
#82319=CARTESIAN_POINT ( 'NONE',  ( 30.93860345374796594, -6.475225279485573360, 13.17908622612278613 ) ) ;
#82335=LINE ( 'NONE', #43293, #41089 ) ;
#82347=ORIENTED_EDGE ( 'NONE', *, *, #91709, .T. ) ;
#82353=ORIENTED_EDGE ( 'NONE', *, *, #72599, .F. ) ;
#82362=ADVANCED_FACE ( 'NONE', ( #38876 ), #86056, .T. ) ;
#82392=VERTEX_POINT ( 'NONE', #46499 ) ;
#82410=EDGE_CURVE ( 'NONE', #22977, #96621, #15534, .T. ) ;
#82418=CARTESIAN_POINT ( 'NONE',  ( 31.46635748159467383, 4.132774720514425404, -3.372935991075822759 ) ) ;
#82422=CARTESIAN_POINT ( 'NONE',  ( 29.80070917940689412, 6.376774720514426953, 27.39560796525321607 ) ) ;
#82427=CARTESIAN_POINT ( 'NONE',  ( 6.190876379491990988, 5.356774720513712396, -27.38145113946987408 ) ) ;
#82433=ORIENTED_EDGE ( 'NONE', *, *, #16129, .F. ) ;
#82441=EDGE_CURVE ( 'NONE', #97857, #32699, #63238, .T. ) ;
#82445=DIRECTION ( 'NONE',  ( 0.2488812114211667315, 0.000000000000000000, 0.9685340172660600322 ) ) ;
#82488=VERTEX_POINT ( 'NONE', #85550 ) ;
#82495=AXIS2_PLACEMENT_3D ( 'NONE', #1376, #71385, #31817 ) ;
#82499=DIRECTION ( 'NONE',  ( 0.7512896232465892110, -0.000000000000000000, 0.6599726524652350657 ) ) ;
#82531=EDGE_CURVE ( 'NONE', #43485, #10013, #17250, .T. ) ;
#82535=ORIENTED_EDGE ( 'NONE', *, *, #24587, .F. ) ;
#82546=ORIENTED_EDGE ( 'NONE', *, *, #92731, .T. ) ;
#82547=DIRECTION ( 'NONE',  ( -0.000000000000000000, -1.000000000000000000, -0.000000000000000000 ) ) ;
#82556=PLANE ( 'NONE',  #62684 ) ;
#82568=CARTESIAN_POINT ( 'NONE',  ( 30.93860345374796594, -6.475225279485573360, 19.84760796525321780 ) ) ;
#82569=VERTEX_POINT ( 'NONE', #39133 ) ;
#82580=CIRCLE ( 'NONE', #71216, 3.979149600822063704 ) ;
#82589=CARTESIAN_POINT ( 'NONE',  ( -2.768609665556983845, -5.965225279485594001, -29.41086200512614823 ) ) ;
#82594=CARTESIAN_POINT ( 'NONE',  ( -19.80875734969026425, 0.3587747205144265483, 31.02402280011862246 ) ) ;
#82606=DIRECTION ( 'NONE',  ( -0.000000000000000000, 1.000000000000000000, -0.000000000000000000 ) ) ;
#82635=DIRECTION ( 'NONE',  ( 0.000000000000000000, 1.000000000000000000, 0.000000000000000000 ) ) ;
#82652=VERTEX_POINT ( 'NONE', #46758 ) ;
#82653=VECTOR ( 'NONE', #3755, 1000.000000000000000 ) ;
#82668=ADVANCED_FACE ( 'NONE', ( #54876 ), #47261, .F. ) ;
#82676=CARTESIAN_POINT ( 'NONE',  ( 32.25249349869194759, 1.684774720514423674, -12.65342752644895263 ) ) ;
#82687=ORIENTED_EDGE ( 'NONE', *, *, #82410, .F. ) ;
#82694=FACE_OUTER_BOUND ( 'NONE', #15488, .T. ) ;
#82699=VERTEX_POINT ( 'NONE', #37271 ) ;
#82702=CARTESIAN_POINT ( 'NONE',  ( 13.59451591917074431, 3.316774720514426456, -28.23515841827053308 ) ) ;
#82708=CARTESIAN_POINT ( 'NONE',  ( 31.63608488009069575, 3.478648800329905644, 27.34773273846989738 ) ) ;
#82715=AXIS2_PLACEMENT_3D ( 'NONE', #31884, #62856, #24265 ) ;
#82718=DIRECTION ( 'NONE',  ( 0.000000000000000000, 0.000000000000000000, -1.000000000000000000 ) ) ;
#82737=EDGE_LOOP ( 'NONE', ( #80488, #4141, #30340, #6965 ) ) ;
#82747=ORIENTED_EDGE ( 'NONE', *, *, #18183, .T. ) ;
#82762=ORIENTED_EDGE ( 'NONE', *, *, #59411, .F. ) ;
#82765=EDGE_CURVE ( 'NONE', #71418, #20569, #43194, .T. ) ;
#82767=EDGE_CURVE ( 'NONE', #79746, #45709, #56165, .T. ) ;
#82771=ORIENTED_EDGE ( 'NONE', *, *, #45308, .F. ) ;
#82789=VECTOR ( 'NONE', #82499, 1000.000000000000227 ) ;
#82808=EDGE_LOOP ( 'NONE', ( #54039, #91854, #27142, #20722, #29573, #71525, #20984, #59530 ) ) ;
#82809=CARTESIAN_POINT ( 'NONE',  ( 10.46399479596398052, 3.316774720514422903, -27.03001098546561209 ) ) ;
#82842=DIRECTION ( 'NONE',  ( -0.000000000000000000, 0.000000000000000000, 1.000000000000000000 ) ) ;
#82859=EDGE_LOOP ( 'NONE', ( #27476, #18237, #3508, #30942 ) ) ;
#82882=EDGE_LOOP ( 'NONE', ( #87621, #9376, #58300 ) ) ;
#82899=ADVANCED_FACE ( 'NONE', ( #24910 ), #33036, .F. ) ;
#82902=CYLINDRICAL_SURFACE ( 'NONE', #79706, 2.040000000000000036 ) ;
#82908=DIRECTION ( 'NONE',  ( -1.000000000000000000, 0.000000000000000000, -0.000000000000000000 ) ) ;
#82913=LINE ( 'NONE', #50485, #92738 ) ;
#82916=CARTESIAN_POINT ( 'NONE',  ( 30.09341516180546350, 1.684774720514424562, -11.39311774897855756 ) ) ;
#82919=CARTESIAN_POINT ( 'NONE',  ( 9.464509667910858681, 5.356774720513593380, -27.03659963401723942 ) ) ;
#82923=AXIS2_PLACEMENT_3D ( 'NONE', #12186, #20793, #91316 ) ;
#82932=PLANE ( 'NONE',  #42329 ) ;
#82947=DIRECTION ( 'NONE',  ( -0.000000000000000000, -1.000000000000000000, -0.000000000000000000 ) ) ;
#82958=VERTEX_POINT ( 'NONE', #67487 ) ;
#82960=CARTESIAN_POINT ( 'NONE',  ( -0.02075734969026423599, 6.376774720514426953, 22.60902280011862686 ) ) ;
#82961=CARTESIAN_POINT ( 'NONE',  ( 29.70220533433690946, 3.316774720514426456, 28.20564067601640801 ) ) ;
#82967=CARTESIAN_POINT ( 'NONE',  ( -29.49875734969025842, -5.965225279485572685, 25.61802280011862720 ) ) ;
#82989=CARTESIAN_POINT ( 'NONE',  ( 31.82032313667048484, 6.376774720514426953, 9.148483289431936782 ) ) ;
#82996=AXIS2_PLACEMENT_3D ( 'NONE', #33509, #64493, #95409 ) ;
#83019=EDGE_CURVE ( 'NONE', #49971, #99116, #50766, .T. ) ;
#83022=EDGE_CURVE ( 'NONE', #54320, #76406, #74585, .T. ) ;
#83039=CARTESIAN_POINT ( 'NONE',  ( -24.90875734969025501, 3.316774720514426456, 26.43402280011862615 ) ) ;
#83047=ADVANCED_FACE ( 'NONE', ( #82694 ), #73599, .F. ) ;
#83048=CARTESIAN_POINT ( 'NONE',  ( -20.27875734969026311, -4.543225279485573864, 24.00402280011862288 ) ) ;
#83063=VERTEX_POINT ( 'NONE', #21286 ) ;
#83075=EDGE_CURVE ( 'NONE', #54184, #44858, #58386, .T. ) ;
#83080=DIRECTION ( 'NONE',  ( 0.000000000000000000, 0.000000000000000000, 1.000000000000000000 ) ) ;
#83081=ADVANCED_FACE ( 'NONE', ( #83187 ), #91844, .T. ) ;
#83087=CARTESIAN_POINT ( 'NONE',  ( -29.49875734969026198, -5.965225279485572685, 2.362022800118626531 ) ) ;
#83098=CARTESIAN_POINT ( 'NONE',  ( -41.32836283488544638, 4.772774720514425972, 39.26872235229541985 ) ) ;
#83111=AXIS2_PLACEMENT_3D ( 'NONE', #33219, #40338, #48958 ) ;
#83113=CARTESIAN_POINT ( 'NONE',  ( 29.70220533433691301, 3.316774720514426456, 28.20564067601639735 ) ) ;
#83119=LINE ( 'NONE', #51693, #12741 ) ;
#83129=VERTEX_POINT ( 'NONE', #61378 ) ;
#83157=CARTESIAN_POINT ( 'NONE',  ( 7.805843057017202824, 3.316774720514425567, -27.15467198446602026 ) ) ;
#83163=CARTESIAN_POINT ( 'NONE',  ( 12.09245314707524876, 4.658029312750951334, -27.52981586573924488 ) ) ;
#83170=FACE_OUTER_BOUND ( 'NONE', #74546, .T. ) ;
#83171=LINE ( 'NONE', #21269, #84892 ) ;
#83187=FACE_OUTER_BOUND ( 'NONE', #96111, .T. ) ;
#83202=EDGE_CURVE ( 'NONE', #38457, #70502, #54557, .T. ) ;
#83218=ADVANCED_FACE ( 'NONE', ( #84189 ), #14680, .T. ) ;
#83221=CARTESIAN_POINT ( 'NONE',  ( -53.01255352321339842, 2.682774720514426559, 35.59556822165056644 ) ) ;
#83260=EDGE_CURVE ( 'NONE', #94215, #20042, #85791, .T. ) ;
#83262=ORIENTED_EDGE ( 'NONE', *, *, #38133, .T. ) ;
#83283=EDGE_CURVE ( 'NONE', #18260, #50853, #15768, .T. ) ;
#83285=DIRECTION ( 'NONE',  ( 0.000000000000000000, -1.000000000000000000, 0.000000000000000000 ) ) ;
#83288=CARTESIAN_POINT ( 'NONE',  ( 6.184520403203631389, 5.356774720514425603, -25.32021290018218451 ) ) ;
#83299=CARTESIAN_POINT ( 'NONE',  ( -16.22218391600152643, 6.376774720514426953, -54.85883559227303863 ) ) ;
#83309=VECTOR ( 'NONE', #67012, 1000.000000000000000 ) ;
#83324=EDGE_CURVE ( 'NONE', #23469, #71932, #86287, .T. ) ;
#83356=CARTESIAN_POINT ( 'NONE',  ( 31.10870921191468597, 5.152774720514429418, -4.748485609378566785 ) ) ;
#83360=B_SPLINE_SURFACE_WITH_KNOTS ( 'NONE', 3, 1, ( 
 ( #60266, #6461 ),
 ( #99300, #21176 ),
 ( #12572, #21662 ),
 ( #60760, #91189 ),
 ( #59256, #82089 ),
 ( #43536, #59763 ),
 ( #52637, #74473 ) ),
 .UNSPECIFIED., .F., .F., .F.,
 ( 4, 1, 1, 1, 4 ),
 ( 2, 2 ),
 ( 0.3452202732246780759, 0.4949101844912719983, 0.6446000957578658097, 0.7942900070244596211, 0.9439799182910535436 ),
 ( 0.000000000000000000, 1.000000000000000000 ),
 .UNSPECIFIED. ) ;
#83362=ORIENTED_EDGE ( 'NONE', *, *, #97147, .T. ) ;
#83363=ORIENTED_EDGE ( 'NONE', *, *, #11638, .F. ) ;
#83376=DIRECTION ( 'NONE',  ( 0.000000000000000000, -1.000000000000000000, 0.000000000000000000 ) ) ;
#83382=CIRCLE ( 'NONE', #49440, 1.149999999999998135 ) ;
#83390=DIRECTION ( 'NONE',  ( 0.000000000000000000, 0.000000000000000000, -1.000000000000000000 ) ) ;
#83405=VERTEX_POINT ( 'NONE', #30494 ) ;
#83441=CARTESIAN_POINT ( 'NONE',  ( 14.52511747680497933, -6.475225279485573360, -27.86035006098926559 ) ) ;
#83456=CARTESIAN_POINT ( 'NONE',  ( 31.13513474936813807, 4.540774720514427543, 3.331262582247328741 ) ) ;
#83466=DIRECTION ( 'NONE',  ( 0.000000000000000000, 0.000000000000000000, 1.000000000000000000 ) ) ;
#83508=ADVANCED_FACE ( 'NONE', ( #41129 ), #10671, .F. ) ;
#83512=ADVANCED_FACE ( 'NONE', ( #89293 ), #11166, .T. ) ;
#83515=LINE ( 'NONE', #21608, #57567 ) ;
#83524=CARTESIAN_POINT ( 'NONE',  ( -0.02075734969026423599, -5.965225279485572685, -0.08597719988137648983 ) ) ;
#83534=LINE ( 'NONE', #45496, #13277 ) ;
#83539=AXIS2_PLACEMENT_3D ( 'NONE', #20264, #53238, #13152 ) ;
#83547=CARTESIAN_POINT ( 'NONE',  ( 13.55016566187448923, -5.965225279485570908, -28.22449608469281657 ) ) ;
#83549=CARTESIAN_POINT ( 'NONE',  ( 32.45853543194704116, 0.3587747205144265483, 9.169203677920338080 ) ) ;
#83551=DIRECTION ( 'NONE',  ( -0.9161084732596779245, 5.365801633547208359E-16, 0.4009304992412300872 ) ) ;
#83561=EDGE_CURVE ( 'NONE', #84112, #44563, #71578, .T. ) ;
#83562=EDGE_LOOP ( 'NONE', ( #968, #61149, #26645, #51930 ) ) ;
#83576=CARTESIAN_POINT ( 'NONE',  ( -28.49194798280534968, 6.376774720514426953, 28.38521343323375490 ) ) ;
#83586=CARTESIAN_POINT ( 'NONE',  ( 32.74409430443929381, 4.661791533294069367, -3.688467650547408994 ) ) ;
#83597=B_SPLINE_CURVE_WITH_KNOTS ( 'NONE', 3,
 ( #96029, #18404, #71701, #25005 ),
 .UNSPECIFIED., .F., .F.,
 ( 4, 4 ),
 ( 0.000000000000000000, 1.000000000000000000 ),
 .UNSPECIFIED. ) ;
#83606=EDGE_LOOP ( 'NONE', ( #69393, #13455, #17604, #44223, #7356 ) ) ;
#83617=ORIENTED_EDGE ( 'NONE', *, *, #40993, .F. ) ;
#83618=LINE ( 'NONE', #38449, #13645 ) ;
#83620=VECTOR ( 'NONE', #24561, 1000.000000000000114 ) ;
#83630=EDGE_CURVE ( 'NONE', #35425, #22324, #37499, .T. ) ;
#83631=LINE ( 'NONE', #68416, #57269 ) ;
#83651=EDGE_CURVE ( 'NONE', #3492, #21600, #12657, .T. ) ;
#83664=EDGE_LOOP ( 'NONE', ( #59821, #7974, #43546, #46723, #22955, #40258 ) ) ;
#83667=FACE_OUTER_BOUND ( 'NONE', #5169, .T. ) ;
#83693=VECTOR ( 'NONE', #8463, 1000.000000000000114 ) ;
#83697=ORIENTED_EDGE ( 'NONE', *, *, #63376, .T. ) ;
#83702=ADVANCED_FACE ( 'NONE', ( #38500 ), #53997, .T. ) ;
#83732=AXIS2_PLACEMENT_3D ( 'NONE', #47765, #11197, #1085 ) ;
#83740=AXIS2_PLACEMENT_3D ( 'NONE', #10101, #96833, #73014 ) ;
#83743=LINE ( 'NONE', #44201, #77093 ) ;
#83745=ORIENTED_EDGE ( 'NONE', *, *, #87842, .F. ) ;
#83750=LINE ( 'NONE', #22833, #5011 ) ;
#83762=ORIENTED_EDGE ( 'NONE', *, *, #2489, .F. ) ;
#83778=EDGE_CURVE ( 'NONE', #69852, #80312, #11051, .T. ) ;
#83800=DIRECTION ( 'NONE',  ( -0.000000000000000000, 1.000000000000000000, -0.000000000000000000 ) ) ;
#83803=B_SPLINE_CURVE_WITH_KNOTS ( 'NONE', 3,
 ( #28526, #43767, #43273, #36642, #81823, #74214, #98028, #82809 ),
 .UNSPECIFIED., .F., .F.,
 ( 4, 2, 2, 4 ),
 ( 0.000000000000000000, 0.0004967474533590028650, 0.0007451211800385037012, 0.0009934949067180044290 ),
 .UNSPECIFIED. ) ;
#83807=VECTOR ( 'NONE', #66488, 1000.000000000000000 ) ;
#83810=ADVANCED_FACE ( 'NONE', ( #25267 ), #72959, .F. ) ;
#83816=AXIS2_PLACEMENT_3D ( 'NONE', #32962, #94849, #17734 ) ;
#83830=ORIENTED_EDGE ( 'NONE', *, *, #64364, .T. ) ;
#83831=DIRECTION ( 'NONE',  ( 0.000000000000000000, 0.000000000000000000, 1.000000000000000000 ) ) ;
#83843=CARTESIAN_POINT ( 'NONE',  ( 27.53860345374808105, 5.356774720496559894, 19.84760796525321780 ) ) ;
#83844=FACE_OUTER_BOUND ( 'NONE', #32219, .T. ) ;
#83848=DIRECTION ( 'NONE',  ( 0.000000000000000000, 0.000000000000000000, 1.000000000000000000 ) ) ;
#83868=CARTESIAN_POINT ( 'NONE',  ( -19.77875734969026311, 3.316774720514426456, 27.45402280011862572 ) ) ;
#83879=CARTESIAN_POINT ( 'NONE',  ( -0.02075734969026423599, 6.376774720514426953, -0.08597719988137648983 ) ) ;
#83895=VECTOR ( 'NONE', #79566, 1000.000000000000000 ) ;
#83901=CARTESIAN_POINT ( 'NONE',  ( 0.000000000000000000, -6.943225279485572443, 0.000000000000000000 ) ) ;
#83903=ORIENTED_EDGE ( 'NONE', *, *, #43321, .F. ) ;
#83909=EDGE_CURVE ( 'NONE', #95461, #23469, #74442, .T. ) ;
#83911=EDGE_LOOP ( 'NONE', ( #781, #67430, #40431, #75007 ) ) ;
#83918=CARTESIAN_POINT ( 'NONE',  ( 32.52533654608641456, 5.023480152701085721, -11.79063777444543781 ) ) ;
#83928=DIRECTION ( 'NONE',  ( 0.000000000000000000, 1.000000000000000000, -0.000000000000000000 ) ) ;
#83958=CARTESIAN_POINT ( 'NONE',  ( -32.30247028140506416, -6.475225279485573360, 27.60502002861223048 ) ) ;
#83992=ORIENTED_EDGE ( 'NONE', *, *, #6645, .F. ) ;
#84005=LINE ( 'NONE', #29725, #79232 ) ;
#84008=VERTEX_POINT ( 'NONE', #58720 ) ;
#84014=EDGE_LOOP ( 'NONE', ( #27624, #97712, #4019, #3512 ) ) ;
#84024=DIRECTION ( 'NONE',  ( 0.000000000000000000, 0.000000000000000000, -1.000000000000000000 ) ) ;
#84039=EDGE_LOOP ( 'NONE', ( #21987, #44605, #61796, #72573 ) ) ;
#84050=DIRECTION ( 'NONE',  ( 0.000000000000000000, 0.000000000000000000, 1.000000000000000000 ) ) ;
#84068=PLANE ( 'NONE',  #75024 ) ;
#84077=FACE_OUTER_BOUND ( 'NONE', #59458, .T. ) ;
#84079=B_SPLINE_CURVE_WITH_KNOTS ( 'NONE', 3,
 ( #2040, #31975, #55325, #56335, #62943 ),
 .UNSPECIFIED., .F., .F.,
 ( 4, 1, 4 ),
 ( 0.1431656576382807078, 0.2545924338564266032, 0.2890741368561012825 ),
 .UNSPECIFIED. ) ;
#84086=VECTOR ( 'NONE', #79866, 1000.000000000000000 ) ;
#84087=B_SPLINE_CURVE_WITH_KNOTS ( 'NONE', 3,
 ( #50779, #88841, #74596, #12692, #34551, #89829 ),
 .UNSPECIFIED., .F., .F.,
 ( 4, 2, 4 ),
 ( -8.871155308958663375E-06, 0.0009003829173646808823, 0.001809636990038320306 ),
 .UNSPECIFIED. ) ;
#84088=EDGE_CURVE ( 'NONE', #57513, #44666, #27770, .T. ) ;
#84090=CARTESIAN_POINT ( 'NONE',  ( 32.23945434255342235, 4.540774721353955989, 2.150384428877208709 ) ) ;
#84097=VECTOR ( 'NONE', #51148, 1000.000000000000000 ) ;
#84110=CIRCLE ( 'NONE', #87367, 251.4258649670780699 ) ;
#84112=VERTEX_POINT ( 'NONE', #22627 ) ;
#84117=CARTESIAN_POINT ( 'NONE',  ( 33.74607884027702909, -5.965225279485572685, -4.999864028243830916 ) ) ;
#84151=CARTESIAN_POINT ( 'NONE',  ( -28.98875734969026041, -5.965225279485572685, 23.37402280011862743 ) ) ;
#84157=CARTESIAN_POINT ( 'NONE',  ( 9.422519371942208011, -6.475225279485576024, -27.03574706870085720 ) ) ;
#84189=FACE_OUTER_BOUND ( 'NONE', #7115, .T. ) ;
#84192=EDGE_CURVE ( 'NONE', #52696, #34410, #90332, .T. ) ;
#84207=ORIENTED_EDGE ( 'NONE', *, *, #59173, .F. ) ;
#84231=VECTOR ( 'NONE', #17476, 1000.000000000000000 ) ;
#84258=CARTESIAN_POINT ( 'NONE',  ( 282.9764569301858046, 4.132774720514426292, 20.79159422840526616 ) ) ;
#84264=ADVANCED_FACE ( 'NONE', ( #85036 ), #92647, .F. ) ;
#84269=VERTEX_POINT ( 'NONE', #47996 ) ;
#84278=EDGE_CURVE ( 'NONE', #70502, #25228, #8919, .T. ) ;
#84279=ADVANCED_FACE ( 'NONE', ( #57118 ), #10419, .F. ) ;
#84282=DIRECTION ( 'NONE',  ( 0.000000000000000000, -1.000000000000000000, 0.000000000000000000 ) ) ;
#84304=AXIS2_PLACEMENT_3D ( 'NONE', #63793, #25192, #56169 ) ;
#84305=B_SPLINE_CURVE_WITH_KNOTS ( 'NONE', 3,
 ( #76480, #98320, #44554, #6986 ),
 .UNSPECIFIED., .F., .F.,
 ( 4, 4 ),
 ( 0.001505373688938434684, 0.001772001984008341434 ),
 .UNSPECIFIED. ) ;
#84306=CARTESIAN_POINT ( 'NONE',  ( 10.68713020350923060, 6.376774720514513106, -28.05292731626249392 ) ) ;
#84307=DIRECTION ( 'NONE',  ( -0.000000000000000000, 1.000000000000000000, -0.000000000000000000 ) ) ;
#84325=CARTESIAN_POINT ( 'NONE',  ( 15.58962545129235799, -6.475225279485573360, -26.91365498785467025 ) ) ;
#84326=DIRECTION ( 'NONE',  ( -0.7512896232465786639, 0.000000000000000000, -0.6599726524652470561 ) ) ;
#84350=VECTOR ( 'NONE', #63835, 1000.000000000000000 ) ;
#84373=DIRECTION ( 'NONE',  ( 0.09721092304694055330, 0.000000000000000000, -0.9952638024365006997 ) ) ;
#84377=ORIENTED_EDGE ( 'NONE', *, *, #77029, .T. ) ;
#84381=CIRCLE ( 'NONE', #66607, 2.040000000000000036 ) ;
#84384=ORIENTED_EDGE ( 'NONE', *, *, #10825, .F. ) ;
#84410=ORIENTED_EDGE ( 'NONE', *, *, #38420, .F. ) ;
#84411=LINE ( 'NONE', #91521, #64352 ) ;
#84416=DIRECTION ( 'NONE',  ( 4.448048651795327725E-16, -1.000000000000000000, 7.118365844322534241E-16 ) ) ;
#84439=DIRECTION ( 'NONE',  ( -0.000000000000000000, -1.000000000000000000, -0.000000000000000000 ) ) ;
#84442=DIRECTION ( 'NONE',  ( -0.000000000000000000, -1.000000000000000000, -0.000000000000000000 ) ) ;
#84445=PLANE ( 'NONE',  #75390 ) ;
#84469=ADVANCED_FACE ( 'NONE', ( #47249 ), #71090, .T. ) ;
#84472=ORIENTED_EDGE ( 'NONE', *, *, #22011, .T. ) ;
#84489=VERTEX_POINT ( 'NONE', #77172 ) ;
#84491=ORIENTED_EDGE ( 'NONE', *, *, #31789, .T. ) ;
#84497=ADVANCED_FACE ( 'NONE', ( #84796 ), #40137, .T. ) ;
#84505=EDGE_CURVE ( 'NONE', #30477, #46180, #100008, .T. ) ;
#84529=AXIS2_PLACEMENT_3D ( 'NONE', #24797, #40033, #64403 ) ;
#84530=EDGE_LOOP ( 'NONE', ( #56927, #36369, #90417, #86138 ) ) ;
#84543=CARTESIAN_POINT ( 'NONE',  ( -32.30247028140506416, 1.684774720514426560, 27.60502002861223048 ) ) ;
#84550=PLANE ( 'NONE',  #94979 ) ;
#84563=DIRECTION ( 'NONE',  ( -0.000000000000000000, -1.000000000000000000, -0.000000000000000000 ) ) ;
#84564=ORIENTED_EDGE ( 'NONE', *, *, #83022, .F. ) ;
#84577=AXIS2_PLACEMENT_3D ( 'NONE', #63012, #93427, #8712 ) ;
#84580=ORIENTED_EDGE ( 'NONE', *, *, #58858, .T. ) ;
#84615=ORIENTED_EDGE ( 'NONE', *, *, #78059, .F. ) ;
#84619=EDGE_LOOP ( 'NONE', ( #2118, #82546, #10635, #49413 ) ) ;
#84630=ORIENTED_EDGE ( 'NONE', *, *, #95387, .F. ) ;
#84631=PLANE ( 'NONE',  #91200 ) ;
#84636=VERTEX_POINT ( 'NONE', #80695 ) ;
#84647=ORIENTED_EDGE ( 'NONE', *, *, #43205, .F. ) ;
#84652=ADVANCED_FACE ( 'NONE', ( #88313 ), #3089, .T. ) ;
#84654=EDGE_CURVE ( 'NONE', #63531, #19596, #71981, .T. ) ;
#84668=CARTESIAN_POINT ( 'NONE',  ( 13.91401389203221406, 0.3587747205144265483, 158.0376437107427137 ) ) ;
#84669=CARTESIAN_POINT ( 'NONE',  ( 0.000000000000000000, -6.943225279485572443, 0.000000000000000000 ) ) ;
#84690=FACE_OUTER_BOUND ( 'NONE', #28900, .T. ) ;
#84699=VECTOR ( 'NONE', #77670, 1000.000000000000000 ) ;
#84703=DIRECTION ( 'NONE',  ( -0.09721092304694051167, 0.000000000000000000, 0.9952638024365005887 ) ) ;
#84707=DIRECTION ( 'NONE',  ( 0.000000000000000000, -1.000000000000000000, 1.478457507934778393E-16 ) ) ;
#84708=CIRCLE ( 'NONE', #32872, 2.249999999999998668 ) ;
#84711=CARTESIAN_POINT ( 'NONE',  ( -24.90875734969025501, -5.965225279485572685, 26.43402280011862615 ) ) ;
#84721=EDGE_CURVE ( 'NONE', #14974, #82488, #53119, .T. ) ;
#84723=CARTESIAN_POINT ( 'NONE',  ( 32.85081302853804885, 3.622774720514426949, -13.10817780685210643 ) ) ;
#84751=VECTOR ( 'NONE', #32856, 1000.000000000000000 ) ;
#84756=CARTESIAN_POINT ( 'NONE',  ( -27.96875734969026084, 6.376774720514426953, 26.43402280011862615 ) ) ;
#84759=CARTESIAN_POINT ( 'NONE',  ( 30.53060340732037048, 2.682774720514426559, -2.322449884495168870 ) ) ;
#84762=DIRECTION ( 'NONE',  ( 0.000000000000000000, -1.000000000000000000, 0.000000000000000000 ) ) ;
#84767=EDGE_CURVE ( 'NONE', #26340, #23597, #7686, .T. ) ;
#84788=PLANE ( 'NONE',  #80515 ) ;
#84796=FACE_OUTER_BOUND ( 'NONE', #85426, .T. ) ;
#84808=CARTESIAN_POINT ( 'NONE',  ( 8.159923944583882260, 6.376774720514430506, -28.14238247108524149 ) ) ;
#84815=DIRECTION ( 'NONE',  ( -0.000000000000000000, -1.000000000000000000, 0.000000000000000000 ) ) ;
#84833=EDGE_CURVE ( 'NONE', #18228, #67714, #27904, .T. ) ;
#84843=DIRECTION ( 'NONE',  ( -1.000000000000000000, 0.000000000000000000, 0.000000000000000000 ) ) ;
#84864=FACE_OUTER_BOUND ( 'NONE', #25344, .T. ) ;
#84879=CARTESIAN_POINT ( 'NONE',  ( -29.49875734969025842, -5.965225279485572685, 23.37402280011862743 ) ) ;
#84889=DIRECTION ( 'NONE',  ( 0.000000000000000000, -1.000000000000000000, 1.478457507934778393E-16 ) ) ;
#84892=VECTOR ( 'NONE', #89801, 1000.000000000000000 ) ;
#84908=DIRECTION ( 'NONE',  ( -1.000000000000000000, 0.000000000000000000, 0.000000000000000000 ) ) ;
#84919=AXIS2_PLACEMENT_3D ( 'NONE', #48690, #24327, #48180 ) ;
#84931=CARTESIAN_POINT ( 'NONE',  ( -15.82668884360736961, -6.475225279485576024, 42.07822029717483758 ) ) ;
#84933=CARTESIAN_POINT ( 'NONE',  ( 23.91005183030481263, 2.682774720514426559, -14.40591128290692069 ) ) ;
#84952=CARTESIAN_POINT ( 'NONE',  ( -41.32836283488544638, 2.682774720514426559, 39.26872235229541985 ) ) ;
#84953=EDGE_CURVE ( 'NONE', #65212, #3035, #952, .T. ) ;
#84958=ADVANCED_FACE ( 'NONE', ( #99886 ), #30897, .F. ) ;
#84978=B_SPLINE_CURVE_WITH_KNOTS ( 'NONE', 3,
 ( #79933, #47999, #9923, #2831, #79431, #32760, #25139, #56121 ),
 .UNSPECIFIED., .F., .F.,
 ( 4, 2, 2, 4 ),
 ( 0.000000000000000000, 0.003897507692133500394, 0.005846261538200250157, 0.007795015384267000788 ),
 .UNSPECIFIED. ) ;
#84984=ORIENTED_EDGE ( 'NONE', *, *, #83202, .T. ) ;
#84985=PLANE ( 'NONE',  #54994 ) ;
#84992=AXIS2_PLACEMENT_3D ( 'NONE', #87235, #10115, #41075 ) ;
#84998=CARTESIAN_POINT ( 'NONE',  ( -24.97666371003640506, 0.3587747205143964613, -15.72894043976419454 ) ) ;
#85017=EDGE_LOOP ( 'NONE', ( #62679, #60499, #35706, #16737 ) ) ;
#85027=EDGE_CURVE ( 'NONE', #54547, #44198, #39007, .T. ) ;
#85036=FACE_OUTER_BOUND ( 'NONE', #64973, .T. ) ;
#85038=DIRECTION ( 'NONE',  ( -0.6401411605457395515, 0.000000000000000000, -0.7682573101345366862 ) ) ;
#85051=DIRECTION ( 'NONE',  ( 0.000000000000000000, -1.000000000000000000, 0.000000000000000000 ) ) ;
#85060=CARTESIAN_POINT ( 'NONE',  ( -4.568292318365942073, 0.3587747205144265483, 30.06720597538392425 ) ) ;
#85119=DIRECTION ( 'NONE',  ( -0.000000000000000000, -1.000000000000000000, -0.000000000000000000 ) ) ;
#85130=VERTEX_POINT ( 'NONE', #4949 ) ;
#85136=ORIENTED_EDGE ( 'NONE', *, *, #39215, .F. ) ;
#85146=CARTESIAN_POINT ( 'NONE',  ( -20.77875734969026311, -6.143225279485574397, 27.35402280011862430 ) ) ;
#85156=EDGE_CURVE ( 'NONE', #94497, #88045, #36393, .T. ) ;
#85162=ADVANCED_FACE ( 'NONE', ( #44511 ), #59238, .F. ) ;
#85164=EDGE_CURVE ( 'NONE', #82652, #15615, #25571, .T. ) ;
#85166=CARTESIAN_POINT ( 'NONE',  ( 8.462785143989153269, -5.965225279485592225, -28.02084008811334215 ) ) ;
#85194=DIRECTION ( 'NONE',  ( 0.000000000000000000, 0.000000000000000000, -1.000000000000000000 ) ) ;
#85215=CIRCLE ( 'NONE', #10622, 2.249999999999998668 ) ;
#85232=EDGE_LOOP ( 'NONE', ( #30379, #20019, #28696, #1926, #18649, #45106 ) ) ;
#85233=PLANE ( 'NONE',  #2369 ) ;
#85235=CARTESIAN_POINT ( 'NONE',  ( 11.98973536156539943, 4.132774720514426292, -26.26140391504922178 ) ) ;
#85244=DIRECTION ( 'NONE',  ( 0.000000000000000000, -1.000000000000000000, 0.000000000000000000 ) ) ;
#85258=FACE_OUTER_BOUND ( 'NONE', #50838, .T. ) ;
#85275=VERTEX_POINT ( 'NONE', #77928 ) ;
#85295=VERTEX_POINT ( 'NONE', #63244 ) ;
#85307=ORIENTED_EDGE ( 'NONE', *, *, #65751, .T. ) ;
#85308=CARTESIAN_POINT ( 'NONE',  ( 9.146648804565860047, 6.376774720514172934, -28.07004961687618660 ) ) ;
#85316=LINE ( 'NONE', #96444, #18170 ) ;
#85340=CARTESIAN_POINT ( 'NONE',  ( 29.57907552664497786, 3.519868637853082571, 29.21818156430573765 ) ) ;
#85353=DIRECTION ( 'NONE',  ( 1.286817348990133408E-16, 0.000000000000000000, -1.000000000000000000 ) ) ;
#85369=CARTESIAN_POINT ( 'NONE',  ( 5.251006604497604258, 6.376774720514426953, -25.47015536487705489 ) ) ;
#85376=VECTOR ( 'NONE', #37248, 1000.000000000000000 ) ;
#85395=DIRECTION ( 'NONE',  ( -0.000000000000000000, -1.000000000000000000, -0.000000000000000000 ) ) ;
#85397=AXIS2_PLACEMENT_3D ( 'NONE', #76569, #34138, #46225 ) ;
#85406=EDGE_CURVE ( 'NONE', #94215, #45125, #26165, .T. ) ;
#85408=PLANE ( 'NONE',  #80998 ) ;
#85413=ORIENTED_EDGE ( 'NONE', *, *, #24203, .T. ) ;
#85426=EDGE_LOOP ( 'NONE', ( #57171, #66829, #39448, #38306 ) ) ;
#85429=FACE_OUTER_BOUND ( 'NONE', #64537, .T. ) ;
#85453=ORIENTED_EDGE ( 'NONE', *, *, #11523, .T. ) ;
#85460=CYLINDRICAL_SURFACE ( 'NONE', #2662, 2.249999999999998668 ) ;
#85464=DIRECTION ( 'NONE',  ( -0.000000000000000000, -1.000000000000000000, 0.000000000000000000 ) ) ;
#85466=CARTESIAN_POINT ( 'NONE',  ( 13.91401389203221406, 3.316774720514426456, 28.26920385068457264 ) ) ;
#85474=EDGE_CURVE ( 'NONE', #15615, #82652, #88829, .T. ) ;
#85480=DIRECTION ( 'NONE',  ( 1.000000000000000000, -0.000000000000000000, -0.000000000000000000 ) ) ;
#85485=ORIENTED_EDGE ( 'NONE', *, *, #79555, .T. ) ;
#85486=CARTESIAN_POINT ( 'NONE',  ( 32.50838937279095120, 1.682774720514426114, -10.74666623472941218 ) ) ;
#85491=CARTESIAN_POINT ( 'NONE',  ( -27.96875734969026084, -6.143225279485573509, 0.7300228001186309656 ) ) ;
#85493=CARTESIAN_POINT ( 'NONE',  ( 29.77147767949874435, 4.540774720514427543, 26.15915692125050995 ) ) ;
#85504=ORIENTED_EDGE ( 'NONE', *, *, #73979, .F. ) ;
#85522=ORIENTED_EDGE ( 'NONE', *, *, #43289, .T. ) ;
#85524=VECTOR ( 'NONE', #11148, 1000.000000000000000 ) ;
#85531=EDGE_CURVE ( 'NONE', #42999, #3225, #48519, .T. ) ;
#85550=CARTESIAN_POINT ( 'NONE',  ( 32.25183987940364005, 0.3587747205144265483, 2.026414261721653176 ) ) ;
#85562=VECTOR ( 'NONE', #57907, 1000.000000000000000 ) ;
#85601=EDGE_CURVE ( 'NONE', #42735, #4321, #89567, .T. ) ;
#85618=CARTESIAN_POINT ( 'NONE',  ( -27.13414387080440093, -5.965225279485594001, -10.21530720150730254 ) ) ;
#85624=DIRECTION ( 'NONE',  ( -0.000000000000000000, -1.000000000000000000, 0.000000000000000000 ) ) ;
#85629=CARTESIAN_POINT ( 'NONE',  ( 15.99960863614631101, 3.577630190450212577, -27.91116951066581819 ) ) ;
#85653=CARTESIAN_POINT ( 'NONE',  ( 27.53860345374808105, 4.772774720514425972, -6.982392034746241372 ) ) ;
#85661=ORIENTED_EDGE ( 'NONE', *, *, #91967, .F. ) ;
#85667=DIRECTION ( 'NONE',  ( -0.1593164160933057683, 0.000000000000000000, 0.9872275723272647685 ) ) ;
#85670=EDGE_CURVE ( 'NONE', #80003, #396, #19546, .T. ) ;
#85683=CARTESIAN_POINT ( 'NONE',  ( 9.478389368232452483, 2.682774720514426559, -23.17485683983816003 ) ) ;
#85684=DIRECTION ( 'NONE',  ( -0.000000000000000000, -1.000000000000000000, -0.000000000000000000 ) ) ;
#85695=ORIENTED_EDGE ( 'NONE', *, *, #17185, .T. ) ;
#85704=LINE ( 'NONE', #54267, #70120 ) ;
#85705=ORIENTED_EDGE ( 'NONE', *, *, #15639, .F. ) ;
#85725=CARTESIAN_POINT ( 'NONE',  ( 10.46399479596396453, 2.682774720514426559, -27.03001098546561920 ) ) ;
#85729=AXIS2_PLACEMENT_3D ( 'NONE', #57636, #88578, #50510 ) ;
#85772=VERTEX_POINT ( 'NONE', #39261 ) ;
#85778=VECTOR ( 'NONE', #30229, 1000.000000000000000 ) ;
#85791=LINE ( 'NONE', #31495, #23831 ) ;
#85797=CARTESIAN_POINT ( 'NONE',  ( -28.47875734969025885, -6.475225279485573360, -0.08597719988137300651 ) ) ;
#85803=CARTESIAN_POINT ( 'NONE',  ( 22.02124265030973760, -6.143225279485574397, 16.20402280011862217 ) ) ;
#85819=CARTESIAN_POINT ( 'NONE',  ( 9.146648804574669001, 3.316774720514593433, -28.07004961703220758 ) ) ;
#85842=DIRECTION ( 'NONE',  ( -0.000000000000000000, -1.000000000000000000, -0.000000000000000000 ) ) ;
#85880=FACE_OUTER_BOUND ( 'NONE', #7888, .T. ) ;
#85889=LINE ( 'NONE', #79268, #3649 ) ;
#85890=EDGE_LOOP ( 'NONE', ( #98870, #84984, #36810, #33024, #76004, #9031, #74248, #34645, #63007, #23149, #32093, #51100, #49212, #67613, #22093, #50223, #68171, #6236, #45026, #2915, #66985, #28026, #62522, #51289, #64303 ) ) ;
#85891=DIRECTION ( 'NONE',  ( -0.000000000000000000, -1.000000000000000000, 0.000000000000000000 ) ) ;
#85893=ORIENTED_EDGE ( 'NONE', *, *, #11576, .F. ) ;
#85897=AXIS2_PLACEMENT_3D ( 'NONE', #91362, #99465, #52814 ) ;
#85906=VECTOR ( 'NONE', #30993, 1000.000000000000000 ) ;
#85928=CYLINDRICAL_SURFACE ( 'NONE', #34956, 84.48086791635432746 ) ;
#85964=DIRECTION ( 'NONE',  ( 1.251281512149627050E-16, 0.000000000000000000, -1.000000000000000000 ) ) ;
#85971=ORIENTED_EDGE ( 'NONE', *, *, #51542, .T. ) ;
#85984=AXIS2_PLACEMENT_3D ( 'NONE', #89186, #57748, #50128 ) ;
#85991=ORIENTED_EDGE ( 'NONE', *, *, #31131, .T. ) ;
#85993=CARTESIAN_POINT ( 'NONE',  ( 10.86264265030973952, -5.965225279485574461, -28.64597719988137570 ) ) ;
#86000=CARTESIAN_POINT ( 'NONE',  ( -10.25272501932627378, 4.561466182953243909, 29.07579354015162210 ) ) ;
#86005=VERTEX_POINT ( 'NONE', #73715 ) ;
#86034=TOROIDAL_SURFACE ( 'NONE', #90883, 1.020000000000000018, 2.040000000000000036 ) ;
#86038=ORIENTED_EDGE ( 'NONE', *, *, #171, .F. ) ;
#86049=VECTOR ( 'NONE', #26669, 1000.000000000000227 ) ;
#86052=ORIENTED_EDGE ( 'NONE', *, *, #21035, .T. ) ;
#86054=CARTESIAN_POINT ( 'NONE',  ( -19.77875734969026311, -6.143225279485574397, 27.31649921512899937 ) ) ;
#86056=CYLINDRICAL_SURFACE ( 'NONE', #40000, 91.74549126261079834 ) ;
#86067=DIRECTION ( 'NONE',  ( -0.000000000000000000, -1.000000000000000000, -0.000000000000000000 ) ) ;
#86083=VERTEX_POINT ( 'NONE', #75204 ) ;
#86088=FACE_OUTER_BOUND ( 'NONE', #61797, .T. ) ;
#86089=EDGE_CURVE ( 'NONE', #27656, #64559, #5696, .T. ) ;
#86114=( BOUNDED_SURFACE ( )  B_SPLINE_SURFACE ( 3, 2, ( 
 ( #93820, #48161, #49172 ),
 ( #41045, #47661, #94315 ),
 ( #31929, #18200, #26316 ),
 ( #79086, #1487, #24801 ),
 ( #55781, #9588, #40548 ),
 ( #80097, #10582, #25306 ),
 ( #41547, #71500, #1987 ),
 ( #32929, #63906, #94819 ),
 ( #56285, #87208, #17699 ),
 ( #66398, #73001, #67381 ) ),
 .UNSPECIFIED., .F., .F., .F. ) 
 B_SPLINE_SURFACE_WITH_KNOTS ( ( 4, 2, 2, 2, 4 ),
 ( 3, 3 ),
 ( -1.454863790203986262E-16, 9.770668801556799598E-05, 0.0001954133760312814648, 0.0002931200640469949336, 0.0003908267520627084295 ),
 ( 0.000000000000000000, 1.000000000000000000 ),
 .UNSPECIFIED. ) 
 GEOMETRIC_REPRESENTATION_ITEM ( )  RATIONAL_B_SPLINE_SURFACE ( (
 ( 1.000000000000000000, 0.8096947957034197341, 1.000000000000000000),
 ( 1.000000000000000000, 0.8369431042627567541, 1.000000000000000000),
 ( 1.000000000000000000, 0.8633772427686626783, 1.000000000000000000),
 ( 1.000000000000000000, 0.9107640641016462313, 1.000000000000000000),
 ( 1.000000000000000000, 0.9319105126974177589, 1.000000000000000000),
 ( 1.000000000000000000, 0.9655776140384774164, 1.000000000000000000),
 ( 1.000000000000000000, 0.9783528158684996479, 1.000000000000000000),
 ( 1.000000000000000000, 0.9955824377509593370, 1.000000000000000000),
 ( 1.000000000000000000, 1.000024029240739631, 1.000000000000000000),
 ( 1.000000000000000000, 1.000000000000000000, 1.000000000000000000) ) ) 
 REPRESENTATION_ITEM ( '' )  SURFACE ( )  );
#86136=ORIENTED_EDGE ( 'NONE', *, *, #60229, .T. ) ;
#86138=ORIENTED_EDGE ( 'NONE', *, *, #74542, .T. ) ;
#86144=LINE ( 'NONE', #1422, #22176 ) ;
#86154=VERTEX_POINT ( 'NONE', #23915 ) ;
#86157=AXIS2_PLACEMENT_3D ( 'NONE', #65972, #95890, #96892 ) ;
#86158=DIRECTION ( 'NONE',  ( -0.000000000000000000, 1.000000000000000000, -0.000000000000000000 ) ) ;
#86178=DIRECTION ( 'NONE',  ( 0.000000000000000000, 1.000000000000000000, 0.000000000000000000 ) ) ;
#86209=ORIENTED_EDGE ( 'NONE', *, *, #33286, .F. ) ;
#86219=CARTESIAN_POINT ( 'NONE',  ( -28.32169924589829080, -5.965225279485592225, -8.244178532169447848 ) ) ;
#86242=EDGE_CURVE ( 'NONE', #24998, #23703, #21899, .T. ) ;
#86243=DIRECTION ( 'NONE',  ( 1.000000000000000000, 0.000000000000000000, 0.000000000000000000 ) ) ;
#86253=ORIENTED_EDGE ( 'NONE', *, *, #59173, .T. ) ;
#86263=CARTESIAN_POINT ( 'NONE',  ( 33.00535138976592719, 3.570691370340881576, -12.97242311383975988 ) ) ;
#86285=ORIENTED_EDGE ( 'NONE', *, *, #40262, .T. ) ;
#86287=LINE ( 'NONE', #71075, #4448 ) ;
#86291=DIRECTION ( 'NONE',  ( -1.000000000000000000, 8.503546450866701308E-16, 0.000000000000000000 ) ) ;
#86294=CARTESIAN_POINT ( 'NONE',  ( 30.53060340732262645, 5.330559497946674163, 2.122526108692961877 ) ) ;
#86302=EDGE_CURVE ( 'NONE', #94426, #32090, #31028, .T. ) ;
#86321=CARTESIAN_POINT ( 'NONE',  ( 8.817327481845893544, 6.376774720514678307, -28.08864864928871086 ) ) ;
#86326=LINE ( 'NONE', #39646, #41012 ) ;
#86329=FACE_OUTER_BOUND ( 'NONE', #90435, .T. ) ;
#86332=EDGE_CURVE ( 'NONE', #33445, #98946, #27305, .T. ) ;
#86336=VERTEX_POINT ( 'NONE', #18681 ) ;
#86342=CARTESIAN_POINT ( 'NONE',  ( -20.27875734969026311, -4.543225279485573864, 22.85402280011862430 ) ) ;
#86356=ORIENTED_EDGE ( 'NONE', *, *, #39227, .T. ) ;
#86378=AXIS2_PLACEMENT_3D ( 'NONE', #19990, #97611, #12371 ) ;
#86389=ORIENTED_EDGE ( 'NONE', *, *, #47851, .T. ) ;
#86402=EDGE_LOOP ( 'NONE', ( #36725, #85971, #21207, #78697 ) ) ;
#86408=CIRCLE ( 'NONE', #2119, 0.8160000000000007248 ) ;
#86432=PLANE ( 'NONE',  #76902 ) ;
#86435=ORIENTED_EDGE ( 'NONE', *, *, #76715, .F. ) ;
#86438=CARTESIAN_POINT ( 'NONE',  ( 3.509873074917118085, -5.965225279485572685, 29.15869884040363758 ) ) ;
#86497=DIRECTION ( 'NONE',  ( 0.000000000000000000, 0.000000000000000000, -1.000000000000000000 ) ) ;
#86525=CARTESIAN_POINT ( 'NONE',  ( 26.73860345374794178, -1.477225279485574028, 19.84760796525321780 ) ) ;
#86553=ORIENTED_EDGE ( 'NONE', *, *, #22365, .F. ) ;
#86557=ADVANCED_FACE ( 'NONE', ( #36908 ), #83360, .T. ) ;
#86573=CARTESIAN_POINT ( 'NONE',  ( -28.98875734969026396, 0.3587747205144265483, 10.11402280011862587 ) ) ;
#86608=CARTESIAN_POINT ( 'NONE',  ( -0.02075734969026423599, -6.475225279485573360, -0.08597719988137648983 ) ) ;
#86613=ORIENTED_EDGE ( 'NONE', *, *, #98007, .F. ) ;
#86623=ORIENTED_EDGE ( 'NONE', *, *, #98696, .F. ) ;
#86644=CARTESIAN_POINT ( 'NONE',  ( -0.02075734969026423599, 3.316774720514426456, -0.08597719988137648983 ) ) ;
#86677=CARTESIAN_POINT ( 'NONE',  ( 11.62916340711181284, -5.965225279485572685, 28.75961759920349792 ) ) ;
#86700=DIRECTION ( 'NONE',  ( 0.7512896232465891000, 0.000000000000000000, 0.6599726524652351767 ) ) ;
#86722=CIRCLE ( 'NONE', #42997, 3.060000000000000497 ) ;
#86739=VECTOR ( 'NONE', #99206, 1000.000000000000000 ) ;
#86766=ORIENTED_EDGE ( 'NONE', *, *, #88150, .T. ) ;
#86769=ORIENTED_EDGE ( 'NONE', *, *, #30392, .F. ) ;
#86775=PLANE ( 'NONE',  #69930 ) ;
#86795=CARTESIAN_POINT ( 'NONE',  ( 25.83488407601165093, 3.407774720514426647, -11.31196583263649558 ) ) ;
#86801=DIRECTION ( 'NONE',  ( 1.000000000000000000, -0.000000000000000000, 0.000000000000000000 ) ) ;
#86804=CARTESIAN_POINT ( 'NONE',  ( -2.449489742783178770, 4.293056017849825601, 2.499999999999999556 ) ) ;
#86810=CARTESIAN_POINT ( 'NONE',  ( -41.32836283488544638, 4.132774720514426292, 39.26872235229541985 ) ) ;
#86814=ADVANCED_FACE ( 'NONE', ( #26184 ), #20029, .T. ) ;
#86839=ORIENTED_EDGE ( 'NONE', *, *, #41188, .F. ) ;
#86841=CARTESIAN_POINT ( 'NONE',  ( 31.69086887328987956, 3.760767191028115519, 29.45064099519496992 ) ) ;
#86861=VERTEX_POINT ( 'NONE', #98677 ) ;
#86881=CARTESIAN_POINT ( 'NONE',  ( 26.73860345374794178, -1.477225279485574028, 19.84760796525321780 ) ) ;
#86883=EDGE_CURVE ( 'NONE', #43602, #27656, #11093, .T. ) ;
#86887=ORIENTED_EDGE ( 'NONE', *, *, #73487, .T. ) ;
#86894=B_SPLINE_CURVE_WITH_KNOTS ( 'NONE', 3,
 ( #25416, #73105, #81205, #33034 ),
 .UNSPECIFIED., .F., .F.,
 ( 4, 4 ),
 ( 0.01303003236488493519, 0.01305095637151315775 ),
 .UNSPECIFIED. ) ;
#86914=DIRECTION ( 'NONE',  ( -0.000000000000000000, -1.000000000000000000, -0.000000000000000000 ) ) ;
#86927=EDGE_CURVE ( 'NONE', #53725, #20580, #37295, .T. ) ;
#86951=AXIS2_PLACEMENT_3D ( 'NONE', #53031, #67260, #35801 ) ;
#86953=CARTESIAN_POINT ( 'NONE',  ( 32.40199294184732537, -6.475225279485573360, -12.82361242714782712 ) ) ;
#86981=CARTESIAN_POINT ( 'NONE',  ( 27.86270917940689174, -5.965225279485572685, 29.49402280011862487 ) ) ;
#86984=EDGE_CURVE ( 'NONE', #61220, #54573, #15435, .T. ) ;
#86995=CARTESIAN_POINT ( 'NONE',  ( -10.23894677657808749, 4.339657088724310441, 29.22408179085893210 ) ) ;
#87004=CARTESIAN_POINT ( 'NONE',  ( 14.76093561896379214, 3.316774720514426456, -27.37148769130089931 ) ) ;
#87005=LINE ( 'NONE', #48461, #45901 ) ;
#87010=AXIS2_PLACEMENT_3D ( 'NONE', #88989, #19459, #18466 ) ;
#87032=EDGE_CURVE ( 'NONE', #92497, #45676, #32239, .T. ) ;
#87034=FACE_OUTER_BOUND ( 'NONE', #74462, .T. ) ;
#87041=ORIENTED_EDGE ( 'NONE', *, *, #64392, .T. ) ;
#87047=LINE ( 'NONE', #57123, #48177 ) ;
#87054=VECTOR ( 'NONE', #312, 1000.000000000000000 ) ;
#87082=VECTOR ( 'NONE', #38450, 1000.000000000000000 ) ;
#87087=DIRECTION ( 'NONE',  ( -0.000000000000000000, 1.000000000000000000, -0.000000000000000000 ) ) ;
#87091=B_SPLINE_CURVE_WITH_KNOTS ( 'NONE', 3,
 ( #59443, #6140, #92374, #90880, #68057, #52824, #76636, #44714 ),
 .UNSPECIFIED., .F., .F.,
 ( 4, 2, 2, 4 ),
 ( 1.199502015590836694E-17, 0.001846270405096679841, 0.003692540810193348840, 0.007385081620386685537 ),
 .UNSPECIFIED. ) ;
#87120=EDGE_CURVE ( 'NONE', #40372, #48919, #25726, .T. ) ;
#87138=EDGE_LOOP ( 'NONE', ( #91336, #67052, #88823, #49809 ) ) ;
#87143=VERTEX_POINT ( 'NONE', #86953 ) ;
#87166=FACE_OUTER_BOUND ( 'NONE', #39187, .T. ) ;
#87171=ORIENTED_EDGE ( 'NONE', *, *, #12441, .F. ) ;
#87191=DIRECTION ( 'NONE',  ( 0.000000000000000000, -0.000000000000000000, 1.000000000000000000 ) ) ;
#87196=DIRECTION ( 'NONE',  ( 0.000000000000000000, 0.000000000000000000, 1.000000000000000000 ) ) ;
#87208=CARTESIAN_POINT ( 'NONE',  ( 33.62498039647005044, 3.398310449796175359, -11.43903334458933507 ) ) ;
#87212=CARTESIAN_POINT ( 'NONE',  ( -28.32169924589829080, 0.3587747205143964613, -8.244178532169451401 ) ) ;
#87235=CARTESIAN_POINT ( 'NONE',  ( -65.05438548721848235, 5.356774720514425603, 0.7300228001186309656 ) ) ;
#87274=PLANE ( 'NONE',  #26190 ) ;
#87286=VECTOR ( 'NONE', #36649, 1000.000000000000000 ) ;
#87294=CARTESIAN_POINT ( 'NONE',  ( 30.53060340732036337, 5.340035977923285770, 2.705756132044150775 ) ) ;
#87307=CARTESIAN_POINT ( 'NONE',  ( 5.395440699609681090, 0.3587747205144061202, -28.51842087987364849 ) ) ;
#87313=DIRECTION ( 'NONE',  ( -0.000000000000000000, -1.000000000000000000, -0.000000000000000000 ) ) ;
#87331=ORIENTED_EDGE ( 'NONE', *, *, #30397, .F. ) ;
#87334=CARTESIAN_POINT ( 'NONE',  ( 32.66876533700883556, -6.475225279485573360, -12.58926540598386445 ) ) ;
#87342=CIRCLE ( 'NONE', #29033, 253.2618649670780826 ) ;
#87345=EDGE_CURVE ( 'NONE', #36941, #25228, #89251, .T. ) ;
#87367=AXIS2_PLACEMENT_3D ( 'NONE', #47566, #46555, #31832 ) ;
#87382=ORIENTED_EDGE ( 'NONE', *, *, #16675, .T. ) ;
#87383=DIRECTION ( 'NONE',  ( -1.000000000000000000, 0.000000000000000000, -0.000000000000000000 ) ) ;
#87385=ORIENTED_EDGE ( 'NONE', *, *, #27378, .F. ) ;
#87394=PLANE ( 'NONE',  #65688 ) ;
#87398=DIRECTION ( 'NONE',  ( 0.000000000000000000, -1.000000000000000000, 0.000000000000000000 ) ) ;
#87399=DIRECTION ( 'NONE',  ( 0.000000000000000000, 1.000000000000000000, -0.000000000000000000 ) ) ;
#87414=DIRECTION ( 'NONE',  ( 0.000000000000000000, -1.000000000000000000, 0.000000000000000000 ) ) ;
#87417=EDGE_CURVE ( 'NONE', #47644, #73404, #93808, .T. ) ;
#87423=CARTESIAN_POINT ( 'NONE',  ( 33.69795529655567634, 0.6647747205144264315, 23.11160796525322070 ) ) ;
#87429=DIRECTION ( 'NONE',  ( 0.000000000000000000, -1.000000000000000000, 0.000000000000000000 ) ) ;
#87453=ORIENTED_EDGE ( 'NONE', *, *, #8305, .T. ) ;
#87454=ADVANCED_FACE ( 'NONE', ( #61312 ), #60312, .F. ) ;
#87456=EDGE_CURVE ( 'NONE', #92122, #51818, #83119, .T. ) ;
#87485=CARTESIAN_POINT ( 'NONE',  ( 8.016553709168819708, 5.226461770140181429, -25.82553693194279276 ) ) ;
#87497=PLANE ( 'NONE',  #64859 ) ;
#87542=DIRECTION ( 'NONE',  ( -0.000000000000000000, -1.000000000000000000, -0.000000000000000000 ) ) ;
#87575=CARTESIAN_POINT ( 'NONE',  ( 15.10352928271630724, 3.582999323269832725, -27.29968155418892195 ) ) ;
#87578=DIRECTION ( 'NONE',  ( -1.000000000000000000, 0.000000000000000000, 0.000000000000000000 ) ) ;
#87592=FACE_OUTER_BOUND ( 'NONE', #23574, .T. ) ;
#87601=CARTESIAN_POINT ( 'NONE',  ( 23.91005183030481263, 2.682774720514426559, -14.40591128290692069 ) ) ;
#87618=ORIENTED_EDGE ( 'NONE', *, *, #17223, .F. ) ;
#87621=ORIENTED_EDGE ( 'NONE', *, *, #94936, .F. ) ;
#87627=EDGE_LOOP ( 'NONE', ( #31052, #28335 ) ) ;
#87634=FACE_OUTER_BOUND ( 'NONE', #18615, .T. ) ;
#87643=CIRCLE ( 'NONE', #3349, 3.060000000000000053 ) ;
#87648=DIRECTION ( 'NONE',  ( -0.000000000000000000, -1.000000000000000000, 0.000000000000000000 ) ) ;
#87661=VERTEX_POINT ( 'NONE', #65819 ) ;
#87664=CIRCLE ( 'NONE', #56897, 0.8160000000000007248 ) ;
#87676=DIRECTION ( 'NONE',  ( 0.000000000000000000, -0.000000000000000000, 1.000000000000000000 ) ) ;
#87686=DIRECTION ( 'NONE',  ( -1.226388327005079762E-16, -0.000000000000000000, 1.000000000000000000 ) ) ;
#87698=ORIENTED_EDGE ( 'NONE', *, *, #85531, .T. ) ;
#87699=DIRECTION ( 'NONE',  ( -0.000000000000000000, -0.000000000000000000, -1.000000000000000000 ) ) ;
#87714=DIRECTION ( 'NONE',  ( -0.000000000000000000, 1.000000000000000000, -0.000000000000000000 ) ) ;
#87733=DIRECTION ( 'NONE',  ( -0.7071067811865475727, 0.000000000000000000, 0.7071067811865475727 ) ) ;
#87748=DIRECTION ( 'NONE',  ( 0.000000000000000000, 0.000000000000000000, -1.000000000000000000 ) ) ;
#87761=EDGE_CURVE ( 'NONE', #39929, #6907, #84005, .T. ) ;
#87787=DIRECTION ( 'NONE',  ( 0.000000000000000000, 1.000000000000000000, -0.000000000000000000 ) ) ;
#87807=CARTESIAN_POINT ( 'NONE',  ( 4.712727796232543120, 5.356774720514425603, -25.55789472434992859 ) ) ;
#87814=PLANE ( 'NONE',  #35869 ) ;
#87815=ADVANCED_FACE ( 'NONE', ( #99222 ), #53077, .F. ) ;
#87828=EDGE_CURVE ( 'NONE', #14476, #62563, #59189, .T. ) ;
#87831=CARTESIAN_POINT ( 'NONE',  ( 12.98941176893815275, 6.376774720517114581, -28.15829778590956067 ) ) ;
#87842=EDGE_CURVE ( 'NONE', #23691, #74261, #92116, .T. ) ;
#87847=DIRECTION ( 'NONE',  ( -0.000000000000000000, 1.000000000000000000, -0.000000000000000000 ) ) ;
#87848=AXIS2_PLACEMENT_3D ( 'NONE', #88339, #10210, #18813 ) ;
#87862=CIRCLE ( 'NONE', #74885, 1.835999999999993859 ) ;
#87863=DIRECTION ( 'NONE',  ( 0.000000000000000000, -1.000000000000000000, 0.000000000000000000 ) ) ;
#87883=VERTEX_POINT ( 'NONE', #68793 ) ;
#87884=FACE_BOUND ( 'NONE', #49197, .T. ) ;
#87931=EDGE_CURVE ( 'NONE', #78861, #12744, #51077, .T. ) ;
#87932=FACE_OUTER_BOUND ( 'NONE', #8619, .T. ) ;
#87945=EDGE_CURVE ( 'NONE', #79911, #38639, #63699, .T. ) ;
#87946=CIRCLE ( 'NONE', #44199, 12.65241003308276113 ) ;
#87980=CIRCLE ( 'NONE', #86378, 2.499999999999998668 ) ;
#87986=AXIS2_PLACEMENT_3D ( 'NONE', #90065, #82445, #36285 ) ;
#88001=DIRECTION ( 'NONE',  ( -0.000000000000000000, -1.000000000000000000, -0.000000000000000000 ) ) ;
#88006=CARTESIAN_POINT ( 'NONE',  ( 29.80070917940689768, 3.316774720514426456, 27.39560796525317343 ) ) ;
#88007=LINE ( 'NONE', #10880, #49945 ) ;
#88010=AXIS2_PLACEMENT_3D ( 'NONE', #62885, #54760, #32916 ) ;
#88012=LINE ( 'NONE', #100075, #93444 ) ;
#88014=DIRECTION ( 'NONE',  ( -0.000000000000000000, -1.000000000000000000, -0.000000000000000000 ) ) ;
#88037=VERTEX_POINT ( 'NONE', #55068 ) ;
#88039=DIRECTION ( 'NONE',  ( 0.000000000000000000, -1.000000000000000000, 0.000000000000000000 ) ) ;
#88040=CYLINDRICAL_SURFACE ( 'NONE', #5104, 129.7684398600581517 ) ;
#88045=VERTEX_POINT ( 'NONE', #94111 ) ;
#88046=ORIENTED_EDGE ( 'NONE', *, *, #81891, .F. ) ;
#88049=CYLINDRICAL_SURFACE ( 'NONE', #9702, 1.150000000000003464 ) ;
#88055=ORIENTED_EDGE ( 'NONE', *, *, #74935, .F. ) ;
#88067=CARTESIAN_POINT ( 'NONE',  ( -19.38764004357183524, -5.965225279485572685, -21.62823517627350611 ) ) ;
#88082=DIRECTION ( 'NONE',  ( 0.000000000000000000, 0.000000000000000000, 1.000000000000000000 ) ) ;
#88107=PLANE ( 'NONE',  #93321 ) ;
#88111=LINE ( 'NONE', #49055, #68102 ) ;
#88125=EDGE_LOOP ( 'NONE', ( #3196, #39909, #16650, #13098 ) ) ;
#88137=CYLINDRICAL_SURFACE ( 'NONE', #65548, 11.85241003308275864 ) ;
#88144=VECTOR ( 'NONE', #14589, 1000.000000000000000 ) ;
#88149=ORIENTED_EDGE ( 'NONE', *, *, #41585, .F. ) ;
#88150=EDGE_CURVE ( 'NONE', #10013, #36340, #22577, .T. ) ;
#88151=CARTESIAN_POINT ( 'NONE',  ( 32.06540688909006320, 1.682774720514426114, -12.44045471929205604 ) ) ;
#88154=ORIENTED_EDGE ( 'NONE', *, *, #58026, .T. ) ;
#88162=EDGE_CURVE ( 'NONE', #12021, #95021, #50449, .T. ) ;
#88168=EDGE_CURVE ( 'NONE', #66710, #55229, #56072, .T. ) ;
#88179=EDGE_CURVE ( 'NONE', #21001, #37842, #6385, .T. ) ;
#88190=CARTESIAN_POINT ( 'NONE',  ( 19.72776355195876263, -5.965225279485572685, 28.39950002376592764 ) ) ;
#88204=CARTESIAN_POINT ( 'NONE',  ( 29.80070917940689412, 0.6647747205144266536, 27.39560796525321607 ) ) ;
#88206=AXIS2_PLACEMENT_3D ( 'NONE', #50189, #13100, #58307 ) ;
#88210=DIRECTION ( 'NONE',  ( -0.000000000000000000, -1.000000000000000000, -0.000000000000000000 ) ) ;
#88222=LINE ( 'NONE', #35918, #2191 ) ;
#88232=DIRECTION ( 'NONE',  ( 0.000000000000000000, -1.000000000000000000, 0.000000000000000000 ) ) ;
#88235=LINE ( 'NONE', #18698, #23627 ) ;
#88240=DIRECTION ( 'NONE',  ( -0.000000000000000000, -1.000000000000000000, 0.000000000000000000 ) ) ;
#88263=ADVANCED_FACE ( 'NONE', ( #44340 ), #12370, .F. ) ;
#88267=EDGE_CURVE ( 'NONE', #52090, #26199, #27466, .T. ) ;
#88286=EDGE_CURVE ( 'NONE', #80243, #68064, #21466, .T. ) ;
#88287=ORIENTED_EDGE ( 'NONE', *, *, #41703, .T. ) ;
#88309=PLANE ( 'NONE',  #13545 ) ;
#88313=FACE_OUTER_BOUND ( 'NONE', #43772, .T. ) ;
#88319=DIRECTION ( 'NONE',  ( -0.000000000000000000, 1.000000000000000000, 0.000000000000000000 ) ) ;
#88332=EDGE_CURVE ( 'NONE', #79545, #73404, #36222, .T. ) ;
#88334=ORIENTED_EDGE ( 'NONE', *, *, #35402, .F. ) ;
#88337=DIRECTION ( 'NONE',  ( 0.000000000000000000, -1.000000000000000000, 0.000000000000000000 ) ) ;
#88339=CARTESIAN_POINT ( 'NONE',  ( 27.53860345374771867, 1.682774720514426114, -9.482392034746240483 ) ) ;
#88340=CARTESIAN_POINT ( 'NONE',  ( -28.98875734969026041, 3.316774720514426456, -0.08597719988137648983 ) ) ;
#88343=FACE_OUTER_BOUND ( 'NONE', #26906, .T. ) ;
#88351=CARTESIAN_POINT ( 'NONE',  ( 15.88393883468562606, 3.596971506840126676, -28.01277999924193551 ) ) ;
#88353=VERTEX_POINT ( 'NONE', #98100 ) ;
#88358=CARTESIAN_POINT ( 'NONE',  ( 29.59866736649642860, 4.678593451839772044, 28.90589631152484174 ) ) ;
#88360=ORIENTED_EDGE ( 'NONE', *, *, #14540, .F. ) ;
#88383=ADVANCED_FACE ( 'NONE', ( #6753 ), #4772, .T. ) ;
#88387=EDGE_CURVE ( 'NONE', #44858, #50853, #35726, .T. ) ;
#88389=DIRECTION ( 'NONE',  ( 0.9913618264504693300, -5.365801633547217234E-16, -0.1311553622875920033 ) ) ;
#88391=CARTESIAN_POINT ( 'NONE',  ( 27.53860345374771867, 4.132774720517318201, -9.482392034746240483 ) ) ;
#88401=AXIS2_PLACEMENT_3D ( 'NONE', #37440, #38433, #45560 ) ;
#88411=CARTESIAN_POINT ( 'NONE',  ( 1.305682803664691249, 0.3587747205144265483, 29.57950906855421991 ) ) ;
#88430=VERTEX_POINT ( 'NONE', #68667 ) ;
#88432=CARTESIAN_POINT ( 'NONE',  ( -0.02075734969026423599, 6.376774720514426953, -0.08597719988137648983 ) ) ;
#88435=ORIENTED_EDGE ( 'NONE', *, *, #39819, .F. ) ;
#88476=EDGE_LOOP ( 'NONE', ( #71538, #27951, #88789, #76605, #34617, #68179, #48968, #7251, #4125, #62819, #90114 ) ) ;
#88486=CARTESIAN_POINT ( 'NONE',  ( -10.17728017005432228, 5.183720752832764234, 29.88674535377839803 ) ) ;
#88504=ORIENTED_EDGE ( 'NONE', *, *, #56229, .F. ) ;
#88506=CARTESIAN_POINT ( 'NONE',  ( -10.21384395349174490, 3.316774720514427344, 29.49402280011862487 ) ) ;
#88513=CARTESIAN_POINT ( 'NONE',  ( -24.90875734969025501, -5.965225279485572685, 30.51402280011862089 ) ) ;
#88517=EDGE_CURVE ( 'NONE', #85275, #68532, #7966, .T. ) ;
#88543=VERTEX_POINT ( 'NONE', #49344 ) ;
#88557=CARTESIAN_POINT ( 'NONE',  ( 11.32388168880214074, 5.356774720514423827, -25.00917421515942962 ) ) ;
#88571=EDGE_CURVE ( 'NONE', #45940, #17901, #68979, .T. ) ;
#88572=ADVANCED_FACE ( 'NONE', ( #72175 ), #37160, .T. ) ;
#88574=DIRECTION ( 'NONE',  ( 0.000000000000000000, 0.000000000000000000, -1.000000000000000000 ) ) ;
#88578=DIRECTION ( 'NONE',  ( -0.000000000000000000, 1.000000000000000000, -0.000000000000000000 ) ) ;
#88580=B_SPLINE_CURVE_WITH_KNOTS ( 'NONE', 3,
 ( #53898, #76700, #23412, #7202, #38151 ),
 .UNSPECIFIED., .F., .F.,
 ( 4, 1, 4 ),
 ( 0.07540175290935291486, 0.07668996298668992462, 0.07797817306402693438 ),
 .UNSPECIFIED. ) ;
#88581=CARTESIAN_POINT ( 'NONE',  ( 13.02968616431334681, 5.152774720514426754, -26.31186222701397526 ) ) ;
#88594=EDGE_CURVE ( 'NONE', #3153, #25992, #73172, .T. ) ;
#88610=ADVANCED_FACE ( 'NONE', ( #24977 ), #55951, .F. ) ;
#88615=AXIS2_PLACEMENT_3D ( 'NONE', #6859, #1258, #53552 ) ;
#88629=ADVANCED_FACE ( 'NONE', ( #79766 ), #10262, .T. ) ;
#88649=VERTEX_POINT ( 'NONE', #98478 ) ;
#88656=CARTESIAN_POINT ( 'NONE',  ( 8.219458839706481612, 3.316774720514422015, -27.11006393991256758 ) ) ;
#88665=CARTESIAN_POINT ( 'NONE',  ( 29.73860345376319358, 3.356774720514427379, 1.647607965253217621 ) ) ;
#88692=AXIS2_PLACEMENT_3D ( 'NONE', #88755, #3022, #87748 ) ;
#88701=EDGE_LOOP ( 'NONE', ( #76126, #82140, #54955, #97512 ) ) ;
#88707=DIRECTION ( 'NONE',  ( 0.000000000000000000, -1.000000000000000000, 0.000000000000000000 ) ) ;
#88712=CARTESIAN_POINT ( 'NONE',  ( 6.671786015990716301, -6.475225279485573360, -27.29955796265488033 ) ) ;
#88715=ORIENTED_EDGE ( 'NONE', *, *, #67775, .T. ) ;
#88718=LINE ( 'NONE', #94317, #94357 ) ;
#88724=EDGE_CURVE ( 'NONE', #70078, #63086, #30714, .T. ) ;
#88731=CARTESIAN_POINT ( 'NONE',  ( -19.77875734969026311, 3.316774720514426456, 29.49402280011862487 ) ) ;
#88744=VERTEX_POINT ( 'NONE', #52823 ) ;
#88755=CARTESIAN_POINT ( 'NONE',  ( 282.9764569301858046, -5.965225279485572685, 20.79159422840526616 ) ) ;
#88761=VERTEX_POINT ( 'NONE', #1034 ) ;
#88779=EDGE_CURVE ( 'NONE', #31830, #65938, #14484, .T. ) ;
#88785=EDGE_CURVE ( 'NONE', #23597, #79746, #6639, .T. ) ;
#88789=ORIENTED_EDGE ( 'NONE', *, *, #4304, .F. ) ;
#88799=DIRECTION ( 'NONE',  ( 1.000000000000000000, 0.000000000000000000, 0.000000000000000000 ) ) ;
#88817=CARTESIAN_POINT ( 'NONE',  ( 0.000000000000000000, -1.473225279485573802, 0.000000000000000000 ) ) ;
#88818=FACE_OUTER_BOUND ( 'NONE', #12754, .T. ) ;
#88823=ORIENTED_EDGE ( 'NONE', *, *, #55865, .T. ) ;
#88829=CIRCLE ( 'NONE', #77419, 3.349999999999998757 ) ;
#88841=CARTESIAN_POINT ( 'NONE',  ( 33.62089986283198328, 3.615790004618635312, -11.40738377976237672 ) ) ;
#88843=ADVANCED_FACE ( 'NONE', ( #85258 ), #69552, .T. ) ;
#88849=ADVANCED_FACE ( 'NONE', ( #92871 ), #23349, .F. ) ;
#88851=ORIENTED_EDGE ( 'NONE', *, *, #13111, .T. ) ;
#88878=ORIENTED_EDGE ( 'NONE', *, *, #27469, .F. ) ;
#88881=VERTEX_POINT ( 'NONE', #48219 ) ;
#88911=FACE_OUTER_BOUND ( 'NONE', #3547, .T. ) ;
#88932=DIRECTION ( 'NONE',  ( -0.000000000000000000, -1.000000000000000000, -0.000000000000000000 ) ) ;
#88934=ORIENTED_EDGE ( 'NONE', *, *, #44459, .T. ) ;
#88943=EDGE_CURVE ( 'NONE', #51332, #55726, #71556, .T. ) ;
#88959=CARTESIAN_POINT ( 'NONE',  ( 13.91401389203221406, -5.965225279485572685, 158.0376437107427137 ) ) ;
#88964=EDGE_CURVE ( 'NONE', #21001, #10246, #10649, .T. ) ;
#88975=LINE ( 'NONE', #64664, #36562 ) ;
#88983=ORIENTED_EDGE ( 'NONE', *, *, #18898, .F. ) ;
#88989=CARTESIAN_POINT ( 'NONE',  ( 27.53860345374771867, -1.477225279485574028, -9.482392034746240483 ) ) ;
#89001=DIRECTION ( 'NONE',  ( 0.000000000000000000, 0.000000000000000000, -1.000000000000000000 ) ) ;
#89005=CARTESIAN_POINT ( 'NONE',  ( 32.33217928425145971, 1.682774720514426114, -12.20610769812826923 ) ) ;
#89020=VERTEX_POINT ( 'NONE', #56844 ) ;
#89028=VECTOR ( 'NONE', #20945, 1000.000000000000000 ) ;
#89048=FACE_OUTER_BOUND ( 'NONE', #77007, .T. ) ;
#89049=B_SPLINE_CURVE_WITH_KNOTS ( 'NONE', 3,
 ( #25657, #27166, #73343, #35284, #11932, #42897, #65746 ),
 .UNSPECIFIED., .F., .F.,
 ( 4, 1, 1, 1, 4 ),
 ( 0.3452202732246780759, 0.4949101844912719983, 0.6446000957578658097, 0.7942900070244596211, 0.9439799182910535436 ),
 .UNSPECIFIED. ) ;
#89057=CARTESIAN_POINT ( 'NONE',  ( 5.659515148182856947, 5.356774720518939326, -27.47062408582486270 ) ) ;
#89058=CARTESIAN_POINT ( 'NONE',  ( 32.16024265030974050, 0.3587747205144265483, 16.27760796525321751 ) ) ;
#89061=LINE ( 'NONE', #11430, #26408 ) ;
#89071=PLANE ( 'NONE',  #63666 ) ;
#89076=DIRECTION ( 'NONE',  ( 0.7512896232465891000, -0.000000000000000000, 0.6599726524652351767 ) ) ;
#89088=EDGE_CURVE ( 'NONE', #28802, #149, #14558, .T. ) ;
#89095=CIRCLE ( 'NONE', #22569, 28.96799999999999287 ) ;
#89096=EDGE_CURVE ( 'NONE', #3302, #24683, #21003, .T. ) ;
#89105=LINE ( 'NONE', #41944, #45441 ) ;
#89108=DIRECTION ( 'NONE',  ( -0.000000000000000000, -1.000000000000000000, 0.000000000000000000 ) ) ;
#89124=VERTEX_POINT ( 'NONE', #66465 ) ;
#89147=DIRECTION ( 'NONE',  ( 0.000000000000000000, 0.000000000000000000, -1.000000000000000000 ) ) ;
#89150=DIRECTION ( 'NONE',  ( -0.000000000000000000, 1.000000000000000000, -0.000000000000000000 ) ) ;
#89160=EDGE_LOOP ( 'NONE', ( #49995, #14730, #48440, #86052 ) ) ;
#89169=CARTESIAN_POINT ( 'NONE',  ( 32.98210467718394767, 3.587965230352024193, -12.99284425914657604 ) ) ;
#89172=LINE ( 'NONE', #50117, #41963 ) ;
#89176=CARTESIAN_POINT ( 'NONE',  ( 28.30015606816038698, 2.682774720514426559, -13.13501953239208575 ) ) ;
#89182=VECTOR ( 'NONE', #17588, 1000.000000000000000 ) ;
#89186=CARTESIAN_POINT ( 'NONE',  ( -24.90875734969025501, -6.475225279485573360, 26.43402280011862615 ) ) ;
#89192=DIRECTION ( 'NONE',  ( -0.000000000000000000, -1.000000000000000000, 0.000000000000000000 ) ) ;
#89216=LINE ( 'NONE', #32046, #35519 ) ;
#89245=DIRECTION ( 'NONE',  ( 0.000000000000000000, 0.000000000000000000, 1.000000000000000000 ) ) ;
#89251=LINE ( 'NONE', #50692, #56524 ) ;
#89260=CARTESIAN_POINT ( 'NONE',  ( 13.10664265030973930, -1.324225279485583551, -28.18129937516353678 ) ) ;
#89261=ORIENTED_EDGE ( 'NONE', *, *, #60826, .F. ) ;
#89271=DIRECTION ( 'NONE',  ( -0.06486421869277853025, 0.000000000000000000, 0.9978940991575084851 ) ) ;
#89293=FACE_OUTER_BOUND ( 'NONE', #57318, .T. ) ;
#89316=DIRECTION ( 'NONE',  ( -1.000000000000000000, -0.000000000000000000, -0.000000000000000000 ) ) ;
#89325=VECTOR ( 'NONE', #78434, 1000.000000000000000 ) ;
#89326=ORIENTED_EDGE ( 'NONE', *, *, #7174, .F. ) ;
#89342=DIRECTION ( 'NONE',  ( 1.000000000000000000, 0.000000000000000000, -0.000000000000000000 ) ) ;
#89356=CARTESIAN_POINT ( 'NONE',  ( 29.67519708478274865, 5.974976214603829661, 27.68766025429119537 ) ) ;
#89363=AXIS2_PLACEMENT_3D ( 'NONE', #94678, #69851, #1845 ) ;
#89373=ORIENTED_EDGE ( 'NONE', *, *, #62637, .T. ) ;
#89383=DIRECTION ( 'NONE',  ( 0.9980236263794188822, 0.000000000000000000, -0.06283980576413537855 ) ) ;
#89391=ORIENTED_EDGE ( 'NONE', *, *, #23347, .T. ) ;
#89411=EDGE_CURVE ( 'NONE', #94830, #57483, #10402, .T. ) ;
#89416=CARTESIAN_POINT ( 'NONE',  ( 14.61581676223891613, 3.316774720514426900, -27.35847991879931485 ) ) ;
#89419=DIRECTION ( 'NONE',  ( 0.000000000000000000, 0.000000000000000000, -1.000000000000000000 ) ) ;
#89440=DIRECTION ( 'NONE',  ( 1.000000000000000000, -0.000000000000000000, 0.000000000000000000 ) ) ;
#89458=TOROIDAL_SURFACE ( 'NONE', #32744, 132.8284398600581540, 3.060000000000000053 ) ;
#89469=DIRECTION ( 'NONE',  ( 1.226388327005079762E-16, 0.000000000000000000, -1.000000000000000000 ) ) ;
#89481=LINE ( 'NONE', #19958, #82224 ) ;
#89486=VERTEX_POINT ( 'NONE', #91017 ) ;
#89506=CARTESIAN_POINT ( 'NONE',  ( 31.42094490286590514, 4.276934461241891583, -0.4045216949806126339 ) ) ;
#89511=ORIENTED_EDGE ( 'NONE', *, *, #79437, .F. ) ;
#89532=EDGE_CURVE ( 'NONE', #64113, #84269, #99609, .T. ) ;
#89544=ORIENTED_EDGE ( 'NONE', *, *, #35220, .F. ) ;
#89567=LINE ( 'NONE', #90064, #6160 ) ;
#89571=LINE ( 'NONE', #72356, #98683 ) ;
#89574=DIRECTION ( 'NONE',  ( -0.000000000000000000, -1.000000000000000000, 0.000000000000000000 ) ) ;
#89591=CARTESIAN_POINT ( 'NONE',  ( 30.61643171255909479, 3.477635932356431869, 27.37433006808820579 ) ) ;
#89611=VECTOR ( 'NONE', #21170, 1000.000000000000000 ) ;
#89616=CARTESIAN_POINT ( 'NONE',  ( -6.741682653110981249, 0.3587747205144265483, 30.62569541381301619 ) ) ;
#89619=AXIS2_PLACEMENT_3D ( 'NONE', #1805, #64223, #95149 ) ;
#89620=ORIENTED_EDGE ( 'NONE', *, *, #57526, .F. ) ;
#89631=ORIENTED_EDGE ( 'NONE', *, *, #64587, .F. ) ;
#89653=EDGE_CURVE ( 'NONE', #22449, #73934, #80984, .T. ) ;
#89660=ORIENTED_EDGE ( 'NONE', *, *, #16939, .T. ) ;
#89666=CARTESIAN_POINT ( 'NONE',  ( 32.96821357219067750, 5.071478440980570213, -13.00504694253962867 ) ) ;
#89715=DIRECTION ( 'NONE',  ( -1.000000000000000000, -1.232047923278981953E-16, 0.000000000000000000 ) ) ;
#89761=ORIENTED_EDGE ( 'NONE', *, *, #89653, .T. ) ;
#89781=CARTESIAN_POINT ( 'NONE',  ( -65.05438548721848235, 3.316774720514426456, 29.49402280011861777 ) ) ;
#89801=DIRECTION ( 'NONE',  ( 1.000000000000000000, -0.000000000000000000, -0.000000000000000000 ) ) ;
#89804=CARTESIAN_POINT ( 'NONE',  ( 27.53860345374771867, 1.682774720514426114, -9.482392034746240483 ) ) ;
#89817=CARTESIAN_POINT ( 'NONE',  ( 30.77564450787170003, 4.772774720514425972, -9.689394075852829857 ) ) ;
#89819=EDGE_CURVE ( 'NONE', #95272, #85275, #77205, .T. ) ;
#89820=ORIENTED_EDGE ( 'NONE', *, *, #89819, .F. ) ;
#89824=EDGE_CURVE ( 'NONE', #74588, #88045, #64097, .T. ) ;
#89829=CARTESIAN_POINT ( 'NONE',  ( 32.84232313084847732, 4.840274619473232676, -11.71291885348859196 ) ) ;
#89831=DIRECTION ( 'NONE',  ( 0.000000000000000000, 0.000000000000000000, -1.000000000000000000 ) ) ;
#89842=EDGE_CURVE ( 'NONE', #94973, #79746, #1611, .T. ) ;
#89871=DIRECTION ( 'NONE',  ( -1.000000000000000000, 0.000000000000000000, 0.000000000000000000 ) ) ;
#89884=VERTEX_POINT ( 'NONE', #19387 ) ;
#89887=AXIS2_PLACEMENT_3D ( 'NONE', #27542, #97539, #38516 ) ;
#89898=DIRECTION ( 'NONE',  ( -0.000000000000000000, -1.000000000000000000, -0.000000000000000000 ) ) ;
#89910=DIRECTION ( 'NONE',  ( -1.226388327005079762E-16, -0.000000000000000000, 1.000000000000000000 ) ) ;
#89916=VECTOR ( 'NONE', #75103, 1000.000000000000000 ) ;
#89919=CARTESIAN_POINT ( 'NONE',  ( -10.79305683637731406, -5.965225279485594001, -27.49869550653260930 ) ) ;
#89920=EDGE_LOOP ( 'NONE', ( #33409, #796, #58970, #9018 ) ) ;
#89926=VECTOR ( 'NONE', #70425, 1000.000000000000000 ) ;
#89963=VERTEX_POINT ( 'NONE', #44239 ) ;
#89964=( BOUNDED_SURFACE ( )  B_SPLINE_SURFACE ( 3, 2, ( 
 ( #34069, #65043, #27456 ),
 ( #88351, #18825, #49807 ),
 ( #3623, #50297, #17841 ),
 ( #58415, #81233, #80740 ),
 ( #25444, #26947, #2624 ),
 ( #11223, #33563, #42200 ),
 ( #34570, #57916, #48803 ),
 ( #50793, #65540, #56420 ) ),
 .UNSPECIFIED., .F., .F., .F. ) 
 B_SPLINE_SURFACE_WITH_KNOTS ( ( 4, 2, 2, 4 ),
 ( 3, 3 ),
 ( -2.579859069429257801E-16, 0.0001012599413938864427, 0.0002025198827880308713, 0.0004050397655763197284 ),
 ( 0.000000000000000000, 1.000000000000000000 ),
 .UNSPECIFIED. ) 
 GEOMETRIC_REPRESENTATION_ITEM ( )  RATIONAL_B_SPLINE_SURFACE ( (
 ( 1.000000000000000000, 0.8117984224358012479, 1.000000000000000000),
 ( 1.000000000000000000, 0.8431000163380963919, 1.000000000000000000),
 ( 1.000000000000000000, 0.8706302742274230066, 1.000000000000000000),
 ( 1.000000000000000000, 0.9180857590576201321, 1.000000000000000000),
 ( 1.000000000000000000, 0.9379650217685419067, 1.000000000000000000),
 ( 1.000000000000000000, 0.9847826944374993285, 1.000000000000000000),
 ( 1.000000000000000000, 1.000057331645191283, 1.000000000000000000),
 ( 1.000000000000000000, 1.000000000000000000, 1.000000000000000000) ) ) 
 REPRESENTATION_ITEM ( '' )  SURFACE ( )  );
#89966=CARTESIAN_POINT ( 'NONE',  ( -28.98875734969026396, -5.965225279485572685, 2.362022800118626531 ) ) ;
#89971=EDGE_CURVE ( 'NONE', #41837, #95120, #95544, .T. ) ;
#89987=LINE ( 'NONE', #96110, #14561 ) ;
#89994=EDGE_CURVE ( 'NONE', #67426, #46485, #8118, .T. ) ;
#90012=LINE ( 'NONE', #12869, #76557 ) ;
#90014=EDGE_LOOP ( 'NONE', ( #87382, #26600, #37222, #78020 ) ) ;
#90033=EDGE_CURVE ( 'NONE', #1553, #9293, #60963, .T. ) ;
#90040=CARTESIAN_POINT ( 'NONE',  ( 33.13288845015618023, 0.3587747205144265483, -0.1650522222209214185 ) ) ;
#90051=FACE_OUTER_BOUND ( 'NONE', #41599, .T. ) ;
#90052=LINE ( 'NONE', #14409, #8313 ) ;
#90064=CARTESIAN_POINT ( 'NONE',  ( 25.61870917940689196, 0.3587747205144265483, 29.49402280011862487 ) ) ;
#90065=CARTESIAN_POINT ( 'NONE',  ( -4.568292318365942073, 0.3587747205144265483, 30.06720597538392425 ) ) ;
#90070=VECTOR ( 'NONE', #46374, 1000.000000000000000 ) ;
#90071=CARTESIAN_POINT ( 'NONE',  ( 7.462166178408539352, -6.475225279485573360, -27.67315496249664974 ) ) ;
#90072=CARTESIAN_POINT ( 'NONE',  ( -65.05438548721848235, 6.376774720514426953, 29.49402280011861777 ) ) ;
#90109=DIRECTION ( 'NONE',  ( 0.000000000000000000, -0.000000000000000000, 1.000000000000000000 ) ) ;
#90114=ORIENTED_EDGE ( 'NONE', *, *, #51496, .T. ) ;
#90117=ORIENTED_EDGE ( 'NONE', *, *, #93228, .T. ) ;
#90120=CARTESIAN_POINT ( 'NONE',  ( 0.000000000000000000, -16.94322527948557422, 0.000000000000000000 ) ) ;
#90125=DIRECTION ( 'NONE',  ( -0.000000000000000000, 1.000000000000000000, -0.000000000000000000 ) ) ;
#90131=DIRECTION ( 'NONE',  ( 0.000000000000000000, 1.000000000000000000, 0.000000000000000000 ) ) ;
#90133=ORIENTED_EDGE ( 'NONE', *, *, #24007, .F. ) ;
#90141=ORIENTED_EDGE ( 'NONE', *, *, #91593, .F. ) ;
#90151=AXIS2_PLACEMENT_3D ( 'NONE', #72714, #96040, #27535 ) ;
#90163=ORIENTED_EDGE ( 'NONE', *, *, #91709, .F. ) ;
#90170=DIRECTION ( 'NONE',  ( 0.000000000000000000, 0.000000000000000000, -1.000000000000000000 ) ) ;
#90173=DIRECTION ( 'NONE',  ( 0.000000000000000000, -0.000000000000000000, -1.000000000000000000 ) ) ;
#90181=DIRECTION ( 'NONE',  ( 0.000000000000000000, 0.000000000000000000, -1.000000000000000000 ) ) ;
#90193=VECTOR ( 'NONE', #94667, 1000.000000000000000 ) ;
#90194=CARTESIAN_POINT ( 'NONE',  ( 30.93860345374796594, -6.475225279485573360, 28.07639619989136293 ) ) ;
#90200=CARTESIAN_POINT ( 'NONE',  ( 16.15056352287345121, 3.622774720514426949, -27.77856273171767398 ) ) ;
#90207=LINE ( 'NONE', #21672, #59785 ) ;
#90233=ORIENTED_EDGE ( 'NONE', *, *, #34693, .T. ) ;
#90235=ORIENTED_EDGE ( 'NONE', *, *, #36044, .F. ) ;
#90240=CIRCLE ( 'NONE', #91825, 28.96799999999999642 ) ;
#90270=ORIENTED_EDGE ( 'NONE', *, *, #78404, .T. ) ;
#90272=PLANE ( 'NONE',  #1227 ) ;
#90282=DIRECTION ( 'NONE',  ( 0.000000000000000000, 1.000000000000000000, 0.000000000000000000 ) ) ;
#90284=CARTESIAN_POINT ( 'NONE',  ( 10.22568704553358643, -6.475225279485576024, -27.02513721610328901 ) ) ;
#90290=CARTESIAN_POINT ( 'NONE',  ( 30.53060340732035982, 4.594240983522013266, 19.84760796525321780 ) ) ;
#90304=CARTESIAN_POINT ( 'NONE',  ( -29.49875734969026198, -5.965225279485572685, 10.11402280011862587 ) ) ;
#90307=ORIENTED_EDGE ( 'NONE', *, *, #2278, .T. ) ;
#90324=DIRECTION ( 'NONE',  ( 0.000000000000000000, 0.000000000000000000, 1.000000000000000000 ) ) ;
#90325=CARTESIAN_POINT ( 'NONE',  ( 31.63207147031214106, 3.934018429836814601, 27.19231918963763661 ) ) ;
#90330=DIRECTION ( 'NONE',  ( 0.000000000000000000, -1.478457507934778393E-16, -1.000000000000000000 ) ) ;
#90331=ORIENTED_EDGE ( 'NONE', *, *, #87945, .F. ) ;
#90332=CIRCLE ( 'NONE', #9340, 1.149999999999998135 ) ;
#90355=CARTESIAN_POINT ( 'NONE',  ( 282.9764569301858046, -6.475225279485573360, 20.79159422840526616 ) ) ;
#90370=FACE_OUTER_BOUND ( 'NONE', #77457, .T. ) ;
#90410=DIRECTION ( 'NONE',  ( 0.000000000000000000, 0.000000000000000000, -1.000000000000000000 ) ) ;
#90417=ORIENTED_EDGE ( 'NONE', *, *, #87120, .F. ) ;
#90435=EDGE_LOOP ( 'NONE', ( #32914, #22501, #70932, #51076 ) ) ;
#90444=EDGE_CURVE ( 'NONE', #12272, #57426, #10043, .T. ) ;
#90445=CARTESIAN_POINT ( 'NONE',  ( -28.98875734969026396, -5.965225279485572685, 7.870022800118625206 ) ) ;
#90446=LINE ( 'NONE', #51897, #1481 ) ;
#90450=DIRECTION ( 'NONE',  ( 0.6755245625654127117, 0.4376337494475115442, 0.5934166046845339437 ) ) ;
#90464=ADVANCED_FACE ( 'NONE', ( #2949 ), #2441, .F. ) ;
#90486=ORIENTED_EDGE ( 'NONE', *, *, #82767, .T. ) ;
#90495=CARTESIAN_POINT ( 'NONE',  ( 30.61643171304413613, 6.376774720514426953, 27.37433008668288181 ) ) ;
#90503=ORIENTED_EDGE ( 'NONE', *, *, #46029, .F. ) ;
#90520=DIRECTION ( 'NONE',  ( 0.6599726524652353987, 0.000000000000000000, -0.7512896232465889890 ) ) ;
#90521=CARTESIAN_POINT ( 'NONE',  ( 15.03452642382691629, 3.688048319827653021, -27.40128341529668887 ) ) ;
#90527=PLANE ( 'NONE',  #72478 ) ;
#90530=EDGE_CURVE ( 'NONE', #28802, #74870, #81056, .T. ) ;
#90536=DIRECTION ( 'NONE',  ( -0.000000000000000000, -1.000000000000000000, -0.000000000000000000 ) ) ;
#90539=CARTESIAN_POINT ( 'NONE',  ( 10.22845072388260768, 5.356774720514425603, -24.98266432381545954 ) ) ;
#90540=EDGE_CURVE ( 'NONE', #99263, #13594, #3945, .T. ) ;
#90542=AXIS2_PLACEMENT_3D ( 'NONE', #98731, #36346, #90625 ) ;
#90552=DIRECTION ( 'NONE',  ( -1.000000000000000000, 0.000000000000000000, -7.994117400814786717E-16 ) ) ;
#90553=DIRECTION ( 'NONE',  ( 0.000000000000000000, 0.000000000000000000, -1.000000000000000000 ) ) ;
#90563=CARTESIAN_POINT ( 'NONE',  ( 13.74975846015576586, -6.475225279485573360, -27.72022515045486557 ) ) ;
#90567=EDGE_CURVE ( 'NONE', #74525, #74870, #89172, .T. ) ;
#90575=PLANE ( 'NONE',  #53217 ) ;
#90584=CARTESIAN_POINT ( 'NONE',  ( 30.59430046144282400, 4.508643932895013862, 26.46466010020539272 ) ) ;
#90587=CARTESIAN_POINT ( 'NONE',  ( 22.81105451610979173, 4.772774720514425972, -18.46691820600746681 ) ) ;
#90589=EDGE_CURVE ( 'NONE', #76855, #45940, #13024, .T. ) ;
#90614=CYLINDRICAL_SURFACE ( 'NONE', #33972, 1.149999999999999911 ) ;
#90625=DIRECTION ( 'NONE',  ( -1.000000000000000000, 0.000000000000000000, -0.000000000000000000 ) ) ;
#90637=DIRECTION ( 'NONE',  ( 1.251281512149627050E-16, 0.000000000000000000, -1.000000000000000000 ) ) ;
#90642=ORIENTED_EDGE ( 'NONE', *, *, #42343, .F. ) ;
#90660=ORIENTED_EDGE ( 'NONE', *, *, #99421, .F. ) ;
#90666=FACE_OUTER_BOUND ( 'NONE', #24721, .T. ) ;
#90690=AXIS2_PLACEMENT_3D ( 'NONE', #5783, #60594, #90520 ) ;
#90693=EDGE_CURVE ( 'NONE', #71246, #14248, #64683, .T. ) ;
#90694=CIRCLE ( 'NONE', #56751, 12.65241003308276113 ) ;
#90701=CARTESIAN_POINT ( 'NONE',  ( 10.64801255963128668, -6.475225279485572472, -27.03041135669327488 ) ) ;
#90706=CARTESIAN_POINT ( 'NONE',  ( 24.71017632900191074, 3.356774720514427379, 1.647607965253217621 ) ) ;
#90708=LINE ( 'NONE', #82594, #33849 ) ;
#90733=EDGE_LOOP ( 'NONE', ( #29453, #32342, #22350, #40218 ) ) ;
#90744=CARTESIAN_POINT ( 'NONE',  ( 29.73860345376319358, -1.477225279485574028, -1.352392034746782823 ) ) ;
#90748=ORIENTED_EDGE ( 'NONE', *, *, #62758, .F. ) ;
#90755=VECTOR ( 'NONE', #91474, 1000.000000000000000 ) ;
#90775=EDGE_CURVE ( 'NONE', #65689, #46666, #95100, .T. ) ;
#90777=ORIENTED_EDGE ( 'NONE', *, *, #14933, .T. ) ;
#90791=CARTESIAN_POINT ( 'NONE',  ( 30.53060340732036693, 5.168534691225920241, 8.812171101699174613 ) ) ;
#90807=CARTESIAN_POINT ( 'NONE',  ( 29.80070917940689412, -5.965225279485572685, 27.39560796525321607 ) ) ;
#90813=LINE ( 'NONE', #51257, #96637 ) ;
#90820=CARTESIAN_POINT ( 'NONE',  ( 10.40220176116686979, 5.447062032237068863, -27.19353416079722763 ) ) ;
#90830=CARTESIAN_POINT ( 'NONE',  ( -24.90875734969025501, -6.475225279485573360, 29.49402280011861777 ) ) ;
#90832=DIRECTION ( 'NONE',  ( 0.06486421869277853025, 0.000000000000000000, -0.9978940991575085961 ) ) ;
#90837=LINE ( 'NONE', #58897, #80840 ) ;
#90842=DIRECTION ( 'NONE',  ( -0.000000000000000000, 1.000000000000000000, -0.000000000000000000 ) ) ;
#90860=ORIENTED_EDGE ( 'NONE', *, *, #16061, .T. ) ;
#90880=CARTESIAN_POINT ( 'NONE',  ( 32.54003107466018463, 4.047905215973556459, -1.500050581001865169 ) ) ;
#90883=AXIS2_PLACEMENT_3D ( 'NONE', #83039, #29264, #84050 ) ;
#90940=EDGE_CURVE ( 'NONE', #61907, #18192, #66177, .T. ) ;
#90946=EDGE_CURVE ( 'NONE', #76643, #49424, #26187, .T. ) ;
#90947=PLANE ( 'NONE',  #11315 ) ;
#90953=CARTESIAN_POINT ( 'NONE',  ( 19.75748517575715368, 0.3587747205144265483, 28.87153971905864580 ) ) ;
#90960=LINE ( 'NONE', #68133, #38763 ) ;
#90966=VECTOR ( 'NONE', #51377, 1000.000000000000000 ) ;
#90976=CARTESIAN_POINT ( 'NONE',  ( 31.20850673110457763, 5.144960210277549351, -4.610511713824573476 ) ) ;
#90994=ORIENTED_EDGE ( 'NONE', *, *, #65203, .F. ) ;
#91000=ORIENTED_EDGE ( 'NONE', *, *, #13555, .F. ) ;
#91010=CARTESIAN_POINT ( 'NONE',  ( -29.49875734969025842, 0.3587747205144265483, 25.61802280011862720 ) ) ;
#91017=CARTESIAN_POINT ( 'NONE',  ( -27.15721599100127648, -5.965225279485572685, -10.22292133548836546 ) ) ;
#91021=ORIENTED_EDGE ( 'NONE', *, *, #313, .F. ) ;
#91023=EDGE_CURVE ( 'NONE', #63208, #24140, #77725, .T. ) ;
#91026=AXIS2_PLACEMENT_3D ( 'NONE', #65270, #89574, #74346 ) ;
#91028=ADVANCED_FACE ( 'NONE', ( #1131 ), #12906, .T. ) ;
#91033=EDGE_LOOP ( 'NONE', ( #61952, #68281, #88851, #8789 ) ) ;
#91037=ORIENTED_EDGE ( 'NONE', *, *, #2219, .T. ) ;
#91059=LINE ( 'NONE', #12929, #72629 ) ;
#91067=DIRECTION ( 'NONE',  ( -0.000000000000000000, 1.000000000000000000, -0.000000000000000000 ) ) ;
#91073=CARTESIAN_POINT ( 'NONE',  ( 31.51256023177338861, 4.716437395117331732, -1.484035900832843868 ) ) ;
#91080=CARTESIAN_POINT ( 'NONE',  ( 30.61138385796263606, 5.156104205939422869, 27.19700247792284031 ) ) ;
#91085=EDGE_LOOP ( 'NONE', ( #13249, #60341, #42099, #58254, #304 ) ) ;
#91099=LINE ( 'NONE', #22561, #905 ) ;
#91115=EDGE_CURVE ( 'NONE', #4424, #24841, #79227, .T. ) ;
#91122=DIRECTION ( 'NONE',  ( -0.9822594791677485837, 0.000000000000000000, 0.1875268396392986980 ) ) ;
#91152=CARTESIAN_POINT ( 'NONE',  ( -22.05275734969026047, -5.965225279485572685, 31.02402280011862246 ) ) ;
#91163=EDGE_CURVE ( 'NONE', #17845, #65436, #72202, .T. ) ;
#91189=CARTESIAN_POINT ( 'NONE',  ( 9.843544857143434967, -6.475225279485573360, -27.49819965379373343 ) ) ;
#91197=DIRECTION ( 'NONE',  ( 1.000000000000000000, -0.000000000000000000, -0.000000000000000000 ) ) ;
#91200=AXIS2_PLACEMENT_3D ( 'NONE', #8516, #78004, #30850 ) ;
#91202=ORIENTED_EDGE ( 'NONE', *, *, #20328, .T. ) ;
#91203=CARTESIAN_POINT ( 'NONE',  ( 30.55234109742892912, 6.376774720514427841, 1.942002712049490487 ) ) ;
#91222=ORIENTED_EDGE ( 'NONE', *, *, #75193, .F. ) ;
#91234=CARTESIAN_POINT ( 'NONE',  ( -28.84663072490566194, -5.965225279485572685, 28.73989617533406715 ) ) ;
#91236=CARTESIAN_POINT ( 'NONE',  ( -0.02075734969026423599, -5.965225279485572685, -28.54397719988136828 ) ) ;
#91241=CARTESIAN_POINT ( 'NONE',  ( 30.09341516180546350, 2.682774720514426559, -11.39311774897855756 ) ) ;
#91246=DIRECTION ( 'NONE',  ( -0.000000000000000000, 1.000000000000000000, -0.000000000000000000 ) ) ;
#91249=ORIENTED_EDGE ( 'NONE', *, *, #89819, .T. ) ;
#91253=ADVANCED_FACE ( 'NONE', ( #83667 ), #6553, .F. ) ;
#91263=ADVANCED_FACE ( 'NONE', ( #36496 ), #22254, .T. ) ;
#91266=EDGE_LOOP ( 'NONE', ( #14746, #93119, #8493, #6914 ) ) ;
#91272=CARTESIAN_POINT ( 'NONE',  ( 14.82775695341588573, 5.152774720514427642, -26.90408793620859385 ) ) ;
#91286=CARTESIAN_POINT ( 'NONE',  ( 12.67628326092776803, 4.091305608280291217, -27.97525530010125294 ) ) ;
#91305=AXIS2_PLACEMENT_3D ( 'NONE', #61829, #88039, #57599 ) ;
#91313=ORIENTED_EDGE ( 'NONE', *, *, #87456, .F. ) ;
#91316=DIRECTION ( 'NONE',  ( 6.220620959342031946E-15, 0.000000000000000000, -1.000000000000000000 ) ) ;
#91318=ORIENTED_EDGE ( 'NONE', *, *, #100404, .T. ) ;
#91322=DIRECTION ( 'NONE',  ( -0.000000000000000000, 1.000000000000000000, -0.000000000000000000 ) ) ;
#91326=VERTEX_POINT ( 'NONE', #1450 ) ;
#91330=LINE ( 'NONE', #67511, #89916 ) ;
#91331=LINE ( 'NONE', #76098, #72734 ) ;
#91335=CARTESIAN_POINT ( 'NONE',  ( 30.09341516180546350, -1.477225279485574028, -11.39311774897855756 ) ) ;
#91336=ORIENTED_EDGE ( 'NONE', *, *, #20786, .F. ) ;
#91347=EDGE_CURVE ( 'NONE', #21600, #4176, #1530, .T. ) ;
#91351=ORIENTED_EDGE ( 'NONE', *, *, #69511, .T. ) ;
#91360=ORIENTED_EDGE ( 'NONE', *, *, #94882, .F. ) ;
#91362=CARTESIAN_POINT ( 'NONE',  ( -0.02075734969026423599, 3.316774720514426456, -0.08597719988137648983 ) ) ;
#91398=ADVANCED_FACE ( 'NONE', ( #80481 ), #25695, .F. ) ;
#91418=AXIS2_PLACEMENT_3D ( 'NONE', #26934, #96442, #65525 ) ;
#91432=VERTEX_POINT ( 'NONE', #32814 ) ;
#91448=CARTESIAN_POINT ( 'NONE',  ( 14.92791587776674334, 5.037605299509791301, -27.26084882802267373 ) ) ;
#91471=PLANE ( 'NONE',  #93942 ) ;
#91472=ORIENTED_EDGE ( 'NONE', *, *, #30454, .T. ) ;
#91474=DIRECTION ( 'NONE',  ( 0.7689940216596065081, -7.885106708985488048E-16, -0.6392559695863502256 ) ) ;
#91482=DIRECTION ( 'NONE',  ( 0.000000000000000000, 1.000000000000000000, 0.000000000000000000 ) ) ;
#91491=VECTOR ( 'NONE', #100283, 1000.000000000000114 ) ;
#91495=ORIENTED_EDGE ( 'NONE', *, *, #27171, .F. ) ;
#91518=EDGE_CURVE ( 'NONE', #35425, #79911, #66282, .T. ) ;
#91520=ORIENTED_EDGE ( 'NONE', *, *, #84654, .T. ) ;
#91521=CARTESIAN_POINT ( 'NONE',  ( 5.097264368846809113, -1.579225279485572342, -27.56135813788808875 ) ) ;
#91526=CARTESIAN_POINT ( 'NONE',  ( 32.87794144969610244, 3.622774687813811845, -13.08434676285136256 ) ) ;
#91532=DIRECTION ( 'NONE',  ( -1.000000000000000000, 8.673617379884040402E-17, -6.938893903907232322E-16 ) ) ;
#91540=CARTESIAN_POINT ( 'NONE',  ( -0.02075734969026423599, 3.316774720514426456, -0.08597719988137648983 ) ) ;
#91557=DIRECTION ( 'NONE',  ( 0.000000000000000000, -1.000000000000000000, 0.000000000000000000 ) ) ;
#91568=CARTESIAN_POINT ( 'NONE',  ( 31.50451260799805198, 4.115674466082359650, -1.392914706732841790 ) ) ;
#91572=LINE ( 'NONE', #68749, #23592 ) ;
#91590=VERTEX_POINT ( 'NONE', #98697 ) ;
#91593=EDGE_CURVE ( 'NONE', #17901, #39863, #87342, .T. ) ;
#91603=CARTESIAN_POINT ( 'NONE',  ( 33.13288845015618023, -5.965225279485572685, -0.1650522222209214185 ) ) ;
#91614=CARTESIAN_POINT ( 'NONE',  ( -28.98875734969026041, -5.965225279485572685, 17.86602280011862476 ) ) ;
#91622=ORIENTED_EDGE ( 'NONE', *, *, #73868, .T. ) ;
#91635=ORIENTED_EDGE ( 'NONE', *, *, #56687, .T. ) ;
#91639=CARTESIAN_POINT ( 'NONE',  ( 31.01539214510847486, 4.736880496761964210, -2.146553774717884444 ) ) ;
#91645=ORIENTED_EDGE ( 'NONE', *, *, #12466, .F. ) ;
#91646=DIRECTION ( 'NONE',  ( 0.000000000000000000, 0.000000000000000000, -1.000000000000000000 ) ) ;
#91649=AXIS2_PLACEMENT_3D ( 'NONE', #84669, #23260, #9049 ) ;
#91657=CARTESIAN_POINT ( 'NONE',  ( -25.92875734969025814, 3.316774720514426456, 0.7300228001186309656 ) ) ;
#91687=B_SPLINE_CURVE_WITH_KNOTS ( 'NONE', 3,
 ( #76866, #23080, #46441, #54071, #32205, #763, #7873, #55062, #86000, #86995, #42352, #49458, #65691, #3288, #41333, #88506 ),
 .UNSPECIFIED., .F., .F.,
 ( 4, 2, 2, 2, 2, 2, 2, 4 ),
 ( -2.132270449955935040E-05, 0.0007770955584725032679, 0.001176304689958539498, 0.001575513821444575729, 0.001974722952930611959, 0.002373932084416648623, 0.002773141215902684420, 0.003172350347388721084 ),
 .UNSPECIFIED. ) ;
#91690=FACE_OUTER_BOUND ( 'NONE', #63107, .T. ) ;
#91709=EDGE_CURVE ( 'NONE', #96497, #5853, #93075, .T. ) ;
#91713=EDGE_LOOP ( 'NONE', ( #18892, #81381, #44712, #91037 ) ) ;
#91722=CARTESIAN_POINT ( 'NONE',  ( 29.68479148105951992, 1.682774720514426114, -9.431263391055118461 ) ) ;
#91725=AXIS2_PLACEMENT_3D ( 'NONE', #71710, #64119, #25529 ) ;
#91729=AXIS2_PLACEMENT_3D ( 'NONE', #40796, #77836, #48924 ) ;
#91739=DIRECTION ( 'NONE',  ( 0.000000000000000000, 0.000000000000000000, 1.000000000000000000 ) ) ;
#91749=VECTOR ( 'NONE', #31229, 1000.000000000000000 ) ;
#91763=DIRECTION ( 'NONE',  ( 0.000000000000000000, 0.000000000000000000, 1.000000000000000000 ) ) ;
#91765=FACE_OUTER_BOUND ( 'NONE', #45662, .T. ) ;
#91772=DIRECTION ( 'NONE',  ( 0.000000000000000000, 0.000000000000000000, -1.000000000000000000 ) ) ;
#91787=AXIS2_PLACEMENT_3D ( 'NONE', #15724, #93341, #23324 ) ;
#91791=AXIS2_PLACEMENT_3D ( 'NONE', #31586, #69661, #100071 ) ;
#91792=EDGE_CURVE ( 'NONE', #51194, #11608, #32179, .T. ) ;
#91799=EDGE_CURVE ( 'NONE', #95525, #96621, #70251, .T. ) ;
#91822=CARTESIAN_POINT ( 'NONE',  ( -27.96875734969026084, -6.475225279485573360, 26.43402280011862615 ) ) ;
#91825=AXIS2_PLACEMENT_3D ( 'NONE', #76001, #85624, #22209 ) ;
#91831=AXIS2_PLACEMENT_3D ( 'NONE', #95654, #80927, #34261 ) ;
#91835=CARTESIAN_POINT ( 'NONE',  ( 22.65031661608482594, 1.684774720501991618, -20.71116937900383448 ) ) ;
#91844=TOROIDAL_SURFACE ( 'NONE', #77200, 253.2618649670780826, 1.835999999999999854 ) ;
#91850=VERTEX_POINT ( 'NONE', #42817 ) ;
#91854=ORIENTED_EDGE ( 'NONE', *, *, #62012, .F. ) ;
#91856=CARTESIAN_POINT ( 'NONE',  ( 22.02124265030973760, -6.143225279485574397, 16.20402280011862217 ) ) ;
#91860=VECTOR ( 'NONE', #78750, 1000.000000000000000 ) ;
#91868=DIRECTION ( 'NONE',  ( -1.000000000000000000, 9.637352644315600173E-17, 0.000000000000000000 ) ) ;
#91873=CARTESIAN_POINT ( 'NONE',  ( 26.37445894957760828, -1.477225279485574028, -11.69480419648520986 ) ) ;
#91874=CARTESIAN_POINT ( 'NONE',  ( -29.49875734969025842, 0.3587747205144265483, 25.61802280011862720 ) ) ;
#91875=VERTEX_POINT ( 'NONE', #36191 ) ;
#91876=ORIENTED_EDGE ( 'NONE', *, *, #43413, .F. ) ;
#91928=ORIENTED_EDGE ( 'NONE', *, *, #63421, .T. ) ;
#91960=CARTESIAN_POINT ( 'NONE',  ( -19.38764004357182813, 6.376774720514426953, -21.62823517627351322 ) ) ;
#91967=EDGE_CURVE ( 'NONE', #58907, #95525, #21435, .T. ) ;
#91972=DIRECTION ( 'NONE',  ( -0.000000000000000000, 1.000000000000000000, -0.000000000000000000 ) ) ;
#91984=VERTEX_POINT ( 'NONE', #52917 ) ;
#91994=EDGE_LOOP ( 'NONE', ( #6496, #55875, #76009, #20593 ) ) ;
#92002=DIRECTION ( 'NONE',  ( 0.000000000000000000, 1.000000000000000000, 0.000000000000000000 ) ) ;
#92022=FACE_OUTER_BOUND ( 'NONE', #52151, .T. ) ;
#92027=EDGE_CURVE ( 'NONE', #39863, #96596, #33905, .T. ) ;
#92029=ORIENTED_EDGE ( 'NONE', *, *, #99713, .F. ) ;
#92055=DIRECTION ( 'NONE',  ( -0.000000000000000000, -1.000000000000000000, -0.000000000000000000 ) ) ;
#92060=B_SPLINE_CURVE_WITH_KNOTS ( 'NONE', 3,
 ( #54645, #344, #100278, #14567, #92683, #38908, #6960, #23163, #22664, #53652 ),
 .UNSPECIFIED., .F., .F.,
 ( 4, 2, 2, 2, 4 ),
 ( 0.000000000000000000, 0.0004833345490728424001, 0.0009666690981456848002, 0.001450003647218527092, 0.001933338196291368299 ),
 .UNSPECIFIED. ) ;
#92116=LINE ( 'NONE', #12992, #71135 ) ;
#92122=VERTEX_POINT ( 'NONE', #14826 ) ;
#92134=ORIENTED_EDGE ( 'NONE', *, *, #28249, .F. ) ;
#92137=VECTOR ( 'NONE', #54382, 1000.000000000000227 ) ;
#92139=ORIENTED_EDGE ( 'NONE', *, *, #98444, .T. ) ;
#92154=EDGE_CURVE ( 'NONE', #76855, #44309, #92268, .T. ) ;
#92173=LINE ( 'NONE', #15547, #8457 ) ;
#92175=ORIENTED_EDGE ( 'NONE', *, *, #75366, .F. ) ;
#92190=VERTEX_POINT ( 'NONE', #25454 ) ;
#92209=VECTOR ( 'NONE', #58762, 1000.000000000000114 ) ;
#92210=FACE_OUTER_BOUND ( 'NONE', #82859, .T. ) ;
#92213=ADVANCED_FACE ( 'NONE', ( #24948 ), #8735, .T. ) ;
#92219=ORIENTED_EDGE ( 'NONE', *, *, #50567, .F. ) ;
#92236=DIRECTION ( 'NONE',  ( -1.000000000000000000, -0.000000000000000000, -0.000000000000000000 ) ) ;
#92237=CARTESIAN_POINT ( 'NONE',  ( 15.77421270221668692, 3.602820947333609691, -28.08718493694523133 ) ) ;
#92240=VERTEX_POINT ( 'NONE', #2141 ) ;
#92247=ORIENTED_EDGE ( 'NONE', *, *, #88964, .F. ) ;
#92266=CARTESIAN_POINT ( 'NONE',  ( 11.93051494998403683, 1.682774720514426114, 10.48039711075945490 ) ) ;
#92268=CIRCLE ( 'NONE', #32377, 129.7684398600581517 ) ;
#92277=CARTESIAN_POINT ( 'NONE',  ( 13.12137440454564796, 3.706387542726002682, -28.15098661896695376 ) ) ;
#92278=CARTESIAN_POINT ( 'NONE',  ( 30.53060340732035982, 5.278399900168558645, 6.051577412957072077 ) ) ;
#92279=VECTOR ( 'NONE', #83376, 1000.000000000000000 ) ;
#92288=LINE ( 'NONE', #45626, #28493 ) ;
#92290=CARTESIAN_POINT ( 'NONE',  ( 0.000000000000000000, 2.682774720514426559, 0.000000000000000000 ) ) ;
#92331=CARTESIAN_POINT ( 'NONE',  ( 33.00535138976592719, 3.570691370340881576, -12.97242311383975988 ) ) ;
#92340=ORIENTED_EDGE ( 'NONE', *, *, #90775, .T. ) ;
#92343=DIRECTION ( 'NONE',  ( 0.000000000000000000, 1.000000000000000000, 0.000000000000000000 ) ) ;
#92348=CIRCLE ( 'NONE', #19420, 1.530000000000000249 ) ;
#92370=EDGE_CURVE ( 'NONE', #82958, #28190, #69484, .T. ) ;
#92374=CARTESIAN_POINT ( 'NONE',  ( 32.64853395142472436, 3.736174708400741729, -2.687157883629963884 ) ) ;
#92406=CARTESIAN_POINT ( 'NONE',  ( 9.478389368232452483, 4.132774720514426292, -23.17485683983816003 ) ) ;
#92408=ORIENTED_EDGE ( 'NONE', *, *, #43736, .F. ) ;
#92415=EDGE_CURVE ( 'NONE', #88543, #28216, #53298, .T. ) ;
#92419=CARTESIAN_POINT ( 'NONE',  ( 6.310942340984578180, 6.376774720514426953, -25.29254520177807208 ) ) ;
#92426=DIRECTION ( 'NONE',  ( -0.7512896232465891000, 0.000000000000000000, -0.6599726524652351767 ) ) ;
#92435=VERTEX_POINT ( 'NONE', #45189 ) ;
#92461=ORIENTED_EDGE ( 'NONE', *, *, #41569, .F. ) ;
#92474=ORIENTED_EDGE ( 'NONE', *, *, #21348, .F. ) ;
#92476=DIRECTION ( 'NONE',  ( 1.000000000000000000, 1.232047923278981953E-16, 0.000000000000000000 ) ) ;
#92488=VECTOR ( 'NONE', #31470, 1000.000000000000000 ) ;
#92494=ORIENTED_EDGE ( 'NONE', *, *, #24007, .T. ) ;
#92497=VERTEX_POINT ( 'NONE', #30949 ) ;
#92507=CARTESIAN_POINT ( 'NONE',  ( 25.50613189835290484, 5.179663042751369240, -8.021752483163538727 ) ) ;
#92524=ORIENTED_EDGE ( 'NONE', *, *, #98007, .T. ) ;
#92534=DIRECTION ( 'NONE',  ( 0.000000000000000000, -0.000000000000000000, -1.000000000000000000 ) ) ;
#92539=DIRECTION ( 'NONE',  ( -0.000000000000000000, -1.000000000000000000, -0.000000000000000000 ) ) ;
#92558=VECTOR ( 'NONE', #17294, 1000.000000000000000 ) ;
#92571=ORIENTED_EDGE ( 'NONE', *, *, #92652, .T. ) ;
#92590=DIRECTION ( 'NONE',  ( 0.000000000000000000, 0.000000000000000000, -1.000000000000000000 ) ) ;
#92602=DIRECTION ( 'NONE',  ( 0.000000000000000000, 0.000000000000000000, -1.000000000000000000 ) ) ;
#92603=CARTESIAN_POINT ( 'NONE',  ( 5.271800844963591359, 3.316774720514426456, -28.56638892015329745 ) ) ;
#92635=ORIENTED_EDGE ( 'NONE', *, *, #44571, .T. ) ;
#92641=PLANE ( 'NONE',  #26263 ) ;
#92647=PLANE ( 'NONE',  #98429 ) ;
#92652=EDGE_CURVE ( 'NONE', #14697, #45943, #66306, .T. ) ;
#92660=FACE_OUTER_BOUND ( 'NONE', #56980, .T. ) ;
#92671=EDGE_LOOP ( 'NONE', ( #34467, #57272, #28743, #94854 ) ) ;
#92675=DIRECTION ( 'NONE',  ( -0.000000000000000000, -0.000000000000000000, -1.000000000000000000 ) ) ;
#92681=DIRECTION ( 'NONE',  ( 4.218136541796977197E-15, -1.000000000000000000, 1.324960360541890271E-16 ) ) ;
#92683=CARTESIAN_POINT ( 'NONE',  ( 30.60443771307607008, 4.296120514312956828, 26.89827953497908908 ) ) ;
#92690=DIRECTION ( 'NONE',  ( 0.000000000000000000, -0.000000000000000000, -1.000000000000000000 ) ) ;
#92692=CARTESIAN_POINT ( 'NONE',  ( 31.81388842165050335, 4.825737335974109143, -4.598239840489335428 ) ) ;
#92731=EDGE_CURVE ( 'NONE', #45676, #99683, #3901, .T. ) ;
#92733=EDGE_CURVE ( 'NONE', #54952, #58907, #89095, .T. ) ;
#92738=VECTOR ( 'NONE', #6298, 1000.000000000000000 ) ;
#92745=EDGE_CURVE ( 'NONE', #44101, #55067, #74459, .T. ) ;
#92782=LINE ( 'NONE', #46128, #44887 ) ;
#92787=ADVANCED_FACE ( 'NONE', ( #59682 ), #90614, .F. ) ;
#92788=DIRECTION ( 'NONE',  ( -0.7689940216596069522, 5.365801633547210331E-16, 0.6392559695863496705 ) ) ;
#92791=AXIS2_PLACEMENT_3D ( 'NONE', #33361, #26758, #48106 ) ;
#92792=DIRECTION ( 'NONE',  ( -0.9994733861282923959, -0.000000000000000000, -0.03244919754393515293 ) ) ;
#92795=EDGE_CURVE ( 'NONE', #69074, #57808, #38813, .T. ) ;
#92804=ORIENTED_EDGE ( 'NONE', *, *, #99188, .T. ) ;
#92827=CARTESIAN_POINT ( 'NONE',  ( 11.23292546672365155, 2.682774720514426559, -27.03842650381641377 ) ) ;
#92830=LINE ( 'NONE', #22807, #70507 ) ;
#92831=PLANE ( 'NONE',  #51740 ) ;
#92841=VECTOR ( 'NONE', #14299, 1000.000000000000000 ) ;
#92857=VERTEX_POINT ( 'NONE', #85486 ) ;
#92871=FACE_OUTER_BOUND ( 'NONE', #23226, .T. ) ;
#92891=DIRECTION ( 'NONE',  ( 0.000000000000000000, 0.000000000000000000, -1.000000000000000000 ) ) ;
#92897=FACE_OUTER_BOUND ( 'NONE', #18242, .T. ) ;
#92915=CARTESIAN_POINT ( 'NONE',  ( 5.548031177074126852, 6.376774720514426953, -25.42222224686167920 ) ) ;
#92918=AXIS2_PLACEMENT_3D ( 'NONE', #27657, #50998, #2827 ) ;
#92920=ORIENTED_EDGE ( 'NONE', *, *, #22365, .T. ) ;
#92921=CARTESIAN_POINT ( 'NONE',  ( -29.49875734969025842, -5.965225279485572685, 17.86602280011862476 ) ) ;
#92926=DIRECTION ( 'NONE',  ( 0.000000000000000000, 0.000000000000000000, 1.000000000000000000 ) ) ;
#92927=CIRCLE ( 'NONE', #49219, 2.249999999999998668 ) ;
#92934=EDGE_CURVE ( 'NONE', #78991, #23706, #80384, .T. ) ;
#92947=CARTESIAN_POINT ( 'NONE',  ( 29.58897068672300179, 4.307329379639823763, 29.06043472499518643 ) ) ;
#92961=CARTESIAN_POINT ( 'NONE',  ( 26.73860345374794534, 1.682774720514426114, 3.440769881205035638E-15 ) ) ;
#92967=EDGE_LOOP ( 'NONE', ( #73151, #32282, #10205, #46980, #31950, #57862, #97369, #36352 ) ) ;
#92976=CARTESIAN_POINT ( 'NONE',  ( -11.64875734969026233, 0.3587747205144265483, 31.02402280011862246 ) ) ;
#92979=EDGE_CURVE ( 'NONE', #52696, #24841, #78366, .T. ) ;
#92988=DIRECTION ( 'NONE',  ( 0.000000000000000000, -1.000000000000000000, 0.000000000000000000 ) ) ;
#93004=CARTESIAN_POINT ( 'NONE',  ( 14.76093561896379214, 3.316774720514426456, -26.55548769130089681 ) ) ;
#93008=VERTEX_POINT ( 'NONE', #32198 ) ;
#93010=CARTESIAN_POINT ( 'NONE',  ( 282.9764569301858046, 2.682774720514426559, 20.79159422840526616 ) ) ;
#93035=CARTESIAN_POINT ( 'NONE',  ( 22.02124265030973760, 3.456774720514426136, 17.35402280011862786 ) ) ;
#93052=EDGE_CURVE ( 'NONE', #36444, #97749, #9363, .T. ) ;
#93069=CARTESIAN_POINT ( 'NONE',  ( 30.43908124610613086, 2.682774720514426559, -13.86910542224436682 ) ) ;
#93075=LINE ( 'NONE', #30179, #9633 ) ;
#93081=ORIENTED_EDGE ( 'NONE', *, *, #20547, .T. ) ;
#93085=EDGE_CURVE ( 'NONE', #23597, #57023, #45421, .T. ) ;
#93087=LINE ( 'NONE', #747, #26969 ) ;
#93094=ORIENTED_EDGE ( 'NONE', *, *, #84953, .F. ) ;
#93102=LINE ( 'NONE', #85491, #55904 ) ;
#93107=CARTESIAN_POINT ( 'NONE',  ( 14.43441819135929727, -5.965225279485572685, -28.36222020317710246 ) ) ;
#93110=EDGE_CURVE ( 'NONE', #46485, #85772, #4264, .T. ) ;
#93117=DIRECTION ( 'NONE',  ( 4.218136541796977197E-15, -1.000000000000000000, 1.324960360541890271E-16 ) ) ;
#93119=ORIENTED_EDGE ( 'NONE', *, *, #89994, .T. ) ;
#93132=CARTESIAN_POINT ( 'NONE',  ( 32.98733314340959311, -5.965225279485572685, 2.074222136288530027 ) ) ;
#93139=ORIENTED_EDGE ( 'NONE', *, *, #45420, .F. ) ;
#93144=DIRECTION ( 'NONE',  ( 1.000000000000000000, 0.000000000000000000, 1.286817348990133408E-16 ) ) ;
#93154=DIRECTION ( 'NONE',  ( 0.000000000000000000, 0.000000000000000000, -1.000000000000000000 ) ) ;
#93172=VECTOR ( 'NONE', #31205, 1000.000000000000000 ) ;
#93186=CARTESIAN_POINT ( 'NONE',  ( -29.49875734969025842, -5.965225279485572685, 17.86602280011862476 ) ) ;
#93204=AXIS2_PLACEMENT_3D ( 'NONE', #94944, #96946, #50282 ) ;
#93206=EDGE_LOOP ( 'NONE', ( #55052, #57800 ) ) ;
#93228=EDGE_CURVE ( 'NONE', #43106, #4626, #42345, .T. ) ;
#93253=VECTOR ( 'NONE', #57223, 1000.000000000000000 ) ;
#93261=DIRECTION ( 'NONE',  ( 0.000000000000000000, 1.000000000000000000, -0.000000000000000000 ) ) ;
#93299=ADVANCED_FACE ( 'NONE', ( #84864 ), #69142, .T. ) ;
#93301=ORIENTED_EDGE ( 'NONE', *, *, #32926, .F. ) ;
#93302=EDGE_CURVE ( 'NONE', #99675, #75250, #21454, .T. ) ;
#93312=VECTOR ( 'NONE', #35625, 1000.000000000000000 ) ;
#93321=AXIS2_PLACEMENT_3D ( 'NONE', #55666, #9469, #48554 ) ;
#93331=DIRECTION ( 'NONE',  ( 0.000000000000000000, 0.000000000000000000, 1.000000000000000000 ) ) ;
#93341=DIRECTION ( 'NONE',  ( -0.000000000000000000, 1.000000000000000000, -0.000000000000000000 ) ) ;
#93358=CARTESIAN_POINT ( 'NONE',  ( 21.97688922017995239, 1.682774720514426114, -18.55878510778117985 ) ) ;
#93405=CARTESIAN_POINT ( 'NONE',  ( -0.02075734969026423599, -5.965225279485572685, -0.08597719988137648983 ) ) ;
#93407=CARTESIAN_POINT ( 'NONE',  ( -23.31187512739357359, -5.965225279485572685, -17.31005501743528185 ) ) ;
#93409=CARTESIAN_POINT ( 'NONE',  ( -29.49875734969026198, 0.3587747205144265483, 2.362022800118626531 ) ) ;
#93416=EDGE_CURVE ( 'NONE', #9293, #75450, #74529, .T. ) ;
#93417=CARTESIAN_POINT ( 'NONE',  ( 5.271800844967073907, 3.316774720514426456, -28.56638892015272191 ) ) ;
#93418=EDGE_CURVE ( 'NONE', #27652, #5624, #99081, .T. ) ;
#93421=VERTEX_POINT ( 'NONE', #45322 ) ;
#93424=LINE ( 'NONE', #94432, #71789 ) ;
#93427=DIRECTION ( 'NONE',  ( 0.1489078231574183508, -6.454799914155188842E-16, -0.9888510809027409865 ) ) ;
#93444=VECTOR ( 'NONE', #37214, 1000.000000000000000 ) ;
#93445=ORIENTED_EDGE ( 'NONE', *, *, #67709, .T. ) ;
#93461=CARTESIAN_POINT ( 'NONE',  ( -27.86046284349297864, 6.376774720514426953, -8.091963836038765123 ) ) ;
#93466=ORIENTED_EDGE ( 'NONE', *, *, #73670, .T. ) ;
#93476=DIRECTION ( 'NONE',  ( 0.000000000000000000, -0.000000000000000000, -1.000000000000000000 ) ) ;
#93487=CARTESIAN_POINT ( 'NONE',  ( 31.04236049493789906, -5.965225279485572685, 19.84760796525321780 ) ) ;
#93497=CARTESIAN_POINT ( 'NONE',  ( 0.000000000000000000, -1.473225279485573802, 0.000000000000000000 ) ) ;
#93531=ORIENTED_EDGE ( 'NONE', *, *, #30131, .F. ) ;
#93541=CARTESIAN_POINT ( 'NONE',  ( -24.90875734969025501, -5.965225279485572685, 26.43402280011862615 ) ) ;
#93612=ORIENTED_EDGE ( 'NONE', *, *, #63457, .F. ) ;
#93645=EDGE_LOOP ( 'NONE', ( #78001, #60864, #42885, #87453 ) ) ;
#93649=CARTESIAN_POINT ( 'NONE',  ( 13.91401389203221406, -5.965225279485572685, 158.0376437107427137 ) ) ;
#93654=LINE ( 'NONE', #77920, #66907 ) ;
#93664=EDGE_CURVE ( 'NONE', #71246, #30854, #95605, .T. ) ;
#93672=CYLINDRICAL_SURFACE ( 'NONE', #65206, 28.45799999999999486 ) ;
#93746=ORIENTED_EDGE ( 'NONE', *, *, #40918, .F. ) ;
#93747=ORIENTED_EDGE ( 'NONE', *, *, #16061, .F. ) ;
#93752=CARTESIAN_POINT ( 'NONE',  ( 22.81105451610979173, -6.475225279485573360, -18.46691820600746681 ) ) ;
#93757=EDGE_CURVE ( 'NONE', #50276, #95120, #34596, .T. ) ;
#93762=VERTEX_POINT ( 'NONE', #58928 ) ;
#93763=VECTOR ( 'NONE', #23933, 1000.000000000000000 ) ;
#93767=FACE_OUTER_BOUND ( 'NONE', #61909, .T. ) ;
#93792=EDGE_CURVE ( 'NONE', #95598, #30477, #59985, .T. ) ;
#93803=CARTESIAN_POINT ( 'NONE',  ( 29.73860345376319003, 5.356471260711259674, 19.84760796525321780 ) ) ;
#93808=CIRCLE ( 'NONE', #4723, 91.74549126261079834 ) ;
#93817=LINE ( 'NONE', #46657, #50868 ) ;
#93820=CARTESIAN_POINT ( 'NONE',  ( 32.84232313084928023, 4.840274619472680229, -11.71291885348849782 ) ) ;
#93830=DIRECTION ( 'NONE',  ( 0.000000000000000000, 0.000000000000000000, -1.000000000000000000 ) ) ;
#93839=AXIS2_PLACEMENT_3D ( 'NONE', #2852, #34293, #3358 ) ;
#93850=DIRECTION ( 'NONE',  ( 0.000000000000000000, 0.000000000000000000, -1.000000000000000000 ) ) ;
#93867=PLANE ( 'NONE',  #53625 ) ;
#93874=AXIS2_PLACEMENT_3D ( 'NONE', #25484, #63573, #3663 ) ;
#93881=ORIENTED_EDGE ( 'NONE', *, *, #14770, .F. ) ;
#93882=VECTOR ( 'NONE', #66546, 1000.000000000000000 ) ;
#93891=CARTESIAN_POINT ( 'NONE',  ( -20.27875734969026311, 3.456774720514426136, 24.00402280011862288 ) ) ;
#93900=CARTESIAN_POINT ( 'NONE',  ( 11.62916340711181284, -5.965225279485572685, 28.75961759920349792 ) ) ;
#93901=CARTESIAN_POINT ( 'NONE',  ( -25.92875734969025814, 3.316774720514426456, 24.50402280011861933 ) ) ;
#93906=LINE ( 'NONE', #86795, #81583 ) ;
#93924=CARTESIAN_POINT ( 'NONE',  ( 6.055070915967790235, 6.376774720520797857, -28.43998667026512095 ) ) ;
#93925=VECTOR ( 'NONE', #64661, 1000.000000000000227 ) ;
#93942=AXIS2_PLACEMENT_3D ( 'NONE', #52429, #61547, #22938 ) ;
#93955=CARTESIAN_POINT ( 'NONE',  ( 31.63608487984670958, 3.398012287350409277, 27.34773272911736797 ) ) ;
#93971=ORIENTED_EDGE ( 'NONE', *, *, #20660, .T. ) ;
#93980=ORIENTED_EDGE ( 'NONE', *, *, #28693, .F. ) ;
#94008=ORIENTED_EDGE ( 'NONE', *, *, #74793, .T. ) ;
#94013=AXIS2_PLACEMENT_3D ( 'NONE', #18822, #87847, #80736 ) ;
#94022=CARTESIAN_POINT ( 'NONE',  ( 0.000000000000000000, -16.94322527948557422, 3.500000000000000000 ) ) ;
#94039=DIRECTION ( 'NONE',  ( 0.000000000000000000, -1.000000000000000000, 0.000000000000000000 ) ) ;
#94044=CARTESIAN_POINT ( 'NONE',  ( -20.77875734969026311, 5.356774720514425603, 0.7300228001186309656 ) ) ;
#94050=CARTESIAN_POINT ( 'NONE',  ( 26.25551457520356635, 4.772774720514425972, -10.59759736550661913 ) ) ;
#94096=ORIENTED_EDGE ( 'NONE', *, *, #43165, .F. ) ;
#94097=EDGE_CURVE ( 'NONE', #48435, #18484, #90813, .T. ) ;
#94103=DIRECTION ( 'NONE',  ( -0.000000000000000000, 1.000000000000000000, -0.000000000000000000 ) ) ;
#94111=CARTESIAN_POINT ( 'NONE',  ( -24.90875734969025501, -6.475225279485573360, 30.00402280011862288 ) ) ;
#94128=CYLINDRICAL_SURFACE ( 'NONE', #62700, 3.349999999999998757 ) ;
#94138=ORIENTED_EDGE ( 'NONE', *, *, #24897, .T. ) ;
#94139=DIRECTION ( 'NONE',  ( 0.000000000000000000, 0.000000000000000000, -1.000000000000000000 ) ) ;
#94147=ORIENTED_EDGE ( 'NONE', *, *, #30454, .F. ) ;
#94148=VERTEX_POINT ( 'NONE', #52258 ) ;
#94152=CARTESIAN_POINT ( 'NONE',  ( 3.180076745125953508, 0.3587747205143968499, -28.87659520466658236 ) ) ;
#94153=CARTESIAN_POINT ( 'NONE',  ( 12.40597316965629560, 5.152774720514427642, -26.28458722401733993 ) ) ;
#94174=CARTESIAN_POINT ( 'NONE',  ( 32.06540688909005610, -6.475225279485576024, -12.44045471929206137 ) ) ;
#94177=LINE ( 'NONE', #78949, #31814 ) ;
#94193=PLANE ( 'NONE',  #40221 ) ;
#94197=EDGE_CURVE ( 'NONE', #60950, #93421, #63388, .T. ) ;
#94211=CARTESIAN_POINT ( 'NONE',  ( 32.76434349455507089, 3.489637856041424957, -3.883594654058048157 ) ) ;
#94215=VERTEX_POINT ( 'NONE', #70985 ) ;
#94224=ADVANCED_FACE ( 'NONE', ( #84690 ), #55769, .F. ) ;
#94230=CARTESIAN_POINT ( 'NONE',  ( 282.9764569301858046, -5.965225279485572685, 20.79159422840526616 ) ) ;
#94250=EDGE_LOOP ( 'NONE', ( #42669, #63410, #93466, #3892 ) ) ;
#94261=ORIENTED_EDGE ( 'NONE', *, *, #51520, .F. ) ;
#94266=ORIENTED_EDGE ( 'NONE', *, *, #36138, .F. ) ;
#94268=CARTESIAN_POINT ( 'NONE',  ( 19.75748517575715368, -5.965225279485572685, 28.87153971905864580 ) ) ;
#94271=CARTESIAN_POINT ( 'NONE',  ( -29.49875734969025842, 0.3587747205144262708, 23.37402280011862743 ) ) ;
#94291=CARTESIAN_POINT ( 'NONE',  ( 14.85834502026402681, 2.682774720514426559, -27.37203305628894867 ) ) ;
#94302=CARTESIAN_POINT ( 'NONE',  ( -53.01255352321339842, 2.682774720514426559, 35.59556822165056644 ) ) ;
#94315=CARTESIAN_POINT ( 'NONE',  ( 33.13630134430571417, 3.554473796596999691, -12.85738972836020899 ) ) ;
#94317=CARTESIAN_POINT ( 'NONE',  ( -29.49875734969026198, -5.965225279485572685, 2.362022800118626531 ) ) ;
#94335=VECTOR ( 'NONE', #9913, 1000.000000000000000 ) ;
#94336=PLANE ( 'NONE',  #84919 ) ;
#94344=CARTESIAN_POINT ( 'NONE',  ( -29.49875734969026198, -5.965225279485572685, 7.870022800118625206 ) ) ;
#94348=CARTESIAN_POINT ( 'NONE',  ( 0.000000000000000000, 1.682774720514426114, -1.352392034746782823 ) ) ;
#94355=ORIENTED_EDGE ( 'NONE', *, *, #83909, .F. ) ;
#94357=VECTOR ( 'NONE', #10584, 1000.000000000000000 ) ;
#94372=LINE ( 'NONE', #26368, #48341 ) ;
#94409=DIRECTION ( 'NONE',  ( 0.6451914333552788428, 0.000000000000000000, 0.7640209514960704107 ) ) ;
#94413=PLANE ( 'NONE',  #399 ) ;
#94414=ORIENTED_EDGE ( 'NONE', *, *, #60941, .F. ) ;
#94424=CARTESIAN_POINT ( 'NONE',  ( 22.81105451610979173, 2.682774720514426559, -18.46691820600746681 ) ) ;
#94426=VERTEX_POINT ( 'NONE', #98791 ) ;
#94429=CARTESIAN_POINT ( 'NONE',  ( 12.98941176919429097, 3.316774720517114972, -28.15829778459866262 ) ) ;
#94431=CARTESIAN_POINT ( 'NONE',  ( 27.86270917940689174, -5.965225279485572685, 29.02104833056109001 ) ) ;
#94432=CARTESIAN_POINT ( 'NONE',  ( -11.64875734969026233, 0.3587747205144265483, 31.02402280011862246 ) ) ;
#94457=B_SPLINE_CURVE_WITH_KNOTS ( 'NONE', 3,
 ( #97184, #68233, #90071, #52011, #20542, #90563, #83441 ),
 .UNSPECIFIED., .F., .F.,
 ( 4, 1, 1, 1, 4 ),
 ( 0.3452202732246780759, 0.4949101844912719983, 0.6446000957578658097, 0.7942900070244596211, 0.9439799182910535436 ),
 .UNSPECIFIED. ) ;
#94459=ORIENTED_EDGE ( 'NONE', *, *, #23821, .F. ) ;
#94462=DIRECTION ( 'NONE',  ( 0.000000000000000000, -1.000000000000000000, 0.000000000000000000 ) ) ;
#94474=CARTESIAN_POINT ( 'NONE',  ( 22.81105451610979173, 1.684774720501991396, -18.46691820600746681 ) ) ;
#94480=ORIENTED_EDGE ( 'NONE', *, *, #28875, .T. ) ;
#94494=CARTESIAN_POINT ( 'NONE',  ( 29.57907552799943218, 3.518969226524878646, 29.21818156447044501 ) ) ;
#94496=AXIS2_PLACEMENT_3D ( 'NONE', #33543, #64527, #95440 ) ;
#94497=VERTEX_POINT ( 'NONE', #73974 ) ;
#94502=ORIENTED_EDGE ( 'NONE', *, *, #29638, .T. ) ;
#94505=ORIENTED_EDGE ( 'NONE', *, *, #63816, .F. ) ;
#94517=ORIENTED_EDGE ( 'NONE', *, *, #10830, .T. ) ;
#94534=DIRECTION ( 'NONE',  ( 0.000000000000000000, -1.000000000000000000, -0.000000000000000000 ) ) ;
#94579=EDGE_CURVE ( 'NONE', #36345, #51956, #60775, .T. ) ;
#94594=VECTOR ( 'NONE', #12051, 999.9999999999998863 ) ;
#94603=ORIENTED_EDGE ( 'NONE', *, *, #24441, .T. ) ;
#94610=DIRECTION ( 'NONE',  ( 0.000000000000000000, -1.000000000000000000, 0.000000000000000000 ) ) ;
#94626=EDGE_CURVE ( 'NONE', #13237, #12021, #30788, .T. ) ;
#94641=AXIS2_PLACEMENT_3D ( 'NONE', #5486, #36934, #59278 ) ;
#94667=DIRECTION ( 'NONE',  ( -0.7689940216596065081, -4.164321980682960499E-15, 0.6392559695863502256 ) ) ;
#94675=CARTESIAN_POINT ( 'NONE',  ( 5.090559816868301724, 3.309281602496330521, -27.56260619295190040 ) ) ;
#94677=CARTESIAN_POINT ( 'NONE',  ( 29.80070917940689412, -5.965225279485572685, 27.39560796525321607 ) ) ;
#94678=CARTESIAN_POINT ( 'NONE',  ( -20.27875734969026311, -4.543225279485573864, 24.00402280011862288 ) ) ;
#94679=FACE_OUTER_BOUND ( 'NONE', #83562, .T. ) ;
#94700=FACE_OUTER_BOUND ( 'NONE', #10833, .T. ) ;
#94709=DIRECTION ( 'NONE',  ( 0.7512896232465892110, -0.000000000000000000, 0.6599726524652350657 ) ) ;
#94742=VERTEX_POINT ( 'NONE', #15055 ) ;
#94761=ORIENTED_EDGE ( 'NONE', *, *, #17827, .T. ) ;
#94768=ORIENTED_EDGE ( 'NONE', *, *, #15749, .T. ) ;
#94787=LINE ( 'NONE', #48640, #83895 ) ;
#94797=ADVANCED_FACE ( 'NONE', ( #33791 ), #63256, .F. ) ;
#94801=ORIENTED_EDGE ( 'NONE', *, *, #58412, .F. ) ;
#94814=EDGE_CURVE ( 'NONE', #50535, #59834, #94177, .T. ) ;
#94819=CARTESIAN_POINT ( 'NONE',  ( 33.63447098073278596, 3.363532777116247541, -11.63841935007238426 ) ) ;
#94830=VERTEX_POINT ( 'NONE', #86573 ) ;
#94843=ORIENTED_EDGE ( 'NONE', *, *, #56004, .T. ) ;
#94845=DIRECTION ( 'NONE',  ( 0.000000000000000000, -0.000000000000000000, 1.000000000000000000 ) ) ;
#94849=DIRECTION ( 'NONE',  ( -0.000000000000000000, 1.000000000000000000, -0.000000000000000000 ) ) ;
#94852=DIRECTION ( 'NONE',  ( -0.000000000000000000, -0.000000000000000000, -1.000000000000000000 ) ) ;
#94854=ORIENTED_EDGE ( 'NONE', *, *, #55005, .F. ) ;
#94859=EDGE_CURVE ( 'NONE', #39472, #74167, #41535, .T. ) ;
#94882=EDGE_CURVE ( 'NONE', #22347, #96941, #18559, .T. ) ;
#94901=DIRECTION ( 'NONE',  ( 0.000000000000000000, -1.000000000000000000, 0.000000000000000000 ) ) ;
#94904=CARTESIAN_POINT ( 'NONE',  ( -20.27875734969026311, -6.143225279485574397, 24.00402280011862288 ) ) ;
#94935=CARTESIAN_POINT ( 'NONE',  ( 12.48433401490028949, 6.376774720514426953, -25.05541855807676299 ) ) ;
#94936=EDGE_CURVE ( 'NONE', #34838, #92190, #75833, .T. ) ;
#94944=CARTESIAN_POINT ( 'NONE',  ( -24.90875734969025501, -5.965225279485572685, 30.00402280011862288 ) ) ;
#94972=CARTESIAN_POINT ( 'NONE',  ( 13.91401389203221406, -6.475225279485573360, 27.75920385068456042 ) ) ;
#94973=VERTEX_POINT ( 'NONE', #70230 ) ;
#94978=VERTEX_POINT ( 'NONE', #31656 ) ;
#94979=AXIS2_PLACEMENT_3D ( 'NONE', #38378, #83551, #76924 ) ;
#94988=CARTESIAN_POINT ( 'NONE',  ( 32.59332756141815679, 2.682774720514426559, -11.41404606144462086 ) ) ;
#94994=CARTESIAN_POINT ( 'NONE',  ( 29.75874681941402855, 6.376774720514429617, 26.36094095093186596 ) ) ;
#94995=CARTESIAN_POINT ( 'NONE',  ( 32.60294298177596062, -6.475225279485573360, -11.48871326860665043 ) ) ;
#94996=ORIENTED_EDGE ( 'NONE', *, *, #16020, .F. ) ;
#95021=VERTEX_POINT ( 'NONE', #15430 ) ;
#95037=CARTESIAN_POINT ( 'NONE',  ( 16.26279755680689476, -5.965225279485572685, -27.67997040356619110 ) ) ;
#95043=LINE ( 'NONE', #11309, #14748 ) ;
#95059=CIRCLE ( 'NONE', #28643, 2.249999999999998668 ) ;
#95060=AXIS2_PLACEMENT_3D ( 'NONE', #37702, #21960, #93476 ) ;
#95073=DIRECTION ( 'NONE',  ( 0.9685340172660600322, 0.000000000000000000, -0.2488812114211667037 ) ) ;
#95079=ORIENTED_EDGE ( 'NONE', *, *, #71318, .T. ) ;
#95082=ORIENTED_EDGE ( 'NONE', *, *, #28695, .T. ) ;
#95096=CYLINDRICAL_SURFACE ( 'NONE', #87010, 2.500000000000000444 ) ;
#95100=LINE ( 'NONE', #56558, #84086 ) ;
#95116=VECTOR ( 'NONE', #44498, 1000.000000000000000 ) ;
#95120=VERTEX_POINT ( 'NONE', #31158 ) ;
#95122=CARTESIAN_POINT ( 'NONE',  ( 19.75748517575715368, 0.3587747205144265483, 28.87153971905864580 ) ) ;
#95138=CARTESIAN_POINT ( 'NONE',  ( 30.58729439590577570, 4.540774720514427543, 26.14186284044645703 ) ) ;
#95149=DIRECTION ( 'NONE',  ( 0.000000000000000000, 0.000000000000000000, 1.000000000000000000 ) ) ;
#95150=ORIENTED_EDGE ( 'NONE', *, *, #85406, .F. ) ;
#95176=LINE ( 'NONE', #48513, #81433 ) ;
#95180=CARTESIAN_POINT ( 'NONE',  ( 22.02124265030973760, -6.143225279485574397, 16.20402280011862217 ) ) ;
#95194=CARTESIAN_POINT ( 'NONE',  ( 13.10664265030973930, -5.965225279485574461, -28.18129937516157568 ) ) ;
#95196=CARTESIAN_POINT ( 'NONE',  ( 15.97264542221207151, 3.406413700670978262, -27.93485542787877662 ) ) ;
#95201=LINE ( 'NONE', #25684, #96661 ) ;
#95237=CARTESIAN_POINT ( 'NONE',  ( 14.67302116299745052, 4.477500275188335266, -27.99481486150953558 ) ) ;
#95259=EDGE_CURVE ( 'NONE', #60428, #55518, #17692, .T. ) ;
#95268=EDGE_CURVE ( 'NONE', #54952, #5853, #90446, .T. ) ;
#95272=VERTEX_POINT ( 'NONE', #30540 ) ;
#95297=FACE_OUTER_BOUND ( 'NONE', #23700, .T. ) ;
#95307=ORIENTED_EDGE ( 'NONE', *, *, #51044, .F. ) ;
#95308=LINE ( 'NONE', #32411, #8833 ) ;
#95350=VERTEX_POINT ( 'NONE', #78204 ) ;
#95372=CARTESIAN_POINT ( 'NONE',  ( 0.000000000000000000, 4.132774720514426292, 0.000000000000000000 ) ) ;
#95387=EDGE_CURVE ( 'NONE', #21581, #24307, #89216, .T. ) ;
#95409=DIRECTION ( 'NONE',  ( 0.000000000000000000, 0.000000000000000000, -1.000000000000000000 ) ) ;
#95432=DIRECTION ( 'NONE',  ( 0.000000000000000000, 0.000000000000000000, -1.000000000000000000 ) ) ;
#95434=ORIENTED_EDGE ( 'NONE', *, *, #61931, .F. ) ;
#95440=DIRECTION ( 'NONE',  ( 7.726610339123061470E-14, 0.000000000000000000, -1.000000000000000000 ) ) ;
#95452=DIRECTION ( 'NONE',  ( -1.000000000000000000, 0.000000000000000000, -1.226388327005079762E-16 ) ) ;
#95461=VERTEX_POINT ( 'NONE', #44538 ) ;
#95462=CARTESIAN_POINT ( 'NONE',  ( 31.62500054620340251, 6.365374413700245704, 26.93529845007237711 ) ) ;
#95466=VECTOR ( 'NONE', #80658, 1000.000000000000000 ) ;
#95468=EDGE_CURVE ( 'NONE', #50118, #3684, #27809, .T. ) ;
#95474=VECTOR ( 'NONE', #81235, 999.9999999999998863 ) ;
#95490=EDGE_CURVE ( 'NONE', #89124, #71759, #90207, .T. ) ;
#95497=CARTESIAN_POINT ( 'NONE',  ( 29.73860345376319358, 4.772774720514425972, 0.000000000000000000 ) ) ;
#95504=EDGE_CURVE ( 'NONE', #12744, #78991, #76461, .T. ) ;
#95508=EDGE_CURVE ( 'NONE', #86083, #53725, #90708, .T. ) ;
#95516=DIRECTION ( 'NONE',  ( -0.9822594791677485837, 0.000000000000000000, 0.1875268396392987258 ) ) ;
#95517=ORIENTED_EDGE ( 'NONE', *, *, #99852, .T. ) ;
#95525=VERTEX_POINT ( 'NONE', #5469 ) ;
#95531=DIRECTION ( 'NONE',  ( 0.000000000000000000, 0.000000000000000000, -1.000000000000000000 ) ) ;
#95535=ORIENTED_EDGE ( 'NONE', *, *, #52164, .F. ) ;
#95544=CIRCLE ( 'NONE', #51800, 2.040000000000000036 ) ;
#95549=EDGE_LOOP ( 'NONE', ( #226, #94480, #35571, #984, #23456, #44541 ) ) ;
#95569=CARTESIAN_POINT ( 'NONE',  ( 32.98733314340959311, -5.965225279485572685, 2.074222136288530027 ) ) ;
#95593=DIRECTION ( 'NONE',  ( -0.000000000000000000, 1.000000000000000000, -0.000000000000000000 ) ) ;
#95598=VERTEX_POINT ( 'NONE', #100285 ) ;
#95605=CIRCLE ( 'NONE', #51869, 3.349999999999998757 ) ;
#95606=ORIENTED_EDGE ( 'NONE', *, *, #56004, .F. ) ;
#95609=DIRECTION ( 'NONE',  ( -1.000000000000000000, 0.000000000000000000, 0.000000000000000000 ) ) ;
#95614=VECTOR ( 'NONE', #70636, 1000.000000000000114 ) ;
#95624=CARTESIAN_POINT ( 'NONE',  ( 26.25551457520356635, 1.682774720514426114, -10.59759736550661913 ) ) ;
#95630=ORIENTED_EDGE ( 'NONE', *, *, #80364, .T. ) ;
#95631=ORIENTED_EDGE ( 'NONE', *, *, #9502, .T. ) ;
#95653=ORIENTED_EDGE ( 'NONE', *, *, #81141, .T. ) ;
#95654=CARTESIAN_POINT ( 'NONE',  ( 4.712727796232550226, 3.316774720514426456, -25.55789472434992859 ) ) ;
#95678=CARTESIAN_POINT ( 'NONE',  ( 29.70220533433691301, 6.376774720514426953, 28.20564067601639735 ) ) ;
#95693=AXIS2_PLACEMENT_3D ( 'NONE', #91152, #28262, #91646 ) ;
#95711=ADVANCED_FACE ( 'NONE', ( #94700 ), #69223, .F. ) ;
#95720=FACE_OUTER_BOUND ( 'NONE', #98812, .T. ) ;
#95722=CARTESIAN_POINT ( 'NONE',  ( 32.04341656622251122, 4.806217029847265287, -4.198923130344409671 ) ) ;
#95734=VERTEX_POINT ( 'NONE', #22054 ) ;
#95737=CARTESIAN_POINT ( 'NONE',  ( 14.83405752585509596, 4.881907540129173384, -27.54622755360215791 ) ) ;
#95749=VECTOR ( 'NONE', #62066, 1000.000000000000000 ) ;
#95757=DIRECTION ( 'NONE',  ( 0.000000000000000000, -0.000000000000000000, 1.000000000000000000 ) ) ;
#95772=ADVANCED_FACE ( 'NONE', ( #5848 ), #73866, .F. ) ;
#95775=ORIENTED_EDGE ( 'NONE', *, *, #56915, .T. ) ;
#95792=DIRECTION ( 'NONE',  ( 0.1489078231574191002, -6.845827386180410961E-16, -0.9888510809027407644 ) ) ;
#95808=DIRECTION ( 'NONE',  ( -0.000000000000000000, 1.000000000000000000, -0.000000000000000000 ) ) ;
#95809=VERTEX_POINT ( 'NONE', #68253 ) ;
#95813=DIRECTION ( 'NONE',  ( 1.000000000000000000, -0.000000000000000000, -0.000000000000000000 ) ) ;
#95814=VECTOR ( 'NONE', #52608, 1000.000000000000114 ) ;
#95818=FACE_OUTER_BOUND ( 'NONE', #19569, .T. ) ;
#95856=PLANE ( 'NONE',  #39940 ) ;
#95886=ORIENTED_EDGE ( 'NONE', *, *, #2278, .F. ) ;
#95890=DIRECTION ( 'NONE',  ( 0.000000000000000000, -1.000000000000000000, 0.000000000000000000 ) ) ;
#95894=DIRECTION ( 'NONE',  ( -0.000000000000000000, -1.000000000000000000, 0.000000000000000000 ) ) ;
#95916=CARTESIAN_POINT ( 'NONE',  ( -23.59123376470063960, -6.143225279485574397, 23.50402280011862288 ) ) ;
#95918=CARTESIAN_POINT ( 'NONE',  ( 5.271800844963591359, 3.316774720514426456, -28.56638892015329745 ) ) ;
#95925=CARTESIAN_POINT ( 'NONE',  ( 9.948453975742596711, -5.965225279485574461, -28.04422933552663366 ) ) ;
#95927=CARTESIAN_POINT ( 'NONE',  ( 31.79364159983995464, 2.682774720514426559, -11.59305536555894278 ) ) ;
#95941=PLANE ( 'NONE',  #62260 ) ;
#95947=CYLINDRICAL_SURFACE ( 'NONE', #28859, 130.2784398600581710 ) ;
#95951=ADVANCED_FACE ( 'NONE', ( #7331 ), #76831, .F. ) ;
#95960=CARTESIAN_POINT ( 'NONE',  ( -0.02075734969026423599, 0.3587747205144213303, -0.08597719988137648983 ) ) ;
#95962=ORIENTED_EDGE ( 'NONE', *, *, #11523, .F. ) ;
#95964=EDGE_LOOP ( 'NONE', ( #19214, #24600, #14204, #65601 ) ) ;
#95966=CARTESIAN_POINT ( 'NONE',  ( 31.61046577166746374, 4.540774708561928108, 26.28065669267635585 ) ) ;
#95979=ORIENTED_EDGE ( 'NONE', *, *, #83651, .T. ) ;
#95984=ORIENTED_EDGE ( 'NONE', *, *, #95268, .F. ) ;
#96000=ORIENTED_EDGE ( 'NONE', *, *, #68012, .T. ) ;
#96011=ORIENTED_EDGE ( 'NONE', *, *, #53172, .F. ) ;
#96029=CARTESIAN_POINT ( 'NONE',  ( 10.46399479596396453, 2.682774720514426559, -27.03001098546561920 ) ) ;
#96032=CARTESIAN_POINT ( 'NONE',  ( 29.73860345376319358, 4.772803916115708311, -4.021109907510727943 ) ) ;
#96040=DIRECTION ( 'NONE',  ( 0.000000000000000000, -1.084202172485504434E-16, -1.000000000000000000 ) ) ;
#96051=PRODUCT_DEFINITION_FORMATION_WITH_SPECIFIED_SOURCE ( 'ANY', '', #5326, .NOT_KNOWN. ) ;
#96054=DIRECTION ( 'NONE',  ( 0.000000000000000000, 0.000000000000000000, -1.000000000000000000 ) ) ;
#96056=CIRCLE ( 'NONE', #28044, 28.96799999999999287 ) ;
#96083=EDGE_LOOP ( 'NONE', ( #49274, #3807, #97039, #12482 ) ) ;
#96100=AXIS2_PLACEMENT_3D ( 'NONE', #10206, #41163, #72117 ) ;
#96110=CARTESIAN_POINT ( 'NONE',  ( 13.91401389203221406, -5.965225279485572685, 27.75920385068456042 ) ) ;
#96111=EDGE_LOOP ( 'NONE', ( #32953, #42121, #22483, #90141 ) ) ;
#96113=CARTESIAN_POINT ( 'NONE',  ( 0.000000000000000000, 1.826774720514426464, 6.000000000000000888 ) ) ;
#96135=CIRCLE ( 'NONE', #92918, 1.325999999999943446 ) ;
#96149=ORIENTED_EDGE ( 'NONE', *, *, #98707, .T. ) ;
#96157=CARTESIAN_POINT ( 'NONE',  ( 13.91401389203221406, 6.376774720514426953, 158.0376437107427137 ) ) ;
#96168=CARTESIAN_POINT ( 'NONE',  ( 10.22011794244940752, 3.316774720515020203, -27.02313658111319938 ) ) ;
#96172=EDGE_CURVE ( 'NONE', #84636, #82268, #6216, .T. ) ;
#96183=DIRECTION ( 'NONE',  ( -0.1875268396392987258, -0.000000000000000000, -0.9822594791677485837 ) ) ;
#96233=CARTESIAN_POINT ( 'NONE',  ( -29.49875734969026198, -5.965225279485572685, 0.1180228001186258285 ) ) ;
#96250=EDGE_LOOP ( 'NONE', ( #51955, #37637, #96000, #16021 ) ) ;
#96256=ORIENTED_EDGE ( 'NONE', *, *, #23294, .T. ) ;
#96271=FACE_OUTER_BOUND ( 'NONE', #8853, .T. ) ;
#96275=DIRECTION ( 'NONE',  ( -1.000000000000000000, -0.000000000000000000, -0.000000000000000000 ) ) ;
#96279=ADVANCED_FACE ( 'NONE', ( #60530 ), #38157, .T. ) ;
#96292=LINE ( 'NONE', #34392, #77684 ) ;
#96318=CARTESIAN_POINT ( 'NONE',  ( -4.993225604111834137, 0.3587747205143964613, -29.11654937215279304 ) ) ;
#96321=DIRECTION ( 'NONE',  ( 0.000000000000000000, 3.740886741919572836E-15, -1.000000000000000000 ) ) ;
#96327=ORIENTED_EDGE ( 'NONE', *, *, #77944, .T. ) ;
#96336=DIRECTION ( 'NONE',  ( -0.000000000000000000, 0.000000000000000000, 1.000000000000000000 ) ) ;
#96363=ORIENTED_EDGE ( 'NONE', *, *, #62029, .F. ) ;
#96366=VECTOR ( 'NONE', #27452, 1000.000000000000114 ) ;
#96370=CARTESIAN_POINT ( 'NONE',  ( -28.49194798280535323, -5.965225279485572685, 28.38521343323375490 ) ) ;
#96375=VECTOR ( 'NONE', #94610, 1000.000000000000000 ) ;
#96381=CARTESIAN_POINT ( 'NONE',  ( 13.91401389203221406, -5.965225279485572685, 158.0376437107427137 ) ) ;
#96393=DIRECTION ( 'NONE',  ( -0.000000000000000000, -1.000000000000000000, -0.000000000000000000 ) ) ;
#96413=EDGE_CURVE ( 'NONE', #22769, #17742, #11713, .T. ) ;
#96418=B_SPLINE_CURVE_WITH_KNOTS ( 'NONE', 3,
 ( #56374, #86294, #87294, #56872 ),
 .UNSPECIFIED., .F., .F.,
 ( 4, 4 ),
 ( 0.000000000000000000, 0.001749918372064178775 ),
 .UNSPECIFIED. ) ;
#96427=CARTESIAN_POINT ( 'NONE',  ( 10.86264265030973952, -5.965225279485574461, -28.05717073599341305 ) ) ;
#96438=CARTESIAN_POINT ( 'NONE',  ( 12.30588647389939538, 3.316774720514762187, -28.11066263608955751 ) ) ;
#96439=VECTOR ( 'NONE', #68507, 1000.000000000000000 ) ;
#96442=DIRECTION ( 'NONE',  ( -0.000000000000000000, 1.000000000000000000, -0.000000000000000000 ) ) ;
#96444=CARTESIAN_POINT ( 'NONE',  ( 22.02124265030973760, -6.143225279485574397, 19.55402280011862004 ) ) ;
#96448=PLANE ( 'NONE',  #32104 ) ;
#96454=FACE_OUTER_BOUND ( 'NONE', #10488, .T. ) ;
#96456=EDGE_CURVE ( 'NONE', #58907, #27652, #12208, .T. ) ;
#96460=ORIENTED_EDGE ( 'NONE', *, *, #10083, .T. ) ;
#96464=CARTESIAN_POINT ( 'NONE',  ( 29.65417061107837071, 5.752153662292248448, 28.02209566695815823 ) ) ;
#96465=ORIENTED_EDGE ( 'NONE', *, *, #81524, .T. ) ;
#96484=CARTESIAN_POINT ( 'NONE',  ( 33.69795529655567634, 0.6647747205144264315, 20.86760796525322093 ) ) ;
#96497=VERTEX_POINT ( 'NONE', #27948 ) ;
#96509=PLANE ( 'NONE',  #33997 ) ;
#96516=CARTESIAN_POINT ( 'NONE',  ( 31.02038118199824268, 5.152774720514427642, -4.893189986691015569 ) ) ;
#96517=VECTOR ( 'NONE', #63556, 1000.000000000000000 ) ;
#96567=LINE ( 'NONE', #58524, #93925 ) ;
#96596=VERTEX_POINT ( 'NONE', #20817 ) ;
#96600=DIRECTION ( 'NONE',  ( 0.000000000000000000, -1.000000000000000000, 0.000000000000000000 ) ) ;
#96610=CARTESIAN_POINT ( 'NONE',  ( -19.80875734969026425, 0.3587747205144265483, 30.51402280011862089 ) ) ;
#96612=DIRECTION ( 'NONE',  ( 0.000000000000000000, -1.000000000000000000, 0.000000000000000000 ) ) ;
#96619=CARTESIAN_POINT ( 'NONE',  ( -41.32836283488544638, 4.132774720514426292, 39.26872235229541985 ) ) ;
#96621=VERTEX_POINT ( 'NONE', #75110 ) ;
#96622=PLANE ( 'NONE',  #47854 ) ;
#96635=CARTESIAN_POINT ( 'NONE',  ( -65.05438548721848235, 3.316774720514426456, 27.45402280011862572 ) ) ;
#96637=VECTOR ( 'NONE', #66511, 1000.000000000000000 ) ;
#96641=ADVANCED_FACE ( 'NONE', ( #8108 ), #75598, .T. ) ;
#96644=EDGE_CURVE ( 'NONE', #85772, #12600, #33921, .T. ) ;
#96650=VECTOR ( 'NONE', #50082, 1000.000000000000000 ) ;
#96661=VECTOR ( 'NONE', #56655, 1000.000000000000000 ) ;
#96664=CARTESIAN_POINT ( 'NONE',  ( 33.10875634548599322, -6.475225279485573360, -11.42349945801155719 ) ) ;
#96670=CARTESIAN_POINT ( 'NONE',  ( 3.509873074917118085, -5.965225279485572685, 29.15869884040363758 ) ) ;
#96679=CARTESIAN_POINT ( 'NONE',  ( 15.32643653063178668, 2.682774720514426559, -27.14485409495428314 ) ) ;
#96724=EDGE_CURVE ( 'NONE', #9882, #67600, #68017, .T. ) ;
#96729=DIRECTION ( 'NONE',  ( 0.000000000000000000, 0.000000000000000000, -1.000000000000000000 ) ) ;
#96749=DIRECTION ( 'NONE',  ( 0.000000000000000000, 0.000000000000000000, 1.000000000000000000 ) ) ;
#96752=CARTESIAN_POINT ( 'NONE',  ( 13.91401389203221406, 3.316774720514426456, 158.0376437107427137 ) ) ;
#96754=VERTEX_POINT ( 'NONE', #91835 ) ;
#96756=DIRECTION ( 'NONE',  ( 0.3133898629642195011, -5.365801633547218220E-16, -0.9496245541219264785 ) ) ;
#96770=ADVANCED_FACE ( 'NONE', ( #61906 ), #92831, .F. ) ;
#96773=ORIENTED_EDGE ( 'NONE', *, *, #58245, .F. ) ;
#96794=CIRCLE ( 'NONE', #15798, 130.2784398600581710 ) ;
#96802=CARTESIAN_POINT ( 'NONE',  ( 17.47419131657910540, -5.965225279485572685, 28.31804950686278843 ) ) ;
#96811=CARTESIAN_POINT ( 'NONE',  ( 22.81105451610979173, -1.477225279485574028, -18.46691820600746681 ) ) ;
#96817=ORIENTED_EDGE ( 'NONE', *, *, #18978, .F. ) ;
#96819=DIRECTION ( 'NONE',  ( 1.000000000000000000, 0.000000000000000000, 0.000000000000000000 ) ) ;
#96829=CARTESIAN_POINT ( 'NONE',  ( 30.53060340732036337, 5.329285123471892760, 3.289350009555732868 ) ) ;
#96831=CIRCLE ( 'NONE', #27165, 0.8159999999999469900 ) ;
#96833=DIRECTION ( 'NONE',  ( 0.000000000000000000, -1.000000000000000000, 0.000000000000000000 ) ) ;
#96854=AXIS2_PLACEMENT_3D ( 'NONE', #2089, #86801, #77672 ) ;
#96855=LINE ( 'NONE', #80130, #49880 ) ;
#96883=DIRECTION ( 'NONE',  ( -0.000000000000000000, 1.000000000000000000, -0.000000000000000000 ) ) ;
#96892=DIRECTION ( 'NONE',  ( 0.000000000000000000, -0.000000000000000000, -1.000000000000000000 ) ) ;
#96917=DIRECTION ( 'NONE',  ( -0.03244919754393515293, 0.000000000000000000, 0.9994733861282923959 ) ) ;
#96926=CARTESIAN_POINT ( 'NONE',  ( 9.032095062437601740, -5.965225279485574461, -28.07116626896318579 ) ) ;
#96933=DIRECTION ( 'NONE',  ( 3.639962309748244178E-15, -1.000000000000000000, -2.135627652102599075E-15 ) ) ;
#96939=AXIS2_PLACEMENT_3D ( 'NONE', #100286, #39420, #47041 ) ;
#96941=VERTEX_POINT ( 'NONE', #82116 ) ;
#96944=VECTOR ( 'NONE', #52275, 1000.000000000000000 ) ;
#96946=DIRECTION ( 'NONE',  ( 0.000000000000000000, 0.000000000000000000, 1.000000000000000000 ) ) ;
#96948=PLANE ( 'NONE',  #17558 ) ;
#96950=AXIS2_PLACEMENT_3D ( 'NONE', #50279, #81221, #11697 ) ;
#96977=ORIENTED_EDGE ( 'NONE', *, *, #36172, .T. ) ;
#96985=B_SPLINE_CURVE_WITH_KNOTS ( 'NONE', 3,
 ( #85629, #47084, #92237, #14613, #54202, #70412, #46577, #77999, #60812, #45584 ),
 .UNSPECIFIED., .F., .F.,
 ( 4, 2, 2, 2, 4 ),
 ( 0.000000000000000000, 0.0004275315936954019597, 0.0008550631873907993657, 0.001282594781086196772, 0.001710126374781594178 ),
 .UNSPECIFIED. ) ;
#97012=B_SPLINE_CURVE_WITH_KNOTS ( 'NONE', 3,
 ( #41057, #47675, #42066, #10098, #64420, #49185 ),
 .UNSPECIFIED., .F., .F.,
 ( 4, 2, 4 ),
 ( -8.872634692045293004E-06, 0.0009000329399760627434, 0.001808938514644170764 ),
 .UNSPECIFIED. ) ;
#97022=VERTEX_POINT ( 'NONE', #27333 ) ;
#97039=ORIENTED_EDGE ( 'NONE', *, *, #18962, .F. ) ;
#97058=CARTESIAN_POINT ( 'NONE',  ( -6.914873625533457968, 6.376774720514426953, 29.95171384920748281 ) ) ;
#97067=EDGE_CURVE ( 'NONE', #72334, #5126, #45288, .T. ) ;
#97071=DIRECTION ( 'NONE',  ( -0.000000000000000000, 1.000000000000000000, -0.000000000000000000 ) ) ;
#97084=EDGE_CURVE ( 'NONE', #64064, #82023, #35584, .T. ) ;
#97119=DIRECTION ( 'NONE',  ( -0.6599726524652346216, 0.000000000000000000, 0.7512896232465895441 ) ) ;
#97140=CARTESIAN_POINT ( 'NONE',  ( 15.00349588318476712, 3.443263483566387784, -27.42854228801664007 ) ) ;
#97147=EDGE_CURVE ( 'NONE', #10305, #32699, #58340, .T. ) ;
#97155=CARTESIAN_POINT ( 'NONE',  ( 22.81105451610979173, -1.475225279485572916, -17.31691820600746823 ) ) ;
#97165=CARTESIAN_POINT ( 'NONE',  ( 5.109298100551870725, 3.316774720514426456, -27.55941679637892250 ) ) ;
#97166=PLANE ( 'NONE',  #9256 ) ;
#97170=ORIENTED_EDGE ( 'NONE', *, *, #38420, .T. ) ;
#97184=CARTESIAN_POINT ( 'NONE',  ( 5.184553252003285984, -6.475225279485573360, -28.06387035751381731 ) ) ;
#97185=CARTESIAN_POINT ( 'NONE',  ( 11.86515846156731335, 5.152774720514426754, -28.09350142571734921 ) ) ;
#97186=CARTESIAN_POINT ( 'NONE',  ( 14.61581676223891613, 2.682774720514426559, -27.35847991879931485 ) ) ;
#97192=CARTESIAN_POINT ( 'NONE',  ( 31.41423154468143153, 2.682774720514426559, -0.3119954678742140053 ) ) ;
#97194=VECTOR ( 'NONE', #50483, 1000.000000000000000 ) ;
#97199=CARTESIAN_POINT ( 'NONE',  ( 29.71119274252842501, 4.341971045292455145, 27.93347042254709223 ) ) ;
#97200=VECTOR ( 'NONE', #88001, 1000.000000000000000 ) ;
#97204=AXIS2_PLACEMENT_3D ( 'NONE', #96381, #20243, #26872 ) ;
#97207=DIRECTION ( 'NONE',  ( 0.000000000000000000, 1.000000000000000000, 0.000000000000000000 ) ) ;
#97217=VECTOR ( 'NONE', #99043, 1000.000000000000000 ) ;
#97235=CARTESIAN_POINT ( 'NONE',  ( 14.53567905697410367, 3.934666312338140237, -28.27917189340610449 ) ) ;
#97253=ORIENTED_EDGE ( 'NONE', *, *, #21034, .F. ) ;
#97255=DIRECTION ( 'NONE',  ( 1.000000000000000000, 0.000000000000000000, -0.000000000000000000 ) ) ;
#97267=ORIENTED_EDGE ( 'NONE', *, *, #76942, .F. ) ;
#97268=ADVANCED_FACE ( 'NONE', ( #17466 ), #41825, .T. ) ;
#97272=EDGE_CURVE ( 'NONE', #4626, #61654, #55072, .T. ) ;
#97275=ORIENTED_EDGE ( 'NONE', *, *, #28936, .F. ) ;
#97285=DIRECTION ( 'NONE',  ( -0.000000000000000000, -1.000000000000000000, -0.000000000000000000 ) ) ;
#97290=DIRECTION ( 'NONE',  ( 1.000000000000000000, -0.000000000000000000, 0.000000000000000000 ) ) ;
#97305=ORIENTED_EDGE ( 'NONE', *, *, #2634, .T. ) ;
#97314=ORIENTED_EDGE ( 'NONE', *, *, #4601, .T. ) ;
#97335=AXIS2_PLACEMENT_3D ( 'NONE', #81033, #87648, #72927 ) ;
#97369=ORIENTED_EDGE ( 'NONE', *, *, #91023, .F. ) ;
#97371=ORIENTED_EDGE ( 'NONE', *, *, #93085, .F. ) ;
#97397=CARTESIAN_POINT ( 'NONE',  ( 31.63608488009067443, 0.6647747205144267646, 27.34773273846992225 ) ) ;
#97420=ORIENTED_EDGE ( 'NONE', *, *, #8071, .T. ) ;
#97437=LINE ( 'NONE', #35047, #74814 ) ;
#97444=LINE ( 'NONE', #75585, #57605 ) ;
#97455=EDGE_CURVE ( 'NONE', #46180, #5514, #86894, .T. ) ;
#97456=DIRECTION ( 'NONE',  ( 0.000000000000000000, 0.000000000000000000, 1.000000000000000000 ) ) ;
#97472=AXIS2_PLACEMENT_3D ( 'NONE', #53639, #45025, #98280 ) ;
#97474=EDGE_LOOP ( 'NONE', ( #71032, #75267, #36408, #24063, #90117 ) ) ;
#97491=CARTESIAN_POINT ( 'NONE',  ( 22.81105451610979173, -6.475225279485573360, -19.61691820600746539 ) ) ;
#97509=CYLINDRICAL_SURFACE ( 'NONE', #77324, 1.149999999999998135 ) ;
#97512=ORIENTED_EDGE ( 'NONE', *, *, #67221, .T. ) ;
#97525=CARTESIAN_POINT ( 'NONE',  ( -29.49875734969026198, 0.3587747205144265483, 10.11402280011862587 ) ) ;
#97539=DIRECTION ( 'NONE',  ( 0.000000000000000000, -0.000000000000000000, 1.000000000000000000 ) ) ;
#97546=VERTEX_POINT ( 'NONE', #33532 ) ;
#97561=VECTOR ( 'NONE', #46229, 1000.000000000000114 ) ;
#97588=CARTESIAN_POINT ( 'NONE',  ( 6.655121222440027573, 5.350247568484731708, -25.44127467601040138 ) ) ;
#97596=VERTEX_POINT ( 'NONE', #50265 ) ;
#97611=DIRECTION ( 'NONE',  ( -0.000000000000000000, 1.000000000000000000, -0.000000000000000000 ) ) ;
#97617=EDGE_LOOP ( 'NONE', ( #92340, #6083, #56814, #23733 ) ) ;
#97620=ORIENTED_EDGE ( 'NONE', *, *, #7371, .F. ) ;
#97631=CARTESIAN_POINT ( 'NONE',  ( 15.29947331669757737, 3.406413700670902323, -27.16854001216721670 ) ) ;
#97632=DIRECTION ( 'NONE',  ( 0.000000000000000000, 0.000000000000000000, 1.000000000000000000 ) ) ;
#97634=EDGE_LOOP ( 'NONE', ( #17658, #78583, #57384, #14497 ) ) ;
#97644=CARTESIAN_POINT ( 'NONE',  ( 31.44230187582509117, 4.132774720514425404, -3.488634554324459014 ) ) ;
#97650=AXIS2_PLACEMENT_3D ( 'NONE', #921, #68550, #6144 ) ;
#97651=ORIENTED_EDGE ( 'NONE', *, *, #45493, .F. ) ;
#97653=EDGE_CURVE ( 'NONE', #51956, #33854, #92348, .T. ) ;
#97655=DIRECTION ( 'NONE',  ( 1.000000000000000000, 0.000000000000000000, 0.000000000000000000 ) ) ;
#97656=ADVANCED_FACE ( 'NONE', ( #22903 ), #90947, .F. ) ;
#97692=CARTESIAN_POINT ( 'NONE',  ( 31.27821779315964790, 4.116118814799345493, -3.972734673865978117 ) ) ;
#97695=DIRECTION ( 'NONE',  ( -0.000000000000000000, -1.000000000000000000, -0.000000000000000000 ) ) ;
#97697=EDGE_CURVE ( 'NONE', #73137, #3035, #60020, .T. ) ;
#97701=ORIENTED_EDGE ( 'NONE', *, *, #88964, .T. ) ;
#97712=ORIENTED_EDGE ( 'NONE', *, *, #78044, .T. ) ;
#97725=VECTOR ( 'NONE', #91739, 1000.000000000000000 ) ;
#97726=ORIENTED_EDGE ( 'NONE', *, *, #74006, .T. ) ;
#97749=VERTEX_POINT ( 'NONE', #55401 ) ;
#97768=CYLINDRICAL_SURFACE ( 'NONE', #1682, 3.060000000000000053 ) ;
#97770=DIRECTION ( 'NONE',  ( 0.1489078231574191002, -6.845827386180410961E-16, -0.9888510809027407644 ) ) ;
#97787=DIRECTION ( 'NONE',  ( -0.000000000000000000, -1.000000000000000000, -0.000000000000000000 ) ) ;
#97817=CARTESIAN_POINT ( 'NONE',  ( 26.73860345374794534, -1.477225279485574028, -7.113848178280766099 ) ) ;
#97822=DIRECTION ( 'NONE',  ( -0.000000000000000000, -0.000000000000000000, 1.000000000000000000 ) ) ;
#97836=ORIENTED_EDGE ( 'NONE', *, *, #92370, .T. ) ;
#97844=CARTESIAN_POINT ( 'NONE',  ( 29.73860345376319358, 1.682774720514426114, -1.352392034746782823 ) ) ;
#97857=VERTEX_POINT ( 'NONE', #58407 ) ;
#97877=CARTESIAN_POINT ( 'NONE',  ( -0.02075734969026423599, 6.376774720514426953, -0.08597719988137648983 ) ) ;
#97878=CARTESIAN_POINT ( 'NONE',  ( 8.205893897551582938, 3.316774720514426456, -27.11136772256261196 ) ) ;
#97888=AXIS2_PLACEMENT_3D ( 'NONE', #11365, #57060, #42338 ) ;
#97904=VERTEX_POINT ( 'NONE', #10218 ) ;
#97952=ORIENTED_EDGE ( 'NONE', *, *, #74861, .F. ) ;
#97981=CIRCLE ( 'NONE', #54271, 129.7684398600581517 ) ;
#98002=PLANE ( 'NONE',  #65941 ) ;
#98007=EDGE_CURVE ( 'NONE', #39472, #70078, #29125, .T. ) ;
#98012=ORIENTED_EDGE ( 'NONE', *, *, #10133, .F. ) ;
#98017=ADVANCED_FACE ( 'NONE', ( #74604 ), #82220, .F. ) ;
#98021=VECTOR ( 'NONE', #85480, 1000.000000000000000 ) ;
#98028=CARTESIAN_POINT ( 'NONE',  ( 10.46399479596578175, 3.400839389856524342, -27.03001098546515735 ) ) ;
#98053=CARTESIAN_POINT ( 'NONE',  ( 14.76093561896379214, -5.965225279485572685, -27.88148769130088667 ) ) ;
#98061=CARTESIAN_POINT ( 'NONE',  ( 14.83405752585509596, 4.881907540129173384, -27.54622755360215791 ) ) ;
#98084=DIRECTION ( 'NONE',  ( 0.000000000000000000, 0.000000000000000000, 1.000000000000000000 ) ) ;
#98094=ADVANCED_FACE ( 'NONE', ( #8099 ), #71010, .F. ) ;
#98100=CARTESIAN_POINT ( 'NONE',  ( -29.49875734969026198, 0.3587747205144262708, 0.1180228001186258285 ) ) ;
#98101=CARTESIAN_POINT ( 'NONE',  ( 31.18725089179298138, 4.540774720514433760, 2.579558749741450718 ) ) ;
#98102=EDGE_CURVE ( 'NONE', #43485, #43478, #15207, .T. ) ;
#98111=CARTESIAN_POINT ( 'NONE',  ( -0.02075734969026423599, -5.965225279485572685, -0.08597719988137648983 ) ) ;
#98125=ORIENTED_EDGE ( 'NONE', *, *, #65166, .F. ) ;
#98141=CARTESIAN_POINT ( 'NONE',  ( 7.227401621296005274, 3.316774720515020203, -27.22638491047315767 ) ) ;
#98166=DIRECTION ( 'NONE',  ( 0.000000000000000000, 0.000000000000000000, -1.000000000000000000 ) ) ;
#98184=ORIENTED_EDGE ( 'NONE', *, *, #83019, .T. ) ;
#98204=LINE ( 'NONE', #96233, #11928 ) ;
#98214=LINE ( 'NONE', #59178, #82789 ) ;
#98231=ORIENTED_EDGE ( 'NONE', *, *, #3842, .T. ) ;
#98237=TOROIDAL_SURFACE ( 'NONE', #35092, 1.020000000000000018, 3.060000000000000053 ) ;
#98280=DIRECTION ( 'NONE',  ( 0.000000000000000000, 0.000000000000000000, 1.000000000000000000 ) ) ;
#98294=CARTESIAN_POINT ( 'NONE',  ( 13.03371494964462407, -6.475225279485575136, -27.13839018153349869 ) ) ;
#98302=VECTOR ( 'NONE', #59707, 1000.000000000000000 ) ;
#98320=CARTESIAN_POINT ( 'NONE',  ( 11.13529270535513760, 4.132774720514426292, -26.87372982997969117 ) ) ;
#98328=ORIENTED_EDGE ( 'NONE', *, *, #20317, .T. ) ;
#98368=ORIENTED_EDGE ( 'NONE', *, *, #73817, .T. ) ;
#98392=EDGE_CURVE ( 'NONE', #42618, #67734, #19579, .T. ) ;
#98400=CARTESIAN_POINT ( 'NONE',  ( -23.29179552176162105, 0.3587747205144061202, -17.29637630388739211 ) ) ;
#98405=CARTESIAN_POINT ( 'NONE',  ( 1.408343819019456028E-16, -6.943225279485572443, 1.149999999999999911 ) ) ;
#98421=FACE_OUTER_BOUND ( 'NONE', #79234, .T. ) ;
#98422=DIRECTION ( 'NONE',  ( 0.000000000000000000, 0.000000000000000000, 1.000000000000000000 ) ) ;
#98427=ORIENTED_EDGE ( 'NONE', *, *, #29493, .F. ) ;
#98429=AXIS2_PLACEMENT_3D ( 'NONE', #15524, #93144, #23630 ) ;
#98433=CARTESIAN_POINT ( 'NONE',  ( 22.02124265030973760, -4.543225279485573864, 16.20402280011862217 ) ) ;
#98434=DIRECTION ( 'NONE',  ( 2.910297583984928910E-15, -1.000000000000000000, -3.056206645085457922E-15 ) ) ;
#98444=EDGE_CURVE ( 'NONE', #27962, #37175, #88111, .T. ) ;
#98452=ORIENTED_EDGE ( 'NONE', *, *, #33990, .F. ) ;
#98456=EDGE_CURVE ( 'NONE', #22596, #50681, #17905, .T. ) ;
#98468=EDGE_CURVE ( 'NONE', #94978, #68827, #89105, .T. ) ;
#98476=CARTESIAN_POINT ( 'NONE',  ( 22.02124265030973760, -6.143225279485574397, 12.85402280011862430 ) ) ;
#98478=CARTESIAN_POINT ( 'NONE',  ( -11.64875734969026233, -5.965225279485572685, 30.51402280011862089 ) ) ;
#98509=VECTOR ( 'NONE', #25475, 1000.000000000000000 ) ;
#98511=EDGE_CURVE ( 'NONE', #87661, #62785, #9787, .T. ) ;
#98527=CARTESIAN_POINT ( 'NONE',  ( -27.96875734969026084, 3.316774720514426456, 0.7300228001186309656 ) ) ;
#98535=CARTESIAN_POINT ( 'NONE',  ( -0.02075734969026423599, 6.376774720514426953, -28.03397719988137382 ) ) ;
#98564=DIRECTION ( 'NONE',  ( -0.000000000000000000, 1.000000000000000000, -0.000000000000000000 ) ) ;
#98582=EDGE_CURVE ( 'NONE', #77754, #3492, #98871, .T. ) ;
#98607=ORIENTED_EDGE ( 'NONE', *, *, #1964, .T. ) ;
#98622=VERTEX_POINT ( 'NONE', #85466 ) ;
#98626=VERTEX_POINT ( 'NONE', #38296 ) ;
#98677=CARTESIAN_POINT ( 'NONE',  ( 28.20688450243577705, 5.356774720514425603, -7.073367244511738150 ) ) ;
#98681=FACE_OUTER_BOUND ( 'NONE', #53365, .T. ) ;
#98682=DIRECTION ( 'NONE',  ( 0.000000000000000000, 1.000000000000000000, -0.000000000000000000 ) ) ;
#98683=VECTOR ( 'NONE', #64770, 1000.000000000000000 ) ;
#98687=CARTESIAN_POINT ( 'NONE',  ( 29.76216731806157867, 5.356774720514427379, 26.42665638500616154 ) ) ;
#98691=DIRECTION ( 'NONE',  ( -0.000000000000000000, 1.000000000000000000, -0.000000000000000000 ) ) ;
#98696=EDGE_CURVE ( 'NONE', #97749, #95734, #18960, .T. ) ;
#98697=CARTESIAN_POINT ( 'NONE',  ( -29.49875734969025842, -5.965225279485572685, 15.62202280011862321 ) ) ;
#98707=EDGE_CURVE ( 'NONE', #44563, #82569, #23892, .T. ) ;
#98723=ORIENTED_EDGE ( 'NONE', *, *, #30131, .T. ) ;
#98728=CARTESIAN_POINT ( 'NONE',  ( 3.509873074917118085, 0.3587747205144265483, 29.15869884040363758 ) ) ;
#98731=CARTESIAN_POINT ( 'NONE',  ( 30.93860345374796594, 0.6647747205144264315, 19.84760796525321780 ) ) ;
#98749=ORIENTED_EDGE ( 'NONE', *, *, #45493, .T. ) ;
#98769=DIRECTION ( 'NONE',  ( -0.9994733861282923959, 0.000000000000000000, -0.03244919754393515293 ) ) ;
#98791=CARTESIAN_POINT ( 'NONE',  ( -29.49875734969025842, -5.965225279485572685, 17.86602280011862476 ) ) ;
#98796=CIRCLE ( 'NONE', #38829, 130.2784398600581710 ) ;
#98797=ORIENTED_EDGE ( 'NONE', *, *, #75302, .T. ) ;
#98812=EDGE_LOOP ( 'NONE', ( #82747, #40858, #63500, #54087 ) ) ;
#98857=AXIS2_PLACEMENT_3D ( 'NONE', #44327, #43329, #49955 ) ;
#98861=LINE ( 'NONE', #13123, #977 ) ;
#98868=ORIENTED_EDGE ( 'NONE', *, *, #8595, .T. ) ;
#98870=ORIENTED_EDGE ( 'NONE', *, *, #42845, .T. ) ;
#98871=CIRCLE ( 'NONE', #56822, 129.7684398600581517 ) ;
#98939=DIRECTION ( 'NONE',  ( 0.000000000000000000, 1.000000000000000000, -0.000000000000000000 ) ) ;
#98940=CARTESIAN_POINT ( 'NONE',  ( 22.81105451610979173, -1.475225279485572916, -18.46691820600746681 ) ) ;
#98941=DIRECTION ( 'NONE',  ( -2.327730190238738523E-16, -1.000000000000000000, 8.064610422320909082E-16 ) ) ;
#98946=VERTEX_POINT ( 'NONE', #60038 ) ;
#98977=DIRECTION ( 'NONE',  ( 0.000000000000000000, 0.000000000000000000, 1.000000000000000000 ) ) ;
#98988=ORIENTED_EDGE ( 'NONE', *, *, #26358, .F. ) ;
#99024=LINE ( 'NONE', #4704, #5148 ) ;
#99026=ADVANCED_FACE ( 'NONE', ( #21933 ), #14328, .F. ) ;
#99030=DIRECTION ( 'NONE',  ( -0.9161084732596777025, -4.164321980682960499E-15, 0.4009304992412306978 ) ) ;
#99039=CARTESIAN_POINT ( 'NONE',  ( 29.73860345376319714, 4.772774720514425972, -4.021250162519585558 ) ) ;
#99043=DIRECTION ( 'NONE',  ( -0.000000000000000000, -1.000000000000000000, -0.000000000000000000 ) ) ;
#99051=CARTESIAN_POINT ( 'NONE',  ( 14.76093561896378148, 3.316774720514426456, -26.55548769130088971 ) ) ;
#99081=LINE ( 'NONE', #77235, #90755 ) ;
#99083=DIRECTION ( 'NONE',  ( 1.000000000000000000, 0.000000000000000000, -0.000000000000000000 ) ) ;
#99088=CARTESIAN_POINT ( 'NONE',  ( -23.62875734969026453, -6.143225279485574397, 23.50402280011862288 ) ) ;
#99102=CIRCLE ( 'NONE', #27852, 84.48086791635432746 ) ;
#99116=VERTEX_POINT ( 'NONE', #18230 ) ;
#99118=DIRECTION ( 'NONE',  ( -1.000000000000000000, 0.000000000000000000, 0.000000000000000000 ) ) ;
#99127=CIRCLE ( 'NONE', #16558, 129.7684398600581517 ) ;
#99162=LINE ( 'NONE', #5827, #32791 ) ;
#99186=ORIENTED_EDGE ( 'NONE', *, *, #8611, .T. ) ;
#99188=EDGE_CURVE ( 'NONE', #32699, #77487, #10617, .T. ) ;
#99189=DIRECTION ( 'NONE',  ( 0.000000000000000000, 0.000000000000000000, 1.000000000000000000 ) ) ;
#99195=VECTOR ( 'NONE', #40772, 1000.000000000000114 ) ;
#99199=AXIS2_PLACEMENT_3D ( 'NONE', #53032, #98682, #61645 ) ;
#99204=ORIENTED_EDGE ( 'NONE', *, *, #57848, .T. ) ;
#99206=DIRECTION ( 'NONE',  ( 0.6451914333552788428, 0.000000000000000000, 0.7640209514960704107 ) ) ;
#99219=CARTESIAN_POINT ( 'NONE',  ( -2.449489742783178770, -1.473225279485573358, 2.499999999999999556 ) ) ;
#99222=FACE_OUTER_BOUND ( 'NONE', #83664, .T. ) ;
#99227=DIRECTION ( 'NONE',  ( 1.000000000000000000, 0.000000000000000000, 0.000000000000000000 ) ) ;
#99252=EDGE_CURVE ( 'NONE', #88761, #17738, #29831, .T. ) ;
#99255=VECTOR ( 'NONE', #14275, 1000.000000000000000 ) ;
#99263=VERTEX_POINT ( 'NONE', #91722 ) ;
#99268=DIRECTION ( 'NONE',  ( -0.000000000000000000, -1.000000000000000000, 0.000000000000000000 ) ) ;
#99269=CARTESIAN_POINT ( 'NONE',  ( -15.82668884360736961, -5.965225279485572685, 42.07822029717483758 ) ) ;
#99283=CARTESIAN_POINT ( 'NONE',  ( 14.76093561896379214, 3.316774720514426456, -28.39148769130089889 ) ) ;
#99300=CARTESIAN_POINT ( 'NONE',  ( 5.949073730962466833, -5.965225279485572685, -27.94053387008862188 ) ) ;
#99309=DIRECTION ( 'NONE',  ( -0.000000000000000000, -1.000000000000000000, -0.000000000000000000 ) ) ;
#99312=CARTESIAN_POINT ( 'NONE',  ( 32.80655795465876423, 4.354682733740601108, -4.311478614910781992 ) ) ;
#99318=CARTESIAN_POINT ( 'NONE',  ( 10.86264264036872440, 0.3587747205144257157, -28.05717073575603138 ) ) ;
#99369=ORIENTED_EDGE ( 'NONE', *, *, #9467, .T. ) ;
#99381=CARTESIAN_POINT ( 'NONE',  ( 11.41483471809167405, 3.316774720514427344, -27.05170832580397189 ) ) ;
#99384=CIRCLE ( 'NONE', #41096, 1.836000000000002075 ) ;
#99390=CARTESIAN_POINT ( 'NONE',  ( 12.40597316965629560, 5.152774720514427642, -26.28458722401733993 ) ) ;
#99406=CARTESIAN_POINT ( 'NONE',  ( 12.66784028006542151, 2.682774720514427003, -27.12025593822526304 ) ) ;
#99413=DIRECTION ( 'NONE',  ( -0.000000000000000000, -1.000000000000000000, -0.000000000000000000 ) ) ;
#99421=EDGE_CURVE ( 'NONE', #33854, #35854, #28554, .T. ) ;
#99439=CARTESIAN_POINT ( 'NONE',  ( -28.98875734969026041, -5.965225279485572685, 17.86602280011862476 ) ) ;
#99463=ADVANCED_FACE ( 'NONE', ( #48584 ), #42962, .T. ) ;
#99465=DIRECTION ( 'NONE',  ( -0.000000000000000000, -1.000000000000000000, -0.000000000000000000 ) ) ;
#99472=CARTESIAN_POINT ( 'NONE',  ( 32.98733314340959311, -5.965225279485572685, 2.074222136288530027 ) ) ;
#99483=VERTEX_POINT ( 'NONE', #13483 ) ;
#99498=PLANE ( 'NONE',  #66813 ) ;
#99507=ORIENTED_EDGE ( 'NONE', *, *, #16946, .F. ) ;
#99518=ORIENTED_EDGE ( 'NONE', *, *, #8115, .T. ) ;
#99523=ADVANCED_FACE ( 'NONE', ( #20102 ), #5383, .T. ) ;
#99525=DIRECTION ( 'NONE',  ( 0.000000000000000000, 1.000000000000000000, 0.000000000000000000 ) ) ;
#99531=CARTESIAN_POINT ( 'NONE',  ( 27.53860345374808105, -1.477225279485574028, 19.84760796525321780 ) ) ;
#99539=CARTESIAN_POINT ( 'NONE',  ( 4.712727796232550226, 6.376774720514426953, -25.55789472434992859 ) ) ;
#99540=CARTESIAN_POINT ( 'NONE',  ( -20.27875734969026311, -4.543225279485573864, 21.75402280011862644 ) ) ;
#99549=PLANE ( 'NONE',  #19341 ) ;
#99578=EDGE_CURVE ( 'NONE', #87143, #17038, #98214, .T. ) ;
#99594=EDGE_LOOP ( 'NONE', ( #20106, #71109, #26835, #48225, #32877, #61815, #68660, #68311, #49386, #576, #50909, #70423, #69551, #42840 ) ) ;
#99609=LINE ( 'NONE', #45358, #29121 ) ;
#99611=CARTESIAN_POINT ( 'NONE',  ( -65.05438548721848235, -6.475225279485573360, 0.7300228001186309656 ) ) ;
#99619=LINE ( 'NONE', #30120, #100022 ) ;
#99624=CARTESIAN_POINT ( 'NONE',  ( 22.02124265030973760, -4.543225279485573864, 13.95402280011862395 ) ) ;
#99641=DIRECTION ( 'NONE',  ( 0.000000000000000000, -0.000000000000000000, -1.000000000000000000 ) ) ;
#99675=VERTEX_POINT ( 'NONE', #26604 ) ;
#99683=VERTEX_POINT ( 'NONE', #80386 ) ;
#99697=DIRECTION ( 'NONE',  ( 0.000000000000000000, 0.000000000000000000, -1.000000000000000000 ) ) ;
#99713=EDGE_CURVE ( 'NONE', #66710, #28190, #87664, .T. ) ;
#99715=CARTESIAN_POINT ( 'NONE',  ( 26.73860345374794534, 1.682774720514426114, -1.352392034746782823 ) ) ;
#99719=ORIENTED_EDGE ( 'NONE', *, *, #70155, .T. ) ;
#99720=EDGE_LOOP ( 'NONE', ( #84491, #40366 ) ) ;
#99721=FACE_OUTER_BOUND ( 'NONE', #97617, .T. ) ;
#99730=ADVANCED_FACE ( 'NONE', ( #79376 ), #19474, .F. ) ;
#99746=ORIENTED_EDGE ( 'NONE', *, *, #12661, .F. ) ;
#99757=DIRECTION ( 'NONE',  ( 0.000000000000000000, 0.000000000000000000, -1.000000000000000000 ) ) ;
#99770=FACE_OUTER_BOUND ( 'NONE', #47683, .T. ) ;
#99781=CARTESIAN_POINT ( 'NONE',  ( 13.91401389203221406, -5.965225279485572685, 158.0376437107427137 ) ) ;
#99805=CIRCLE ( 'NONE', #47985, 3.060000000000000053 ) ;
#99818=EDGE_CURVE ( 'NONE', #50118, #96754, #27099, .T. ) ;
#99830=ORIENTED_EDGE ( 'NONE', *, *, #26757, .F. ) ;
#99837=ORIENTED_EDGE ( 'NONE', *, *, #93052, .T. ) ;
#99852=EDGE_CURVE ( 'NONE', #22614, #17829, #84381, .T. ) ;
#99875=VECTOR ( 'NONE', #64253, 1000.000000000000227 ) ;
#99886=FACE_OUTER_BOUND ( 'NONE', #53931, .T. ) ;
#99916=CARTESIAN_POINT ( 'NONE',  ( -24.55517127435777169, -5.965225279485592225, -15.44180958690142802 ) ) ;
#99917=CIRCLE ( 'NONE', #18889, 1.529999999999999805 ) ;
#99967=LINE ( 'NONE', #98476, #15770 ) ;
#99979=CARTESIAN_POINT ( 'NONE',  ( 14.61581670307174008, 6.376774720514426953, -27.35847990810646024 ) ) ;
#99985=DIRECTION ( 'NONE',  ( -1.000000000000000000, -0.000000000000000000, -0.000000000000000000 ) ) ;
#99987=CARTESIAN_POINT ( 'NONE',  ( 30.93860345374796594, -6.475225279485573360, 19.84760796525321780 ) ) ;
#99988=CARTESIAN_POINT ( 'NONE',  ( 14.76093561896379214, -5.965225279485572685, -26.55548769130089681 ) ) ;
#100008=CIRCLE ( 'NONE', #25510, 1.020000000000000018 ) ;
#100010=ORIENTED_EDGE ( 'NONE', *, *, #28603, .T. ) ;
#100013=CIRCLE ( 'NONE', #56326, 1.835999999999999632 ) ;
#100022=VECTOR ( 'NONE', #61093, 1000.000000000000000 ) ;
#100044=CARTESIAN_POINT ( 'NONE',  ( -19.80875734969026425, -5.965225279485572685, 31.02402280011862246 ) ) ;
#100058=ORIENTED_EDGE ( 'NONE', *, *, #92733, .F. ) ;
#100071=DIRECTION ( 'NONE',  ( -0.1254312216594016538, 0.000000000000000000, -0.9921023176230513441 ) ) ;
#100075=CARTESIAN_POINT ( 'NONE',  ( 14.61581670307174008, 6.376774720514426953, -27.35847990810646024 ) ) ;
#100102=ORIENTED_EDGE ( 'NONE', *, *, #88168, .T. ) ;
#100113=ORIENTED_EDGE ( 'NONE', *, *, #97697, .F. ) ;
#100117=ORIENTED_EDGE ( 'NONE', *, *, #28257, .T. ) ;
#100126=ORIENTED_EDGE ( 'NONE', *, *, #90540, .T. ) ;
#100130=CYLINDRICAL_SURFACE ( 'NONE', #48908, 12.65241003308275936 ) ;
#100158=DIRECTION ( 'NONE',  ( -1.000000000000000000, -1.232047923278981953E-16, 0.000000000000000000 ) ) ;
#100177=CARTESIAN_POINT ( 'NONE',  ( 27.53860345374771867, 4.772774720514425972, -9.482392034746240483 ) ) ;
#100189=CARTESIAN_POINT ( 'NONE',  ( -0.02075734969026423599, -5.965225279485572685, -0.08597719988137648983 ) ) ;
#100192=ADVANCED_FACE ( 'NONE', ( #90370 ), #20845, .T. ) ;
#100193=ORIENTED_EDGE ( 'NONE', *, *, #57526, .T. ) ;
#100206=ORIENTED_EDGE ( 'NONE', *, *, #6924, .T. ) ;
#100213=ORIENTED_EDGE ( 'NONE', *, *, #97455, .F. ) ;
#100218=CARTESIAN_POINT ( 'NONE',  ( -20.27875734969026311, -6.143225279485574397, 24.00402280011862288 ) ) ;
#100223=EDGE_CURVE ( 'NONE', #14845, #99263, #7636, .T. ) ;
#100227=VECTOR ( 'NONE', #36298, 1000.000000000000000 ) ;
#100255=AXIS2_PLACEMENT_3D ( 'NONE', #20659, #67358, #6446 ) ;
#100261=CARTESIAN_POINT ( 'NONE',  ( 30.53060340732036337, 4.484642458114688424, -4.073424848557150924 ) ) ;
#100278=CARTESIAN_POINT ( 'NONE',  ( 30.59431191903084013, 4.508530027678929741, 26.46517314890041916 ) ) ;
#100279=EDGE_CURVE ( 'NONE', #13521, #80017, #83750, .T. ) ;
#100283=DIRECTION ( 'NONE',  ( -0.9978940991575084851, -0.000000000000000000, -0.06486421869277853025 ) ) ;
#100285=CARTESIAN_POINT ( 'NONE',  ( -0.02075734969026423599, 3.316774720514426456, -28.03397719988137382 ) ) ;
#100286=CARTESIAN_POINT ( 'NONE',  ( -24.97666371003640506, 0.3587747205143964613, -15.72894043976419454 ) ) ;
#100290=CARTESIAN_POINT ( 'NONE',  ( 31.55302460176084978, 5.360765615368469739, -3.312397695011010335 ) ) ;
#100299=VECTOR ( 'NONE', #89469, 1000.000000000000000 ) ;
#100321=DIRECTION ( 'NONE',  ( 0.000000000000000000, -1.000000000000000000, 0.000000000000000000 ) ) ;
#100360=VECTOR ( 'NONE', #10874, 1000.000000000000000 ) ;
#100367=CARTESIAN_POINT ( 'NONE',  ( 13.43165536947796213, 3.316774720514427344, -28.18099828186571187 ) ) ;
#100380=DIRECTION ( 'NONE',  ( 0.000000000000000000, -0.000000000000000000, -1.000000000000000000 ) ) ;
#100404=EDGE_CURVE ( 'NONE', #78861, #3153, #84079, .T. ) ;
#100408=DIRECTION ( 'NONE',  ( -0.000000000000000000, 1.000000000000000000, -0.000000000000000000 ) ) ;
#100413=ADVANCED_FACE ( 'NONE', ( #32473 ), #93867, .F. ) ;
#100416=FACE_OUTER_BOUND ( 'NONE', #66190, .T. ) ;
#100455=COLOUR_RGB('Slate Gray', 0.72549020, 0.75294118, 0.79215686);
#100456=FILL_AREA_STYLE_COLOUR('',#100455);
#100457=FILL_AREA_STYLE('',(#100456));
#100458=SURFACE_STYLE_FILL_AREA(#100457);
#100459=SURFACE_SIDE_STYLE('',(#100458));
#100460=SURFACE_STYLE_USAGE(.BOTH.,#100459);
#100461=PRESENTATION_STYLE_ASSIGNMENT((#100460));
#100478=STYLED_ITEM('',(#100461),#11338);
#100479=MECHANICAL_DESIGN_GEOMETRIC_PRESENTATION_REPRESENTATION('',(#100478),#11455);
ENDSEC;
END-ISO-10303-21;
